ISO-10303-21;
HEADER;
FILE_DESCRIPTION (('STEP AP214'),
    '1' );
FILE_NAME ('clamping lever.step',
    '2026-10-26T19:46:16',
    ( '' ),
    ( '' ),
    'SwSTEP 2.0',
    'SolidWorks 2025',
    '' );
FILE_SCHEMA (( 'AUTOMOTIVE_DESIGN' ));
ENDSEC;

DATA;
#9=CARTESIAN_POINT ( 'NONE',  ( -7.999999999999991118, 0.000000000000000000, 5.386552784329824206 ) ) ;
#10=CARTESIAN_POINT ( 'NONE',  ( 3.313708498984756279, 7.999999999999991118, 4.861552779823363757 ) ) ;
#15=CIRCLE ( 'NONE', #38546, 16.70329308849007077 ) ;
#16=CARTESIAN_POINT ( 'NONE',  ( 2.977408999572646486, 7.188101187499992051, 28.01780278187175455 ) ) ;
#28=CARTESIAN_POINT ( 'NONE',  ( 1.469576158976822172E-15, -7.999999999999991118, 20.89280278392014623 ) ) ;
#53=CARTESIAN_POINT ( 'NONE',  ( 7.188101187499991163, 2.977408999572648707, 4.205302781871751883 ) ) ;
#67=CARTESIAN_POINT ( 'NONE',  ( 2.977408999572650927, -7.188101187499990274, 0.8303027818717529929 ) ) ;
#86=CARTESIAN_POINT ( 'NONE',  ( -3.313708498984757167, 7.999999999999991118, 23.04905277982336642 ) ) ;
#98=CARTESIAN_POINT ( 'NONE',  ( -7.999999999999991118, 0.000000000000000000, 21.88655278432982243 ) ) ;
#132=CARTESIAN_POINT ( 'NONE',  ( -5.082755093536319713, 5.082755093536319713, 16.29905278187175455 ) ) ;
#156=CARTESIAN_POINT ( 'NONE',  ( -7.188101187499992051, 2.977408999572646930, 18.26780278187175455 ) ) ;
#176=CARTESIAN_POINT ( 'NONE',  ( -5.656854249492373476, -5.656854249492376141, 5.517802779823364645 ) ) ;
#189=CARTESIAN_POINT ( 'NONE',  ( 7.458676001334752392, -2.916525548322098427, -0.000000000000000000 ) ) ;
#203=CARTESIAN_POINT ( 'NONE',  ( -4.903558642999205574E-16, 8.008118988124991233, 12.63811528394063011 ) ) ;
#210=CARTESIAN_POINT ( 'NONE',  ( 5.082755093536320601, -5.082755093536318824, 14.04905278187175455 ) ) ;
#222=CARTESIAN_POINT ( 'NONE',  ( 7.999999999999992895, -3.313708498984756279, 9.174052783920144449 ) ) ;
#236=CARTESIAN_POINT ( 'NONE',  ( -7.188101187499992051, 0.000000000000000000, 15.36155278187175455 ) ) ;
#237=AXIS2_PLACEMENT_3D ( 'NONE', #10666, #63087, #11411 ) ;
#260=CARTESIAN_POINT ( 'NONE',  ( -5.656854249492373476, -5.656854249492376141, 22.01780277982336997 ) ) ;
#279=CARTESIAN_POINT ( 'NONE',  ( 5.656854249492376141, -5.656854249492374365, 13.58030278392014623 ) ) ;
#285=EDGE_CURVE ( 'NONE', #59945, #25965, #51151, .T. ) ;
#310=CARTESIAN_POINT ( 'NONE',  ( -3.313708498984759387, -7.999999999999989342, 19.11155277982337353 ) ) ;
#329=CARTESIAN_POINT ( 'NONE',  ( -2.977408999572648707, -7.188101187499990274, 4.767802781871753659 ) ) ;
#353=CARTESIAN_POINT ( 'NONE',  ( -4.401442555609577197E-16, 7.188101187499992051, 8.986552781871752771 ) ) ;
#356=CARTESIAN_POINT ( 'NONE',  ( 7.999999999999991118, 3.313708498984757611, 1.730302784329821320 ) ) ;
#366=CARTESIAN_POINT ( 'NONE',  ( 5.656854249492374365, 5.656854249492375253, 1.767802779823364423 ) ) ;
#381=CARTESIAN_POINT ( 'NONE',  ( 3.313708498984762496, -7.999999999999989342, 7.355302784329823318 ) ) ;
#388=CARTESIAN_POINT ( 'NONE',  ( 1.320432766682872962E-15, -7.188101187499992051, 24.36155278187175810 ) ) ;
#402=CARTESIAN_POINT ( 'NONE',  ( 5.656854249492374365, 5.656854249492375253, 19.95530278392014623 ) ) ;
#411=CARTESIAN_POINT ( 'NONE',  ( 7.188101187499993827, -2.977408999572645598, 24.64280278187176165 ) ) ;
#425=CARTESIAN_POINT ( 'NONE',  ( 2.977408999572650927, -7.188101187499990274, 0.8303027818717529929 ) ) ;
#429=CARTESIAN_POINT ( 'NONE',  ( -3.317071493978880348, -8.008118988124989457, 5.794365283940630995 ) ) ;
#433=CARTESIAN_POINT ( 'NONE',  ( -5.656854249492373476, -5.656854249492376141, 7.017802779823365533 ) ) ;
#436=CARTESIAN_POINT ( 'NONE',  ( 5.082755093536318824, 5.082755093536319713, 25.29905278187175810 ) ) ;
#454=CARTESIAN_POINT ( 'NONE',  ( 7.999999999999991118, 9.797174393178815797E-16, 22.58030277982336997 ) ) ;
#467=CARTESIAN_POINT ( 'NONE',  ( 7.999999999999992895, -3.313708498984756279, 24.04280278432983309 ) ) ;
#471=VERTEX_POINT ( 'NONE', #17185 ) ;
#489=( BOUNDED_CURVE ( )  B_SPLINE_CURVE ( 2, ( #5942, #35723, #28941, #1035, #12332, #51960, #24015, #40634, #63634 ),
 .UNSPECIFIED., .F., .F. ) 
 B_SPLINE_CURVE_WITH_KNOTS ( ( 3, 2, 2, 2, 3 ),
 ( 0.5824082574719842142, 0.5890265270166560319, 0.5956448026011128549, 0.6022630781855697890, 0.6088813560782819767 ),
 .UNSPECIFIED. ) 
 CURVE ( )  GEOMETRIC_REPRESENTATION_ITEM ( )  RATIONAL_B_SPLINE_CURVE ( ( 1.000000000000000000, 0.9238795325112867385, 1.000000000000000000, 0.9238795325112867385, 1.000000000000000000, 0.9238795325112867385, 1.000000000000000000, 0.9238795325112867385, 1.000000000000000000 ) ) 
 REPRESENTATION_ITEM ( '' )  );
#499=CARTESIAN_POINT ( 'NONE',  ( 7.188101187499993827, -2.977408999572645598, 11.14280278187175810 ) ) ;
#522=CARTESIAN_POINT ( 'NONE',  ( 2.977408999572650927, -7.188101187499990274, 12.83030278187175277 ) ) ;
#526=CARTESIAN_POINT ( 'NONE',  ( -7.999999999999991118, 0.000000000000000000, 24.83030277982336642 ) ) ;
#527=ORIENTED_EDGE ( 'NONE', *, *, #13294, .T. ) ;
#542=CARTESIAN_POINT ( 'NONE',  ( 7.999999999999991118, 9.797174393178815797E-16, 1.580302779823364201 ) ) ;
#546=CARTESIAN_POINT ( 'NONE',  ( -7.999999999999948486, 3.313708498984799355, 11.23655277982336642 ) ) ;
#565=ORIENTED_EDGE ( 'NONE', *, *, #46470, .T. ) ;
#568=CARTESIAN_POINT ( 'NONE',  ( -3.317071493978878571, 8.008118988124991233, 17.23186528394063188 ) ) ;
#571=ADVANCED_FACE ( 'NONE', ( #36403 ), #25054, .F. ) ;
#576=CARTESIAN_POINT ( 'NONE',  ( 5.082755093536320601, -5.082755093536318824, 11.04905278187175455 ) ) ;
#585=EDGE_CURVE ( 'NONE', #64535, #11426, #41555, .T. ) ;
#589=CARTESIAN_POINT ( 'NONE',  ( 3.313708498984762496, -7.999999999999989342, 8.986552783920146226 ) ) ;
#606=CARTESIAN_POINT ( 'NONE',  ( -7.188101187499990274, -2.977408999572651371, 19.95530278187175810 ) ) ;
#632=CARTESIAN_POINT ( 'NONE',  ( -4.898587196589407898E-16, 7.999999999999991118, 19.95530277982336642 ) ) ;
#650=CARTESIAN_POINT ( 'NONE',  ( -3.313708498984757167, 7.999999999999991118, 5.236552783920145338 ) ) ;
#699=CARTESIAN_POINT ( 'NONE',  ( -2.977408999572647819, 7.188101187499991163, 5.705302781871753659 ) ) ;
#723=CARTESIAN_POINT ( 'NONE',  ( 7.188101187499993827, -2.977408999572645598, 10.01780278187175632 ) ) ;
#727=CARTESIAN_POINT ( 'NONE',  ( -5.656854249492373476, -5.656854249492376141, 1.074052784329823984 ) ) ;
#737=CARTESIAN_POINT ( 'NONE',  ( 3.313708498984762496, -7.999999999999989342, 22.48655278392014623 ) ) ;
#738=DIRECTION ( 'NONE',  ( 0.000000000000000000, 0.2588190451025140781, -0.9659258262890700886 ) ) ;
#758=CARTESIAN_POINT ( 'NONE',  ( -7.188101187499990274, -2.977408999572651815, 25.58030278187175455 ) ) ;
#769=CARTESIAN_POINT ( 'NONE',  ( -7.999999999999991118, 3.313708498984756723, 18.92405278392014978 ) ) ;
#771=ORIENTED_EDGE ( 'NONE', *, *, #45418, .F. ) ;
#779=AXIS2_PLACEMENT_3D ( 'NONE', #50257, #71768, #60455 ) ;
#780=CARTESIAN_POINT ( 'NONE',  ( 7.188101187499992051, 8.802885111219154394E-16, 21.73655278187175455 ) ) ;
#798=CARTESIAN_POINT ( 'NONE',  ( -8.008118988124989457, -3.317071493978883900, 2.606865283940627886 ) ) ;
#804=CARTESIAN_POINT ( 'NONE',  ( -5.082755093536319713, 5.082755093536319713, 27.17405278187175455 ) ) ;
#822=CARTESIAN_POINT ( 'NONE',  ( -4.898587196589407898E-16, 7.999999999999991118, 21.45530277982336642 ) ) ;
#837=CARTESIAN_POINT ( 'NONE',  ( 7.999999999999991118, 3.313708498984757611, 22.73030278432982598 ) ) ;
#848=ADVANCED_FACE ( 'NONE', ( #30384 ), #19058, .F. ) ;
#852=VERTEX_POINT ( 'NONE', #71097 ) ;
#860=CARTESIAN_POINT ( 'NONE',  ( -4.898587196589407898E-16, 7.999999999999991118, 12.64280278392014623 ) ) ;
#861=EDGE_LOOP ( 'NONE', ( #74104, #6053, #73709, #24682 ) ) ;
#869=CARTESIAN_POINT ( 'NONE',  ( -7.188101187499992051, 0.000000000000000000, 11.98655278187175277 ) ) ;
#871=EDGE_LOOP ( 'NONE', ( #7452, #65352, #2298, #33672 ) ) ;
#893=CARTESIAN_POINT ( 'NONE',  ( -2.977408999572647819, 7.188101187499992051, 10.58030278187175455 ) ) ;
#905=DIRECTION ( 'NONE',  ( 1.000000000000000000, 0.000000000000000000, 0.000000000000000000 ) ) ;
#941=CARTESIAN_POINT ( 'NONE',  ( 3.317071493978877683, 8.008118988124991233, 17.04436528394063188 ) ) ;
#946=CARTESIAN_POINT ( 'NONE',  ( -5.082755093536317936, -5.082755093536320601, 10.67405278187175455 ) ) ;
#950=( BOUNDED_CURVE ( )  B_SPLINE_CURVE ( 2, ( #55035, #25590, #9002, #49353, #9376, #32395, #72371, #19562, #36927, #14266, #65590, #13888, #20681 ),
 .UNSPECIFIED., .F., .F. ) 
 B_SPLINE_CURVE_WITH_KNOTS ( ( 3, 2, 2, 2, 2, 2, 3 ),
 ( 0.3176771498271482308, 0.3176772280539318372, 0.3242955036383868839, 0.3309137792228418751, 0.3375320548072968108, 0.3441503303917518020, 0.3441504249343935173 ),
 .UNSPECIFIED. ) 
 CURVE ( )  GEOMETRIC_REPRESENTATION_ITEM ( )  RATIONAL_B_SPLINE_CURVE ( ( 0.9999982005617984449, 0.9999991002702646181, 1.000000000000000000, 0.9238795325112867385, 1.000000000000000000, 0.9238795325112867385, 1.000000000000000000, 0.9238795325112867385, 1.000000000000000000, 0.9238795325112867385, 1.000000000000000000, 0.9999989126125087280, 0.9999978252560842718 ) ) 
 REPRESENTATION_ITEM ( '' )  );
#960=CARTESIAN_POINT ( 'NONE',  ( 1.469576158976822172E-15, -7.999999999999991118, 2.892802783920144005 ) ) ;
#975=CARTESIAN_POINT ( 'NONE',  ( 5.082755093536318824, 5.082755093536319713, 19.29905278187175455 ) ) ;
#1000=CARTESIAN_POINT ( 'NONE',  ( 7.999999999999991118, 9.797174393178815797E-16, 15.08030277982336642 ) ) ;
#1012=DIRECTION ( 'NONE',  ( -0.000000000000000000, -0.000000000000000000, 1.000000000000000000 ) ) ;
#1018=CARTESIAN_POINT ( 'NONE',  ( -3.313708498984758943, -7.999999999999989342, 7.299052783920144449 ) ) ;
#1035=CARTESIAN_POINT ( 'NONE',  ( -3.313708498984757611, 7.999999999999991118, 11.23655278392014445 ) ) ;
#1067=CARTESIAN_POINT ( 'NONE',  ( -7.188101187499992051, 0.000000000000000000, 5.986552781871753659 ) ) ;
#1091=CARTESIAN_POINT ( 'NONE',  ( -4.401442555609577197E-16, 7.188101187499992051, 11.98655278187175632 ) ) ;
#1094=CARTESIAN_POINT ( 'NONE',  ( -5.867873826482948196, -5.445834672501801421, -0.4343901754555773431 ) ) ;
#1105=CARTESIAN_POINT ( 'NONE',  ( 3.313708498984762496, -7.999999999999989342, 25.48655278392014623 ) ) ;
#1126=CARTESIAN_POINT ( 'NONE',  ( 2.977408999572646486, 7.188101187499992051, 26.51780278187175455 ) ) ;
#1134=CARTESIAN_POINT ( 'NONE',  ( -5.656854249492373476, -5.656854249492376141, 22.20530278392014623 ) ) ;
#1138=LINE ( 'NONE', #36196, #1728 ) ;
#1145=CARTESIAN_POINT ( 'NONE',  ( -4.401442555609577197E-16, 7.188101187499992051, 26.61155278187175455 ) ) ;
#1161=ADVANCED_FACE ( 'NONE', ( #45741 ), #17816, .F. ) ;
#1164=CARTESIAN_POINT ( 'NONE',  ( -5.662595241051933570, -5.662595241051936235, 4.200615283940629219 ) ) ;
#1187=CARTESIAN_POINT ( 'NONE',  ( -7.999999999999991118, 0.000000000000000000, 15.83030277982336642 ) ) ;
#1202=CARTESIAN_POINT ( 'NONE',  ( -5.656854249492373476, -5.656854249492376141, 16.07405278432982954 ) ) ;
#1236=CARTESIAN_POINT ( 'NONE',  ( 2.977408999572650927, -7.188101187499990274, 12.45530278187175277 ) ) ;
#1238=EDGE_CURVE ( 'NONE', #27473, #33233, #43075, .T. ) ;
#1239=VERTEX_POINT ( 'NONE', #43744 ) ;
#1260=CARTESIAN_POINT ( 'NONE',  ( -2.977408999572647819, 7.188101187499992051, 12.08030278187175277 ) ) ;
#1292=CARTESIAN_POINT ( 'NONE',  ( 3.313708498984756279, 7.999999999999991118, 9.361552779823366421 ) ) ;
#1306=CARTESIAN_POINT ( 'NONE',  ( 3.317071493978877683, 8.008118988124991233, 12.54436528394063011 ) ) ;
#1312=CARTESIAN_POINT ( 'NONE',  ( 7.188101187499993827, -2.977408999572645598, 11.14280278187175455 ) ) ;
#1326=CARTESIAN_POINT ( 'NONE',  ( -3.313708498984757167, 7.999999999999991118, 0.7365527839201455595 ) ) ;
#1342=CARTESIAN_POINT ( 'NONE',  ( -4.401442555609577197E-16, 7.188101187499992051, 14.98655278187175455 ) ) ;
#1350=CARTESIAN_POINT ( 'NONE',  ( 1.320432766682872962E-15, -7.188101187499992051, 27.73655278187175455 ) ) ;
#1359=CARTESIAN_POINT ( 'NONE',  ( 5.656854249492376141, -5.656854249492374365, 25.39280277982336642 ) ) ;
#1367=CARTESIAN_POINT ( 'NONE',  ( -5.656854249492375253, 5.656854249492375253, 14.14280277982336465 ) ) ;
#1386=CARTESIAN_POINT ( 'NONE',  ( -7.999999999999991118, 3.313708498984756723, 6.924052783920144449 ) ) ;
#1425=VECTOR ( 'NONE', #22117, 1000.000000000000000 ) ;
#1438=CARTESIAN_POINT ( 'NONE',  ( -5.082755093536317936, -5.082755093536320601, 9.174052781871752771 ) ) ;
#1440=ORIENTED_EDGE ( 'NONE', *, *, #10946, .F. ) ;
#1462=CARTESIAN_POINT ( 'NONE',  ( -4.401442555609577197E-16, 7.188101187499992051, 5.986552781871753659 ) ) ;
#1475=CARTESIAN_POINT ( 'NONE',  ( -7.999999999999989342, -3.313708498984762496, 26.61155278392014978 ) ) ;
#1498=CARTESIAN_POINT ( 'NONE',  ( 7.188101187499992051, 2.977408999572647819, 23.33030278187175455 ) ) ;
#1510=CARTESIAN_POINT ( 'NONE',  ( -7.999999999999989342, -3.313708498984762496, 17.61155278392014623 ) ) ;
#1522=CARTESIAN_POINT ( 'NONE',  ( 7.188101187499991163, 2.977408999572648707, 24.83030278187175455 ) ) ;
#1536=CARTESIAN_POINT ( 'NONE',  ( -8.008118988124989457, -3.317071493978883900, 1.106865283940629885 ) ) ;
#1543=CARTESIAN_POINT ( 'NONE',  ( -2.977408999572647819, 7.188101187499991163, 19.58030278187175455 ) ) ;
#1560=CARTESIAN_POINT ( 'NONE',  ( -7.999999999999991118, 0.000000000000000000, 14.33030277982336465 ) ) ;
#1572=DIRECTION ( 'NONE',  ( 0.000000000000000000, 0.2588190451025140781, -0.9659258262890700886 ) ) ;
#1573=CARTESIAN_POINT ( 'NONE',  ( -3.313708498984758943, -7.999999999999989342, 16.16780278432982598 ) ) ;
#1602=CARTESIAN_POINT ( 'NONE',  ( 5.082755093536318824, 5.082755093536319713, 15.92405278187175632 ) ) ;
#1626=CARTESIAN_POINT ( 'NONE',  ( -7.188101187499992051, 0.000000000000000000, 12.36155278187175277 ) ) ;
#1631=CARTESIAN_POINT ( 'NONE',  ( -3.313708498984757611, 7.999999999999991118, 3.736552783920145338 ) ) ;
#1640=CARTESIAN_POINT ( 'NONE',  ( -7.999999999999991118, 9.797174393178815797E-16, 30.00000000000000000 ) ) ;
#1656=FACE_OUTER_BOUND ( 'NONE', #38500, .T. ) ;
#1671=CARTESIAN_POINT ( 'NONE',  ( 3.317071493978877683, 8.008118988124991233, 11.04436528394063366 ) ) ;
#1676=CARTESIAN_POINT ( 'NONE',  ( -2.977408999572647819, -7.188101187499990274, 7.767802781871751883 ) ) ;
#1691=CARTESIAN_POINT ( 'NONE',  ( -4.898587196589407898E-16, 7.999999999999991118, 2.142802783920143117 ) ) ;
#1707=CARTESIAN_POINT ( 'NONE',  ( 2.977408999572646486, 7.188101187499991163, 10.39280278187175810 ) ) ;
#1709=CARTESIAN_POINT ( 'NONE',  ( -5.656854249492375253, 5.656854249492375253, 3.642802779823362869 ) ) ;
#1712=CARTESIAN_POINT ( 'NONE',  ( 1.469576158976822172E-15, -7.999999999999991118, 19.39280278392014978 ) ) ;
#1716=CARTESIAN_POINT ( 'NONE',  ( 2.977408999572646486, 7.188101187499992051, 26.89280278187175455 ) ) ;
#1722=ORIENTED_EDGE ( 'NONE', *, *, #33764, .F. ) ;
#1728=VECTOR ( 'NONE', #41845, 1000.000000000000000 ) ;
#1731=CARTESIAN_POINT ( 'NONE',  ( 7.999999999999992895, -3.313708498984756279, 13.67405278392014800 ) ) ;
#1732=CARTESIAN_POINT ( 'NONE',  ( -7.999999999999991118, 3.313708498984756723, 12.73655277982336287 ) ) ;
#1740=ORIENTED_EDGE ( 'NONE', *, *, #19433, .T. ) ;
#1782=CARTESIAN_POINT ( 'NONE',  ( -3.313708498984757611, 7.999999999999991118, 6.549052779823365533 ) ) ;
#1790=CARTESIAN_POINT ( 'NONE',  ( 2.977408999572650927, -7.188101187499990274, 1.955302781871753881 ) ) ;
#1814=CARTESIAN_POINT ( 'NONE',  ( 2.977408999572646486, 7.188101187499991163, 2.892802781871751439 ) ) ;
#1829=CARTESIAN_POINT ( 'NONE',  ( -5.656854249492375253, 5.656854249492375253, 27.83030278392014978 ) ) ;
#1848=ORIENTED_EDGE ( 'NONE', *, *, #40554, .F. ) ;
#1850=CARTESIAN_POINT ( 'NONE',  ( -7.188101187499992051, 0.000000000000000000, 20.98655278187175455 ) ) ;
#1858=CARTESIAN_POINT ( 'NONE',  ( -7.999999999999991118, 3.313708498984756723, 12.92405278392014800 ) ) ;
#1870=CARTESIAN_POINT ( 'NONE',  ( -7.188101187499990274, -2.977408999572651371, 27.08030278187175810 ) ) ;
#1886=CARTESIAN_POINT ( 'NONE',  ( 3.317071493978883456, -8.008118988124989457, 5.981865283940630995 ) ) ;
#1892=CARTESIAN_POINT ( 'NONE',  ( -7.188101187499992051, 0.000000000000000000, 24.36155278187175810 ) ) ;
#1910=CARTESIAN_POINT ( 'NONE',  ( -3.313708498984758943, -7.999999999999989342, 14.61155277982336465 ) ) ;
#1925=CARTESIAN_POINT ( 'NONE',  ( -7.999999999999991118, 0.000000000000000000, 15.88655278432982776 ) ) ;
#1948=EDGE_LOOP ( 'NONE', ( #65152, #64749, #21103, #7580, #48981, #52895, #23273, #15632, #6768, #23054, #10594, #55276, #74576, #29728, #47741, #59446, #66811, #18384, #2114, #41930, #66850, #47110, #57660, #37417, #41912, #30625, #21531, #43796, #16201, #22550, #33624, #68574, #58484, #50377, #39556, #3342, #36108, #62978, #39030, #73499, #59739, #15430, #24758 ) ) ;
#1956=CARTESIAN_POINT ( 'NONE',  ( -7.188101187499990274, -2.977408999572651371, 12.08030278187175099 ) ) ;
#1978=CARTESIAN_POINT ( 'NONE',  ( 5.082755093536320601, -5.082755093536318824, 8.424052781871752771 ) ) ;
#2026=CARTESIAN_POINT ( 'NONE',  ( 3.317071493978877683, 8.008118988124991233, 6.544365283940627442 ) ) ;
#2032=CARTESIAN_POINT ( 'NONE',  ( 7.188101187499992051, 8.802885111219154394E-16, 9.736552781871754547 ) ) ;
#2045=CARTESIAN_POINT ( 'NONE',  ( -7.999999999999989342, -3.313708498984762496, 4.111552783920145338 ) ) ;
#2066=CARTESIAN_POINT ( 'NONE',  ( -7.999999999999991118, 0.000000000000000000, 5.330302779823363757 ) ) ;
#2067=CARTESIAN_POINT ( 'NONE',  ( 7.188101187499992051, 2.977408999572647819, 28.20530278187175810 ) ) ;
#2069=CYLINDRICAL_SURFACE ( 'NONE', #18024, 7.999999999999991118 ) ;
#2085=CARTESIAN_POINT ( 'NONE',  ( 7.999999999999991118, 9.797174393178815797E-16, 16.58030277982336287 ) ) ;
#2102=CARTESIAN_POINT ( 'NONE',  ( 7.999999999999991118, 3.313708498984758055, 6.361552783920146226 ) ) ;
#2114=ORIENTED_EDGE ( 'NONE', *, *, #17459, .T. ) ;
#2116=CARTESIAN_POINT ( 'NONE',  ( 1.471067592899761672E-15, -8.008118988124991233, 23.88811528394063188 ) ) ;
#2151=CARTESIAN_POINT ( 'NONE',  ( -5.082755093536319713, 5.082755093536319713, 27.17405278187175455 ) ) ;
#2175=CARTESIAN_POINT ( 'NONE',  ( -2.977408999572647819, 7.188101187499991163, 1.580302781871753437 ) ) ;
#2190=CARTESIAN_POINT ( 'NONE',  ( -7.999999999999991118, 0.000000000000000000, 25.01780278392014978 ) ) ;
#2192=CARTESIAN_POINT ( 'NONE',  ( -7.999999999999991118, 0.000000000000000000, 29.09592778084756048 ) ) ;
#2213=CARTESIAN_POINT ( 'NONE',  ( 1.320432766682872962E-15, -7.188101187499992051, 21.36155278187175455 ) ) ;
#2221=CARTESIAN_POINT ( 'NONE',  ( 5.656854249492374365, 5.656854249492375253, 13.95530278392014623 ) ) ;
#2232=CARTESIAN_POINT ( 'NONE',  ( 7.188101187499992051, 8.802885111219154394E-16, 17.23655278187175810 ) ) ;
#2246=CARTESIAN_POINT ( 'NONE',  ( 7.999999999999991118, 9.797174393178815797E-16, 25.58030277982336997 ) ) ;
#2252=CARTESIAN_POINT ( 'NONE',  ( 1.469576158976822172E-15, -7.999999999999991118, 25.39280278392014978 ) ) ;
#2258=CARTESIAN_POINT ( 'NONE',  ( 7.188101187499992051, 8.802885111219154394E-16, 23.61155278187175455 ) ) ;
#2275=CARTESIAN_POINT ( 'NONE',  ( 7.999999999999992895, -3.313708498984756279, 16.48655277982336642 ) ) ;
#2288=CARTESIAN_POINT ( 'NONE',  ( 7.999999999999991118, 9.797174393178815797E-16, 15.13655278432982421 ) ) ;
#2298=ORIENTED_EDGE ( 'NONE', *, *, #34648, .T. ) ;
#2321=CARTESIAN_POINT ( 'NONE',  ( 2.977408999572646486, 7.188101187499991163, 5.517802781871753659 ) ) ;
#2347=CARTESIAN_POINT ( 'NONE',  ( 7.188101187499992051, 2.977408999572647819, 2.705302781871750994 ) ) ;
#2352=CARTESIAN_POINT ( 'NONE',  ( -7.999999999999991118, 0.000000000000000000, 4.017802783920145338 ) ) ;
#2369=CARTESIAN_POINT ( 'NONE',  ( -3.313708498984759387, -7.999999999999989342, 23.61155277982336997 ) ) ;
#2388=CARTESIAN_POINT ( 'NONE',  ( 7.999999999999991118, 9.797174393178815797E-16, 13.58030277982336465 ) ) ;
#2390=CARTESIAN_POINT ( 'NONE',  ( 8.008118988124991233, 3.317071493978879015, 9.356865283940631883 ) ) ;
#2398=CARTESIAN_POINT ( 'NONE',  ( 7.188101187499992051, 8.802885111219154394E-16, 0.7365527818717527708 ) ) ;
#2414=CARTESIAN_POINT ( 'NONE',  ( -5.082755093536319713, 5.082755093536319713, 28.29905278187175810 ) ) ;
#2457=CARTESIAN_POINT ( 'NONE',  ( 7.999999999999991118, 3.313708498984757611, 12.17405277982336642 ) ) ;
#2477=ORIENTED_EDGE ( 'NONE', *, *, #61577, .F. ) ;
#2487=CARTESIAN_POINT ( 'NONE',  ( 3.317071493978877683, 8.008118988124991233, 27.54436528394063188 ) ) ;
#2507=FACE_OUTER_BOUND ( 'NONE', #40414, .T. ) ;
#2511=CARTESIAN_POINT ( 'NONE',  ( 7.999999999996472155, 7.505344305739403062E-06, 9.267802996260090964 ) ) ;
#2520=ORIENTED_EDGE ( 'NONE', *, *, #40133, .F. ) ;
#2523=CARTESIAN_POINT ( 'NONE',  ( 5.082755093536320601, -5.082755093536318824, 27.92405278187175455 ) ) ;
#2548=CARTESIAN_POINT ( 'NONE',  ( -2.977408999572648707, -7.188101187499990274, 2.142802781871754103 ) ) ;
#2566=CARTESIAN_POINT ( 'NONE',  ( -3.313708498984758943, -7.999999999999989342, 20.79905278392014978 ) ) ;
#2589=CARTESIAN_POINT ( 'NONE',  ( 1.320432766682872962E-15, -7.188101187499992051, 18.36155278187175455 ) ) ;
#2593=VERTEX_POINT ( 'NONE', #73922 ) ;
#2599=CARTESIAN_POINT ( 'NONE',  ( 1.469576158976822172E-15, -7.999999999999991118, 14.89280278392014623 ) ) ;
#2601=AXIS2_PLACEMENT_3D ( 'NONE', #6625, #11534, #40202 ) ;
#2611=CARTESIAN_POINT ( 'NONE',  ( -5.082755093536317936, -5.082755093536320601, 19.67405278187175455 ) ) ;
#2629=CARTESIAN_POINT ( 'NONE',  ( 8.008118988124991233, 9.807117285998411148E-16, 0.2631152839406289967 ) ) ;
#2636=CARTESIAN_POINT ( 'NONE',  ( 5.082755093536320601, -5.082755093536318824, 20.42405278187175810 ) ) ;
#2651=CARTESIAN_POINT ( 'NONE',  ( -7.999999999999989342, -3.313708498984762496, 6.924052779823366421 ) ) ;
#2664=CARTESIAN_POINT ( 'NONE',  ( -3.313708498984757167, 7.999999999999991118, 18.60530278432982598 ) ) ;
#2692=DIRECTION ( 'NONE',  ( 1.000000000000000000, 0.000000000000000000, 0.000000000000000000 ) ) ;
#2697=CARTESIAN_POINT ( 'NONE',  ( 2.977408999572650927, -7.188101187499990274, 7.955302781871752771 ) ) ;
#2720=CARTESIAN_POINT ( 'NONE',  ( 1.320432766682872962E-15, -7.188101187499992051, 3.736552781871751883 ) ) ;
#2722=DIRECTION ( 'NONE',  ( 1.000000000000000000, 0.000000000000000000, 0.000000000000000000 ) ) ;
#2726=DIRECTION ( 'NONE',  ( 1.000000000000000000, 0.000000000000000000, 0.000000000000000000 ) ) ;
#2739=EDGE_CURVE ( 'NONE', #69617, #51761, #46584, .T. ) ;
#2747=ORIENTED_EDGE ( 'NONE', *, *, #2739, .F. ) ;
#2750=CARTESIAN_POINT ( 'NONE',  ( 7.999999999999991118, 9.797174393178815797E-16, 4.767802783920145338 ) ) ;
#2752=DIRECTION ( 'NONE',  ( 0.000000000000000000, 0.9659258262890700886, 0.2588190451025146888 ) ) ;
#2768=CARTESIAN_POINT ( 'NONE',  ( 8.008118988124991233, 9.807117285998411148E-16, 9.263115283940630107 ) ) ;
#2775=CARTESIAN_POINT ( 'NONE',  ( 2.977408999572650927, -7.188101187499990274, 3.455302781871751883 ) ) ;
#2787=CARTESIAN_POINT ( 'NONE',  ( 2.977408999572650927, -7.188101187499990274, 27.45530278187175810 ) ) ;
#2792=CARTESIAN_POINT ( 'NONE',  ( 4.041179811480690276, 6.985140028428005188, 0.000000000000000000 ) ) ;
#2811=CARTESIAN_POINT ( 'NONE',  ( -2.977408999572647819, 7.188101187499992051, 25.58030278187175455 ) ) ;
#2827=CARTESIAN_POINT ( 'NONE',  ( 7.999999999999992895, -3.313708498984756279, 11.98655277982336997 ) ) ;
#2829=CARTESIAN_POINT ( 'NONE',  ( -5.908781966428503729, -5.087229025050659104, 0.8834915628530353171 ) ) ;
#2836=EDGE_CURVE ( 'NONE', #73226, #26236, #69233, .T. ) ;
#2856=EDGE_LOOP ( 'NONE', ( #15865, #18406, #15269, #67416 ) ) ;
#2858=CARTESIAN_POINT ( 'NONE',  ( -3.317071493978878571, 8.008118988124991233, 26.23186528394063188 ) ) ;
#2877=DIRECTION ( 'NONE',  ( 1.000000000000000000, -0.000000000000000000, 0.000000000000000000 ) ) ;
#2892=CARTESIAN_POINT ( 'NONE',  ( 7.188101187499992051, 8.802885111219154394E-16, 0.7365527818717527708 ) ) ;
#2895=DIRECTION ( 'NONE',  ( 1.000000000000000000, 0.000000000000000000, 0.000000000000000000 ) ) ;
#2919=CARTESIAN_POINT ( 'NONE',  ( 2.977408999572650927, -7.188101187499990274, 6.830302781871755435 ) ) ;
#2937=CARTESIAN_POINT ( 'NONE',  ( -7.999999999999991118, 0.000000000000000000, 17.51780278392014623 ) ) ;
#2953=CARTESIAN_POINT ( 'NONE',  ( -5.656854249492373476, -5.656854249492376141, 11.70530278392014445 ) ) ;
#2959=CARTESIAN_POINT ( 'NONE',  ( -5.082755093536319713, 5.082755093536319713, 20.79905278187175455 ) ) ;
#2968=CARTESIAN_POINT ( 'NONE',  ( -5.656854249492375253, 5.656854249492375253, 14.33030278392014800 ) ) ;
#2979=CARTESIAN_POINT ( 'NONE',  ( -7.188101187499990274, -2.977408999572651371, 18.08030278187175455 ) ) ;
#2980=ORIENTED_EDGE ( 'NONE', *, *, #7143, .F. ) ;
#2984=CARTESIAN_POINT ( 'NONE',  ( -5.656854249492373476, -5.656854249492376141, 5.705302783920146226 ) ) ;
#2999=CARTESIAN_POINT ( 'NONE',  ( -7.999999999999991118, 3.313708498984756723, 27.92405278392015333 ) ) ;
#3006=CARTESIAN_POINT ( 'NONE',  ( -4.401442555609577197E-16, 7.188101187499992051, 20.98655278187175455 ) ) ;
#3020=CARTESIAN_POINT ( 'NONE',  ( 3.313708498984756279, 7.999999999999991118, 7.861552779823362869 ) ) ;
#3039=CARTESIAN_POINT ( 'NONE',  ( 5.656854249492374365, 5.656854249492375253, 10.82405278432982598 ) ) ;
#3052=ORIENTED_EDGE ( 'NONE', *, *, #19188, .T. ) ;
#3070=CARTESIAN_POINT ( 'NONE',  ( 1.320432766682872962E-15, -7.188101187499992051, 6.361552781871754547 ) ) ;
#3071=EDGE_LOOP ( 'NONE', ( #40009, #63604, #12298, #27396 ) ) ;
#3083=CARTESIAN_POINT ( 'NONE',  ( 7.188101187499993827, -2.977408999572645598, 10.01780278187175632 ) ) ;
#3096=CARTESIAN_POINT ( 'NONE',  ( -5.082755093536319713, 5.082755093536319713, 7.674052781871751883 ) ) ;
#3113=CARTESIAN_POINT ( 'NONE',  ( 1.469576158976822172E-15, -7.999999999999991118, 26.70530277982336642 ) ) ;
#3119=CARTESIAN_POINT ( 'NONE',  ( 5.656854249492376141, -5.656854249492374365, 25.58030278392014978 ) ) ;
#3127=CARTESIAN_POINT ( 'NONE',  ( 3.313708498984756279, 7.999999999999991118, 5.049052783920146226 ) ) ;
#3144=CARTESIAN_POINT ( 'NONE',  ( -5.662595241051933570, -5.662595241051936235, 8.700615283940630107 ) ) ;
#3149=CARTESIAN_POINT ( 'NONE',  ( 2.977408999572646486, 7.188101187499992051, 5.517802781871753659 ) ) ;
#3160=CARTESIAN_POINT ( 'NONE',  ( 5.656854249492376141, -5.656854249492374365, 10.39280277982336465 ) ) ;
#3161=CARTESIAN_POINT ( 'NONE',  ( 5.082755093536320601, -5.082755093536318824, 26.04905278187175810 ) ) ;
#3180=CARTESIAN_POINT ( 'NONE',  ( -7.999994399014834556, 3.313714099969915505, 24.92405255982296808 ) ) ;
#3181=CARTESIAN_POINT ( 'NONE',  ( 7.999999999999991118, 9.797174393178815797E-16, 22.58030277982336997 ) ) ;
#3187=CARTESIAN_POINT ( 'NONE',  ( 5.082755093536320601, -5.082755093536318824, 20.42405278187175810 ) ) ;
#3189=CARTESIAN_POINT ( 'NONE',  ( 5.656854249492376141, -5.656854249492374365, 22.58030278392014623 ) ) ;
#3205=CARTESIAN_POINT ( 'NONE',  ( -7.999999999999991118, 3.313708498984756723, 11.23655277982336820 ) ) ;
#3214=CARTESIAN_POINT ( 'NONE',  ( -7.999999999961182162, -1.665870058181487338E-05, 5.518425684709454160 ) ) ;
#3257=CARTESIAN_POINT ( 'NONE',  ( 1.469576158976822172E-15, -7.999999999999991118, 8.892802783920146226 ) ) ;
#3266=VERTEX_POINT ( 'NONE', #45914 ) ;
#3268=CARTESIAN_POINT ( 'NONE',  ( -4.401442555609577197E-16, 7.188101187499992051, 26.98655278187175455 ) ) ;
#3270=DIRECTION ( 'NONE',  ( 1.000000000000000000, 0.000000000000000000, 0.000000000000000000 ) ) ;
#3281=ORIENTED_EDGE ( 'NONE', *, *, #19126, .T. ) ;
#3294=CARTESIAN_POINT ( 'NONE',  ( -7.999999999999991118, 3.313708498984756723, 27.73655277982336642 ) ) ;
#3311=CARTESIAN_POINT ( 'NONE',  ( 7.999999999999991118, 9.797174393178815797E-16, 19.76780278392014623 ) ) ;
#3314=CARTESIAN_POINT ( 'NONE',  ( 7.999999999999992895, -9.797174393178815797E-16, 0.000000000000000000 ) ) ;
#3332=CARTESIAN_POINT ( 'NONE',  ( 7.188101187499993827, -2.977408999572645598, 12.64280278187175277 ) ) ;
#3341=CARTESIAN_POINT ( 'NONE',  ( -7.999999999999991118, 0.000000000000000000, 11.51780278392014445 ) ) ;
#3342=ORIENTED_EDGE ( 'NONE', *, *, #46210, .T. ) ;
#3353=CARTESIAN_POINT ( 'NONE',  ( 2.977408999572646486, 7.188101187499991163, 19.01780278187175810 ) ) ;
#3372=CARTESIAN_POINT ( 'NONE',  ( -3.313708498984758943, -7.999999999999989342, 26.79905278392014623 ) ) ;
#3379=CARTESIAN_POINT ( 'NONE',  ( -5.082755093536319713, 5.082755093536319713, 13.67405278187175455 ) ) ;
#3387=CARTESIAN_POINT ( 'NONE',  ( 8.000000000000012434, 3.313708498984737183, 18.17405277982336997 ) ) ;
#3396=CARTESIAN_POINT ( 'NONE',  ( 7.999999999999991118, 3.313708498984757611, 12.17405277982336642 ) ) ;
#3409=CARTESIAN_POINT ( 'NONE',  ( -7.999985422794280154, -3.313723076190473016, 2.611553367158739647 ) ) ;
#3412=CARTESIAN_POINT ( 'NONE',  ( -3.313708498984757167, 7.999999999999991118, 9.605302784329824206 ) ) ;
#3442=CARTESIAN_POINT ( 'NONE',  ( -5.082755093536319713, 5.082755093536319713, 8.799052781871752771 ) ) ;
#3454=CARTESIAN_POINT ( 'NONE',  ( 5.082755093536320601, -5.082755093536318824, 11.42405278187175455 ) ) ;
#3469=CARTESIAN_POINT ( 'NONE',  ( -2.977408999572647819, 7.188101187499992051, 3.080302781871751439 ) ) ;
#3485=FACE_OUTER_BOUND ( 'NONE', #69403, .T. ) ;
#3498=CARTESIAN_POINT ( 'NONE',  ( 3.313708498984756279, 7.999999999999991118, 2.049052783920143117 ) ) ;
#3504=VERTEX_POINT ( 'NONE', #68555 ) ;
#3520=CARTESIAN_POINT ( 'NONE',  ( 7.188101187499993827, -2.977408999572645598, 2.142802781871750550 ) ) ;
#3532=CARTESIAN_POINT ( 'NONE',  ( 7.999999999999991118, 9.797174393178815797E-16, 10.58030277982336465 ) ) ;
#3533=CARTESIAN_POINT ( 'NONE',  ( 5.082755093536318824, 5.082755093536319713, 26.42405278187175455 ) ) ;
#3559=CARTESIAN_POINT ( 'NONE',  ( 1.320432766682872962E-15, -7.188101187499992051, 21.73655278187175455 ) ) ;
#3570=CARTESIAN_POINT ( 'NONE',  ( 3.313708498984756279, 7.999999999999991118, 17.04905278392014623 ) ) ;
#3578=CARTESIAN_POINT ( 'NONE',  ( 1.469576158976822172E-15, -7.999999999999991118, 11.70530277982336642 ) ) ;
#3583=CARTESIAN_POINT ( 'NONE',  ( 7.999986417242976877, 3.313722081741772296, 13.86155332737053314 ) ) ;
#3605=CARTESIAN_POINT ( 'NONE',  ( -8.008118988124991233, 0.000000000000000000, 28.01311528394063188 ) ) ;
#3625=CARTESIAN_POINT ( 'NONE',  ( -7.999999999999991118, 0.000000000000000000, 14.33030277982336465 ) ) ;
#3638=CARTESIAN_POINT ( 'NONE',  ( -2.977408999572648707, -7.188101187499990274, 23.14280278187176165 ) ) ;
#3652=ORIENTED_EDGE ( 'NONE', *, *, #7614, .F. ) ;
#3664=CARTESIAN_POINT ( 'NONE',  ( 7.188101187499993827, -2.977408999572645598, 1.017802781871753215 ) ) ;
#3683=CARTESIAN_POINT ( 'NONE',  ( -5.656854249492373476, -5.656854249492376141, 16.20530278392014978 ) ) ;
#3689=EDGE_CURVE ( 'NONE', #58023, #12693, #33137, .T. ) ;
#3697=CARTESIAN_POINT ( 'NONE',  ( 5.656854249492376141, -5.656854249492374365, 27.08030278392014978 ) ) ;
#3707=AXIS2_PLACEMENT_3D ( 'NONE', #58865, #47517, #59594 ) ;
#3708=CARTESIAN_POINT ( 'NONE',  ( -7.188101187499992051, 0.000000000000000000, 13.48655278187175455 ) ) ;
#3715=ORIENTED_EDGE ( 'NONE', *, *, #61577, .T. ) ;
#3718=CARTESIAN_POINT ( 'NONE',  ( -7.999999999999989342, -3.313708498984762496, 8.611552783920146226 ) ) ;
#3729=CARTESIAN_POINT ( 'NONE',  ( 7.188101187499991163, 2.977408999572648707, 15.83030278187175277 ) ) ;
#3747=CARTESIAN_POINT ( 'NONE',  ( -3.313708498984758943, -7.999999999999989342, 23.79905278392014978 ) ) ;
#3754=CARTESIAN_POINT ( 'NONE',  ( -5.082755093536317936, -5.082755093536320601, 18.54905278187175455 ) ) ;
#3762=CARTESIAN_POINT ( 'NONE',  ( 5.656854249492374365, 5.656854249492375253, 18.26780277982336642 ) ) ;
#3771=CARTESIAN_POINT ( 'NONE',  ( 7.999999999999991118, 9.797174393178815797E-16, 12.08030277982336642 ) ) ;
#3784=CARTESIAN_POINT ( 'NONE',  ( -7.999999999961178609, -1.665943300379353739E-05, 2.518425711869641592 ) ) ;
#3787=CARTESIAN_POINT ( 'NONE',  ( -3.313708498984758943, -7.999999999999989342, 11.66780278432982421 ) ) ;
#3819=CARTESIAN_POINT ( 'NONE',  ( -4.898587196589407898E-16, 7.999999999999991118, 16.95530277982336287 ) ) ;
#3823=CARTESIAN_POINT ( 'NONE',  ( 7.188101187499991163, 2.977408999572648707, 5.330302781871753659 ) ) ;
#3836=CARTESIAN_POINT ( 'NONE',  ( -7.188101187499991163, 2.977408999572646930, 10.76780278187175632 ) ) ;
#3843=CARTESIAN_POINT ( 'NONE',  ( 7.999999999999991118, 0.000000000000000000, 30.00000000000000000 ) ) ;
#3846=CARTESIAN_POINT ( 'NONE',  ( -5.447321192899549303, -4.689935021205116961, 0.1569292013794422458 ) ) ;
#3849=CARTESIAN_POINT ( 'NONE',  ( 5.082755093536318824, 5.082755093536319713, 5.799052781871753659 ) ) ;
#3867=CARTESIAN_POINT ( 'NONE',  ( -7.999999999999991118, 3.313708498984756723, 26.23655277982336642 ) ) ;
#3878=CARTESIAN_POINT ( 'NONE',  ( 7.999999999999991118, 9.797174393178815797E-16, 1.767802783920142895 ) ) ;
#3901=CARTESIAN_POINT ( 'NONE',  ( -2.977408999572647819, -7.188101187499990274, 3.267802781871751439 ) ) ;
#3919=CARTESIAN_POINT ( 'NONE',  ( 5.082755093536318824, 5.082755093536319713, 24.92405278187175810 ) ) ;
#3941=CARTESIAN_POINT ( 'NONE',  ( -5.082755093536317936, -5.082755093536320601, 23.04905278187175455 ) ) ;
#3960=CARTESIAN_POINT ( 'NONE',  ( -7.999999999999991118, 0.000000000000000000, 11.33030277982336642 ) ) ;
#3963=VERTEX_POINT ( 'NONE', #44349 ) ;
#3991=CARTESIAN_POINT ( 'NONE',  ( 3.317071493978883456, -8.008118988124989457, 22.48186528394063544 ) ) ;
#3992=CARTESIAN_POINT ( 'NONE',  ( 3.313708498984756279, 7.999999999999991118, 23.04905278392014623 ) ) ;
#4001=EDGE_CURVE ( 'NONE', #64740, #71548, #69649, .T. ) ;
#4008=CARTESIAN_POINT ( 'NONE',  ( -4.898587196589407898E-16, 7.999999999999991118, 13.95530277982336465 ) ) ;
#4023=CARTESIAN_POINT ( 'NONE',  ( -5.082755093536319713, 5.082755093536319713, 21.17405278187175455 ) ) ;
#4050=CARTESIAN_POINT ( 'NONE',  ( 3.313708498984756279, 7.999999999999991118, 25.86155277982337353 ) ) ;
#4068=CARTESIAN_POINT ( 'NONE',  ( 5.656854249492374365, 5.656854249492375253, 19.95530278392014623 ) ) ;
#4088=CARTESIAN_POINT ( 'NONE',  ( 7.188101187499993827, -2.977408999572645598, 14.14280278187175455 ) ) ;
#4099=CARTESIAN_POINT ( 'NONE',  ( -7.999999999999989342, -3.313708498984762496, 10.11155278392014623 ) ) ;
#4111=CARTESIAN_POINT ( 'NONE',  ( 5.082755093536320601, -5.082755093536318824, 14.04905278187175455 ) ) ;
#4116=CARTESIAN_POINT ( 'NONE',  ( -7.999994587436531468, -3.313713911548220814, 23.61155300047851568 ) ) ;
#4121=AXIS2_PLACEMENT_3D ( 'NONE', #63883, #6551, #905 ) ;
#4138=CARTESIAN_POINT ( 'NONE',  ( 5.082755093536320601, -5.082755093536318824, 18.92405278187175455 ) ) ;
#4154=CARTESIAN_POINT ( 'NONE',  ( 3.313708498984762496, -7.999999999999989342, 10.29905277982336465 ) ) ;
#4170=CARTESIAN_POINT ( 'NONE',  ( 7.999999999999992895, -3.313708498984756279, 12.04280278432982243 ) ) ;
#4210=CARTESIAN_POINT ( 'NONE',  ( 7.188101187499992051, 8.802885111219154394E-16, 13.11155278187175277 ) ) ;
#4224=CARTESIAN_POINT ( 'NONE',  ( 1.320432766682872962E-15, -7.188101187499992051, 0.7365527818717527708 ) ) ;
#4241=CARTESIAN_POINT ( 'NONE',  ( -7.999999999999991118, 3.313708498984756723, 29.23655277982336642 ) ) ;
#4246=CARTESIAN_POINT ( 'NONE',  ( -3.313708498984759387, -7.999999999999989342, 25.29905278392014978 ) ) ;
#4252=CARTESIAN_POINT ( 'NONE',  ( -3.313708498984757167, 7.999999999999991118, 27.60530278432982954 ) ) ;
#4284=CARTESIAN_POINT ( 'NONE',  ( -2.977408999572647819, 7.188101187499991163, 20.70530278187175455 ) ) ;
#4285=ORIENTED_EDGE ( 'NONE', *, *, #28200, .T. ) ;
#4310=CARTESIAN_POINT ( 'NONE',  ( -5.082755093536317936, -5.082755093536320601, 24.54905278187175810 ) ) ;
#4320=CARTESIAN_POINT ( 'NONE',  ( -7.999999999999991118, 9.797174393178815797E-16, 30.00000000000000000 ) ) ;
#4328=CARTESIAN_POINT ( 'NONE',  ( -7.999999999999991118, 3.313708498984756723, 6.736552779823365533 ) ) ;
#4333=CARTESIAN_POINT ( 'NONE',  ( 3.313708498984756279, 7.999999999999991118, 1.861552779823364867 ) ) ;
#4339=CARTESIAN_POINT ( 'NONE',  ( -7.999999999999991118, -6.056862366737761932E-06, 20.51780295527825970 ) ) ;
#4355=CARTESIAN_POINT ( 'NONE',  ( 3.317071493978877683, 8.008118988124991233, 21.54436528394063188 ) ) ;
#4372=AXIS2_PLACEMENT_3D ( 'NONE', #43857, #2752, #25740 ) ;
#4388=CARTESIAN_POINT ( 'NONE',  ( 5.082755093536318824, 5.082755093536319713, 20.79905278187175455 ) ) ;
#4395=CARTESIAN_POINT ( 'NONE',  ( 0.000000000000000000, 15.08051212944140218, 15.04081104653146994 ) ) ;
#4412=CARTESIAN_POINT ( 'NONE',  ( 3.313708498984756279, 7.999999999999991118, 24.36155277982336997 ) ) ;
#4417=CARTESIAN_POINT ( 'NONE',  ( -7.999999999999991118, 9.797174393178815797E-16, 30.00000000000000000 ) ) ;
#4422=VERTEX_POINT ( 'NONE', #28593 ) ;
#4430=CARTESIAN_POINT ( 'NONE',  ( 5.656854249492374365, 5.656854249492375253, 10.95530278392014800 ) ) ;
#4436=AXIS2_PLACEMENT_3D ( 'NONE', #53754, #42413, #42784 ) ;
#4443=VERTEX_POINT ( 'NONE', #74242 ) ;
#4452=CARTESIAN_POINT ( 'NONE',  ( 2.977408999572646486, 7.188101187499992051, 14.51780278187175455 ) ) ;
#4455=( BOUNDED_CURVE ( )  B_SPLINE_CURVE ( 2, ( #27328, #33390, #43947, #27704, #43562, #26960, #56390, #50715, #67336, #38673, #61675 ),
 .UNSPECIFIED., .F., .F. ) 
 B_SPLINE_CURVE_WITH_KNOTS ( ( 3, 2, 2, 2, 2, 3 ),
 ( 0.6088813560782819767, 0.6154996293544834352, 0.6221179049389403692, 0.6287361805233971923, 0.6353544561078539044, 0.6353544975714136012 ),
 .UNSPECIFIED. ) 
 CURVE ( )  GEOMETRIC_REPRESENTATION_ITEM ( )  RATIONAL_B_SPLINE_CURVE ( ( 1.000000000000000000, 0.9238795325112867385, 1.000000000000000000, 0.9238795325112867385, 1.000000000000000000, 0.9238795325112867385, 1.000000000000000000, 0.9238795325112867385, 1.000000000000000000, 0.9999995231045452071, 0.9999990462150658566 ) ) 
 REPRESENTATION_ITEM ( '' )  );
#4480=CARTESIAN_POINT ( 'NONE',  ( 2.977408999572650927, -7.188101187499990274, 15.45530278187175455 ) ) ;
#4485=CARTESIAN_POINT ( 'NONE',  ( -3.313708498984759387, -7.999999999999989342, 17.61155277982336997 ) ) ;
#4503=CARTESIAN_POINT ( 'NONE',  ( -7.188101187499990274, -2.977408999572651371, 18.45530278187175455 ) ) ;
#4519=CARTESIAN_POINT ( 'NONE',  ( -5.656854249492373476, -5.656854249492376141, 1.017802779823363757 ) ) ;
#4523=CLOSED_SHELL ( 'NONE', ( #71611, #47029, #11209, #22063, #61453, #46945, #73459, #68338, #22077, #31450, #31803, #63904, #26056, #46855, #59388, #5652, #28398, #53352, #7024, #13467, #40132, #30038, #38139, #50262, #848, #17255, #65211, #37387, #10011, #1161, #63333, #7871, #54554, #32526, #57451, #69911, #28215, #571, #57405, #65582, #27835, #66650, #24853, #18743, #18795, #71637, #66629, #15426, #8446, #27623, #34422, #34348, #47600 ) ) ;
#4535=CARTESIAN_POINT ( 'NONE',  ( 3.313708498984762496, -7.999999999999989342, 8.855302784329824206 ) ) ;
#4566=CARTESIAN_POINT ( 'NONE',  ( 7.188101187499992051, 8.802885111219154394E-16, 3.736552781871751883 ) ) ;
#4579=CARTESIAN_POINT ( 'NONE',  ( 7.188101187499993827, -2.977408999572645598, 7.017802781871755435 ) ) ;
#4608=CARTESIAN_POINT ( 'NONE',  ( -3.313708498984757167, 7.999999999999991118, 27.54905277982337353 ) ) ;
#4613=CARTESIAN_POINT ( 'NONE',  ( -7.999999999999991118, 0.000000000000000000, 6.830302779823365533 ) ) ;
#4619=CARTESIAN_POINT ( 'NONE',  ( 7.999999999999991118, 9.797174393178815797E-16, 3.267802783920144449 ) ) ;
#4627=VECTOR ( 'NONE', #71642, 1000.000000000000000 ) ;
#4657=CARTESIAN_POINT ( 'NONE',  ( -2.977408999572648707, -7.188101187499990274, 19.76780278187175455 ) ) ;
#4682=CARTESIAN_POINT ( 'NONE',  ( -7.188101187499992051, 0.000000000000000000, 16.86155278187175810 ) ) ;
#4686=CARTESIAN_POINT ( 'NONE',  ( -7.999999999974042098, 1.357258486152048259E-05, 14.51729352187485311 ) ) ;
#4701=CARTESIAN_POINT ( 'NONE',  ( 5.656854249492376141, -5.656854249492374365, 2.892802779823365533 ) ) ;
#4709=VERTEX_POINT ( 'NONE', #13447 ) ;
#4710=EDGE_CURVE ( 'NONE', #60564, #73315, #70805, .T. ) ;
#4728=CARTESIAN_POINT ( 'NONE',  ( 3.317071493978883456, -8.008118988124989457, 20.98186528394063899 ) ) ;
#4747=EDGE_CURVE ( 'NONE', #64535, #4422, #24416, .T. ) ;
#4764=CARTESIAN_POINT ( 'NONE',  ( -7.188101187499992051, 0.000000000000000000, 24.36155278187175810 ) ) ;
#4789=CARTESIAN_POINT ( 'NONE',  ( -7.999999999999991118, 0.000000000000000000, 18.83030277982336642 ) ) ;
#4806=CARTESIAN_POINT ( 'NONE',  ( -4.898587196589407898E-16, 7.999999999999991118, 22.95530277982336642 ) ) ;
#4808=CARTESIAN_POINT ( 'NONE',  ( -7.999999999999991118, 3.313708498984756723, 15.92405278392014623 ) ) ;
#4817=DIRECTION ( 'NONE',  ( 1.000000000000000000, 0.000000000000000000, 0.000000000000000000 ) ) ;
#4831=CARTESIAN_POINT ( 'NONE',  ( 2.977408999572646486, 7.188101187499992051, 17.51780278187175455 ) ) ;
#4844=SPHERICAL_SURFACE ( 'NONE', #19763, 20.00000000000000355 ) ;
#4856=CARTESIAN_POINT ( 'NONE',  ( 7.188101187499993827, -2.977408999572645598, 12.64280278187175277 ) ) ;
#4871=ORIENTED_EDGE ( 'NONE', *, *, #5667, .F. ) ;
#4880=CARTESIAN_POINT ( 'NONE',  ( 2.977408999572646486, 7.188101187499991163, 16.39280278187175455 ) ) ;
#4882=CARTESIAN_POINT ( 'NONE',  ( -3.313708498984759387, -7.999999999999989342, 1.299052783920146226 ) ) ;
#4893=CARTESIAN_POINT ( 'NONE',  ( -4.898587196589407898E-16, 7.999999999999991118, 4.955302779823363757 ) ) ;
#4915=CARTESIAN_POINT ( 'NONE',  ( -3.313708498984758943, -7.999999999999989342, 4.167802784329823318 ) ) ;
#4916=CARTESIAN_POINT ( 'NONE',  ( -4.898587196589407898E-16, 7.999999999999991118, 4.955302779823363757 ) ) ;
#4943=CARTESIAN_POINT ( 'NONE',  ( -7.188101187499991163, 2.977408999572646930, 1.392802781871753437 ) ) ;
#4956=CARTESIAN_POINT ( 'NONE',  ( -7.188101187499992051, 0.000000000000000000, 4.861552781871752771 ) ) ;
#4985=CARTESIAN_POINT ( 'NONE',  ( 5.656854249492376141, -5.656854249492374365, 19.39280277982336642 ) ) ;
#4999=CARTESIAN_POINT ( 'NONE',  ( 3.313708498984762496, -7.999999999999989342, 23.85530278432982954 ) ) ;
#5033=CARTESIAN_POINT ( 'NONE',  ( -7.188101187499991163, 2.977408999572646930, 20.89280278187176521 ) ) ;
#5056=CARTESIAN_POINT ( 'NONE',  ( -7.188101187499992051, 2.977408999572646930, 16.76780278187175455 ) ) ;
#5076=CARTESIAN_POINT ( 'NONE',  ( -5.656854249492375253, 5.656854249492375253, 2.142802779823364645 ) ) ;
#5077=CARTESIAN_POINT ( 'NONE',  ( 7.999999999999991118, 9.797174393178815797E-16, 21.26780278392014623 ) ) ;
#5105=CARTESIAN_POINT ( 'NONE',  ( 5.662595241051936235, -5.662595241051934458, 22.57561528394063188 ) ) ;
#5118=ORIENTED_EDGE ( 'NONE', *, *, #65592, .F. ) ;
#5134=CARTESIAN_POINT ( 'NONE',  ( -7.323353171866783917, -3.228862220574169939, 0.000000000000000000 ) ) ;
#5138=CARTESIAN_POINT ( 'NONE',  ( 5.082755093536320601, -5.082755093536318824, 24.92405278187175810 ) ) ;
#5139=FACE_OUTER_BOUND ( 'NONE', #37402, .T. ) ;
#5149=CARTESIAN_POINT ( 'NONE',  ( 8.000000000000049738, 3.313708498984697215, 27.36155278392014623 ) ) ;
#5155=EDGE_CURVE ( 'NONE', #73412, #60564, #50018, .T. ) ;
#5164=CARTESIAN_POINT ( 'NONE',  ( -7.999999999999991118, 3.313708498984756723, 20.23655277982336642 ) ) ;
#5180=CARTESIAN_POINT ( 'NONE',  ( 3.313708498984762496, -7.999999999999989342, 11.98655278392014445 ) ) ;
#5225=CARTESIAN_POINT ( 'NONE',  ( 5.082755093536320601, -5.082755093536318824, 11.04905278187175455 ) ) ;
#5236=B_SPLINE_CURVE_WITH_KNOTS ( 'NONE', 3,
 ( #29765, #47102, #70500, #69388 ),
 .UNSPECIFIED., .F., .F.,
 ( 4, 4 ),
 ( 0.000000000000000000, 0.2375773127046199029 ),
 .UNSPECIFIED. ) ;
#5252=CARTESIAN_POINT ( 'NONE',  ( -5.082755093536317936, -5.082755093536320601, 9.549052781871754547 ) ) ;
#5255=CARTESIAN_POINT ( 'NONE',  ( -4.898587196589407898E-16, 7.999999999999991118, 3.511552784329822874 ) ) ;
#5267=CARTESIAN_POINT ( 'NONE',  ( -7.999999999999989342, -3.313708498984762496, 3.924052779823362425 ) ) ;
#5268=CARTESIAN_POINT ( 'NONE',  ( 1.469576158976822172E-15, -7.999999999999991118, 4.392802783920145338 ) ) ;
#5276=ORIENTED_EDGE ( 'NONE', *, *, #61338, .T. ) ;
#5283=CARTESIAN_POINT ( 'NONE',  ( -7.999999999999989342, -3.313708498984762496, 6.980302784329822430 ) ) ;
#5293=ORIENTED_EDGE ( 'NONE', *, *, #38478, .F. ) ;
#5309=CARTESIAN_POINT ( 'NONE',  ( -5.082755093536317936, -5.082755093536320601, 3.174052781871751439 ) ) ;
#5323=CARTESIAN_POINT ( 'NONE',  ( -5.082755093536317936, -5.082755093536320601, 3.549052781871751883 ) ) ;
#5332=CARTESIAN_POINT ( 'NONE',  ( 7.999999999999991118, 9.797174393178815797E-16, 7.580302779823366421 ) ) ;
#5334=CARTESIAN_POINT ( 'NONE',  ( -7.188101187499991163, 2.977408999572646930, 25.76780278187175810 ) ) ;
#5337=( BOUNDED_CURVE ( )  B_SPLINE_CURVE ( 2, ( #8867, #49218, #9623, #65824, #60916, #55279, #32643, #3583, #14131 ),
 .UNSPECIFIED., .F., .F. ) 
 B_SPLINE_CURVE_WITH_KNOTS ( ( 3, 2, 2, 2, 3 ),
 ( 0.4765158731794318925, 0.4831341176653472513, 0.4897523932498040744, 0.4963706688342608420, 0.5029889089742047847 ),
 .UNSPECIFIED. ) 
 CURVE ( )  GEOMETRIC_REPRESENTATION_ITEM ( )  RATIONAL_B_SPLINE_CURVE ( ( 0.9999992846401264401, 0.9238798901929041740, 1.000000000000000000, 0.9238795325112867385, 1.000000000000000000, 0.9238795325112867385, 1.000000000000000000, 0.9238799401783380771, 0.9999991846702638298 ) ) 
 REPRESENTATION_ITEM ( '' )  );
#5351=CARTESIAN_POINT ( 'NONE',  ( 7.999999999999992895, -3.313708498984756279, 19.48655277982336642 ) ) ;
#5366=CARTESIAN_POINT ( 'NONE',  ( 3.313708498984762496, -7.999999999999989342, 20.85530278432983309 ) ) ;
#5372=CARTESIAN_POINT ( 'NONE',  ( 5.656854249492374365, 5.656854249492375253, 24.26780277982336642 ) ) ;
#5384=CARTESIAN_POINT ( 'NONE',  ( 0.000000000000000000, 0.000000000000000000, 11.00000000000000000 ) ) ;
#5398=CARTESIAN_POINT ( 'NONE',  ( 1.320432766682872962E-15, -7.188101187499992051, 21.36155278187175455 ) ) ;
#5419=CARTESIAN_POINT ( 'NONE',  ( -5.082755093536317936, -5.082755093536320601, 17.04905278187175810 ) ) ;
#5424=CARTESIAN_POINT ( 'NONE',  ( 7.999999999999991118, 0.000000000000000000, 29.33030277982336642 ) ) ;
#5442=CARTESIAN_POINT ( 'NONE',  ( -5.656854249492373476, -5.656854249492376141, 2.517802779823365089 ) ) ;
#5457=CARTESIAN_POINT ( 'NONE',  ( 6.803355351215364166, -4.261158589325806823, -0.000000000000000000 ) ) ;
#5471=CARTESIAN_POINT ( 'NONE',  ( -3.317071493978878571, 8.008118988124991233, 18.73186528394063188 ) ) ;
#5491=CARTESIAN_POINT ( 'NONE',  ( 5.656854249492374365, 5.656854249492375253, 7.955302783920145338 ) ) ;
#5505=CARTESIAN_POINT ( 'NONE',  ( -4.401442555609577197E-16, 7.188101187499992051, 19.48655278187175455 ) ) ;
#5506=DIRECTION ( 'NONE',  ( 1.000000000000000000, 0.000000000000000000, 0.000000000000000000 ) ) ;
#5529=CARTESIAN_POINT ( 'NONE',  ( -7.999999999999989342, -3.313708498984762496, 20.42405277982336642 ) ) ;
#5546=CARTESIAN_POINT ( 'NONE',  ( -4.898587196589407898E-16, 7.999999999999991118, 12.64280278392014623 ) ) ;
#5549=VERTEX_POINT ( 'NONE', #63676 ) ;
#5600=CARTESIAN_POINT ( 'NONE',  ( 7.188101187499993827, -2.977408999572645598, 8.142802781871750994 ) ) ;
#5623=CARTESIAN_POINT ( 'NONE',  ( 7.188101187499991163, 2.977408999572648707, 8.705302781871752771 ) ) ;
#5626=CARTESIAN_POINT ( 'NONE',  ( 5.656854249492376141, -5.656854249492374365, 2.949052784329821986 ) ) ;
#5636=CARTESIAN_POINT ( 'NONE',  ( 5.656854249492374365, 5.656854249492375253, 6.267802779823364645 ) ) ;
#5650=CARTESIAN_POINT ( 'NONE',  ( 5.656854249492376141, -5.656854249492374365, 4.449052784329823318 ) ) ;
#5652=ADVANCED_FACE ( 'NONE', ( #65531 ), #60237, .F. ) ;
#5658=CARTESIAN_POINT ( 'NONE',  ( 1.320432766682872962E-15, -7.188101187499992051, 27.36155278187175455 ) ) ;
#5667=EDGE_CURVE ( 'NONE', #60631, #26236, #8562, .T. ) ;
#5672=CARTESIAN_POINT ( 'NONE',  ( 5.656854249492376141, -5.656854249492374365, 21.08030278392014623 ) ) ;
#5680=CARTESIAN_POINT ( 'NONE',  ( -5.272365137108047328, -4.893145049964592097, 0.1656095422372733106 ) ) ;
#5694=CARTESIAN_POINT ( 'NONE',  ( 1.320432766682872962E-15, -7.188101187499992051, 8.236552781871752771 ) ) ;
#5703=CARTESIAN_POINT ( 'NONE',  ( -4.401442555609577197E-16, 7.188101187499992051, 26.98655278187175455 ) ) ;
#5721=CARTESIAN_POINT ( 'NONE',  ( 3.313708498984762496, -7.999999999999989342, 20.79905277982336642 ) ) ;
#5735=CARTESIAN_POINT ( 'NONE',  ( 1.469576158976822172E-15, -7.999999999999991118, 22.26155278432982243 ) ) ;
#5763=DIRECTION ( 'NONE',  ( 1.000000000000000000, 0.000000000000000000, 0.000000000000000000 ) ) ;
#5770=CARTESIAN_POINT ( 'NONE',  ( 7.188101187499992051, 8.802885111219154394E-16, 17.23655278187175810 ) ) ;
#5774=( BOUNDED_CURVE ( )  B_SPLINE_CURVE ( 2, ( #5332, #35491, #12092, #41508, #40768, #63775, #433, #17378, #34392 ),
 .UNSPECIFIED., .F., .F. ) 
 B_SPLINE_CURVE_WITH_KNOTS ( ( 3, 2, 2, 2, 3 ),
 ( 0.7631578947368420351, 0.7697368421052630527, 0.7763157894736840703, 0.7828947368421053099, 0.7894736842105263275 ),
 .UNSPECIFIED. ) 
 CURVE ( )  GEOMETRIC_REPRESENTATION_ITEM ( )  RATIONAL_B_SPLINE_CURVE ( ( 1.000000000000001332, 0.9238795325112854062, 1.000000000000000000, 0.9238795325112867385, 1.000000000000000000, 0.9238795325112867385, 1.000000000000000000, 0.9238795325112867385, 1.000000000000000000 ) ) 
 REPRESENTATION_ITEM ( '' )  );
#5785=ORIENTED_EDGE ( 'NONE', *, *, #31346, .T. ) ;
#5796=CARTESIAN_POINT ( 'NONE',  ( -7.188101187499992051, 2.977408999572646930, 19.76780278187175455 ) ) ;
#5806=AXIS2_PLACEMENT_3D ( 'NONE', #15438, #48652, #7934 ) ;
#5817=CARTESIAN_POINT ( 'NONE',  ( -4.898587196589407898E-16, 7.999999999999991118, 4.955302779823363757 ) ) ;
#5847=CARTESIAN_POINT ( 'NONE',  ( 5.662595241051936235, -5.662595241051934458, 16.57561528394063188 ) ) ;
#5865=CARTESIAN_POINT ( 'NONE',  ( -5.656854249492373476, -5.656854249492376141, 10.20530278392014623 ) ) ;
#5880=CARTESIAN_POINT ( 'NONE',  ( -4.401442555609577197E-16, 7.188101187499992051, 17.98655278187175810 ) ) ;
#5904=CARTESIAN_POINT ( 'NONE',  ( 5.656854249492374365, 5.656854249492375253, 21.26780277982336642 ) ) ;
#5911=CARTESIAN_POINT ( 'NONE',  ( -8.000000000000033751, -3.313708498984719864, 8.424052779823361092 ) ) ;
#5922=CARTESIAN_POINT ( 'NONE',  ( 7.999999999999991118, 9.797174393178815797E-16, 10.76780278392014800 ) ) ;
#5938=CARTESIAN_POINT ( 'NONE',  ( -5.656854249492373476, -5.656854249492376141, 26.51780277982336997 ) ) ;
#5942=CARTESIAN_POINT ( 'NONE',  ( -7.999999999999015010, 2.678670460604446806E-06, 11.51770387648012317 ) ) ;
#5969=CARTESIAN_POINT ( 'NONE',  ( -7.188101187499992051, 0.000000000000000000, 7.486552781871751883 ) ) ;
#5995=CARTESIAN_POINT ( 'NONE',  ( 7.188101187499993827, -2.977408999572645598, 8.517802781871754547 ) ) ;
#5999=CARTESIAN_POINT ( 'NONE',  ( 1.469576158976822172E-15, -7.999999999999991118, 1.261552784329824206 ) ) ;
#6009=CARTESIAN_POINT ( 'NONE',  ( 7.999999999999992895, -3.313708498984756279, 5.986552779823365533 ) ) ;
#6022=CARTESIAN_POINT ( 'NONE',  ( -5.656854249492375253, 5.656854249492375253, 8.199052784329824206 ) ) ;
#6029=CARTESIAN_POINT ( 'NONE',  ( -2.977408999572647819, -7.188101187499990274, 27.26780278187175455 ) ) ;
#6041=CARTESIAN_POINT ( 'NONE',  ( 7.999999999999992895, -3.313708498984756279, 22.67405278392015333 ) ) ;
#6046=CARTESIAN_POINT ( 'NONE',  ( -7.999999999999991118, 0.000000000000000000, 8.330302779823362869 ) ) ;
#6052=CARTESIAN_POINT ( 'NONE',  ( -2.977408999572648707, -7.188101187499990274, 24.26780278187175455 ) ) ;
#6053=ORIENTED_EDGE ( 'NONE', *, *, #74560, .T. ) ;
#6065=CARTESIAN_POINT ( 'NONE',  ( 7.188101187499991163, 2.977408999572648707, 2.705302781871750994 ) ) ;
#6070=CARTESIAN_POINT ( 'NONE',  ( -3.317071493978880348, -8.008118988124989457, 2.794365283940627886 ) ) ;
#6076=CARTESIAN_POINT ( 'NONE',  ( -7.188101187499992051, 0.000000000000000000, 25.86155278187175810 ) ) ;
#6097=CARTESIAN_POINT ( 'NONE',  ( 1.469576158976822172E-15, -7.999999999999991118, 23.70530277982336642 ) ) ;
#6111=CARTESIAN_POINT ( 'NONE',  ( 5.656854249492374365, 5.656854249492375253, 22.82405278432982598 ) ) ;
#6143=CARTESIAN_POINT ( 'NONE',  ( 7.188101187499992051, 8.802885111219154394E-16, 11.23655278187175455 ) ) ;
#6157=VERTEX_POINT ( 'NONE', #23601 ) ;
#6167=CARTESIAN_POINT ( 'NONE',  ( 5.082755093536318824, 5.082755093536319713, 14.79905278187175455 ) ) ;
#6188=CARTESIAN_POINT ( 'NONE',  ( 5.656854249492374365, 5.656854249492375253, 1.767802779823364423 ) ) ;
#6201=CARTESIAN_POINT ( 'NONE',  ( -7.999999999999991118, 9.797174393178815797E-16, 30.00000000000000000 ) ) ;
#6217=CARTESIAN_POINT ( 'NONE',  ( -5.662595241051933570, -5.662595241051936235, 14.70061528394063188 ) ) ;
#6226=CARTESIAN_POINT ( 'NONE',  ( -7.188101187499992051, 0.000000000000000000, 8.986552781871752771 ) ) ;
#6231=FACE_OUTER_BOUND ( 'NONE', #3071, .T. ) ;
#6240=CARTESIAN_POINT ( 'NONE',  ( 5.656854249492374365, 5.656854249492375253, 9.455302783920146226 ) ) ;
#6254=CARTESIAN_POINT ( 'NONE',  ( -2.977408999572647819, 7.188101187499991163, 16.58030278187175455 ) ) ;
#6272=DIRECTION ( 'NONE',  ( -1.000000000000000000, 0.000000000000000000, 0.000000000000000000 ) ) ;
#6279=CARTESIAN_POINT ( 'NONE',  ( 5.656854249492376141, -5.656854249492374365, 19.39280277982336642 ) ) ;
#6298=CARTESIAN_POINT ( 'NONE',  ( 7.999999999999992895, -3.313708498984756279, 6.174052783920146226 ) ) ;
#6352=CARTESIAN_POINT ( 'NONE',  ( 1.320432766682872962E-15, -7.188101187499992051, 4.861552781871752771 ) ) ;
#6374=CARTESIAN_POINT ( 'NONE',  ( 7.188101187499991163, 2.977408999572648707, 7.205302781871754547 ) ) ;
#6378=CARTESIAN_POINT ( 'NONE',  ( -5.656854249492373476, -5.656854249492376141, 2.574052784329821986 ) ) ;
#6385=CARTESIAN_POINT ( 'NONE',  ( 7.999999999999991118, 0.000000000000000000, 30.00000000000000000 ) ) ;
#6388=CARTESIAN_POINT ( 'NONE',  ( 7.999999999999992895, -3.313708498984756279, 24.17405278392015333 ) ) ;
#6417=CARTESIAN_POINT ( 'NONE',  ( -3.313708498984758943, -7.999999999999989342, 17.79905278392014623 ) ) ;
#6428=CARTESIAN_POINT ( 'NONE',  ( 5.082755093536318824, 5.082755093536319713, 24.92405278187175810 ) ) ;
#6432=ORIENTED_EDGE ( 'NONE', *, *, #48728, .F. ) ;
#6444=CARTESIAN_POINT ( 'NONE',  ( -7.188101187499992051, 0.000000000000000000, 1.861552781871753881 ) ) ;
#6448=CARTESIAN_POINT ( 'NONE',  ( 8.008118988124991233, 9.807117285998411148E-16, 4.763115283940630107 ) ) ;
#6462=CARTESIAN_POINT ( 'NONE',  ( 7.999999999999991118, 0.000000000000000000, 30.00000000000000000 ) ) ;
#6472=CARTESIAN_POINT ( 'NONE',  ( 3.313708498984756279, 7.999999999999991118, 19.86155277982336997 ) ) ;
#6485=CARTESIAN_POINT ( 'NONE',  ( -7.999999999999989342, -3.313708498984762496, 23.48030278432982954 ) ) ;
#6514=CARTESIAN_POINT ( 'NONE',  ( -5.082755093536319713, 5.082755093536319713, 10.29905278187175455 ) ) ;
#6532=CARTESIAN_POINT ( 'NONE',  ( 3.313708498984756279, 7.999999999999991118, 26.04905278392014623 ) ) ;
#6537=CARTESIAN_POINT ( 'NONE',  ( -2.977408999572647819, -7.188101187499990274, 12.64280278187175277 ) ) ;
#6551=DIRECTION ( 'NONE',  ( -0.000000000000000000, -0.000000000000000000, 1.000000000000000000 ) ) ;
#6568=CARTESIAN_POINT ( 'NONE',  ( -4.898587196589407898E-16, 7.999999999999991118, 9.455302779823364645 ) ) ;
#6584=CARTESIAN_POINT ( 'NONE',  ( 8.008118988124993010, -3.317071493978877239, 15.16936528394063011 ) ) ;
#6590=CARTESIAN_POINT ( 'NONE',  ( 1.320432766682872962E-15, -7.188101187499992051, 7.861552781871751883 ) ) ;
#6596=VERTEX_POINT ( 'NONE', #66934 ) ;
#6605=CARTESIAN_POINT ( 'NONE',  ( 7.999999999999991118, 9.797174393178815797E-16, 0.2678027839201451155 ) ) ;
#6621=CARTESIAN_POINT ( 'NONE',  ( 5.082755093536320601, -5.082755093536318824, 17.42405278187175810 ) ) ;
#6624=DIRECTION ( 'NONE',  ( -0.000000000000000000, -0.000000000000000000, 1.000000000000000000 ) ) ;
#6625=CARTESIAN_POINT ( 'NONE',  ( 0.000000000000000000, 130.3999865490244190, 45.94057108883949070 ) ) ;
#6638=CARTESIAN_POINT ( 'NONE',  ( -3.313708498984759387, -7.999999999999989342, 25.11155277982336997 ) ) ;
#6646=CARTESIAN_POINT ( 'NONE',  ( -7.999999999999991118, 0.000000000000000000, 17.33030277982336287 ) ) ;
#6650=( BOUNDED_CURVE ( )  B_SPLINE_CURVE ( 2, ( #7382, #20160, #43177, #1731, #25818, #30389, #8480, #8114, #24351, #54147, #59437 ),
 .UNSPECIFIED., .F., .F. ) 
 B_SPLINE_CURVE_WITH_KNOTS ( ( 3, 2, 2, 2, 2, 3 ),
 ( 0.5029889089742047847, 0.5029889444187176650, 0.5096072200031744881, 0.5162254955876313112, 0.5228437711720881342, 0.5294620445568896105 ),
 .UNSPECIFIED. ) 
 CURVE ( )  GEOMETRIC_REPRESENTATION_ITEM ( )  RATIONAL_B_SPLINE_CURVE ( ( 0.9999991846702638298, 0.9999995923329486613, 1.000000000000000000, 0.9238795325112867385, 1.000000000000000000, 0.9238795325112867385, 1.000000000000000000, 0.9238795325112867385, 1.000000000000000000, 0.9238795325112867385, 1.000000000000000000 ) ) 
 REPRESENTATION_ITEM ( '' )  );
#6664=CARTESIAN_POINT ( 'NONE',  ( -7.999999999999989342, -3.313708498984762496, 4.111552783920145338 ) ) ;
#6711=CARTESIAN_POINT ( 'NONE',  ( -5.082755093536319713, 5.082755093536319713, 8.799052781871752771 ) ) ;
#6724=AXIS2_PLACEMENT_3D ( 'NONE', #46656, #69675, #41007 ) ;
#6736=CARTESIAN_POINT ( 'NONE',  ( 7.188101187499992051, 8.802885111219154394E-16, 11.61155278187175632 ) ) ;
#6740=CARTESIAN_POINT ( 'NONE',  ( 5.656854249492374365, 5.656854249492375253, 1.824052784329821097 ) ) ;
#6742=CARTESIAN_POINT ( 'NONE',  ( -7.999999999999989342, -3.313708498984762496, 7.111552783920144449 ) ) ;
#6750=CARTESIAN_POINT ( 'NONE',  ( -7.999999999999991118, 3.313708498984756723, 26.42405278392015333 ) ) ;
#6758=VERTEX_POINT ( 'NONE', #5424 ) ;
#6768=ORIENTED_EDGE ( 'NONE', *, *, #54813, .T. ) ;
#6782=CARTESIAN_POINT ( 'NONE',  ( -3.313708498984757167, 7.999999999999991118, 17.23655278392014978 ) ) ;
#6791=CARTESIAN_POINT ( 'NONE',  ( 2.977408999572650927, -7.188101187499990274, 27.45530278187175810 ) ) ;
#6793=VERTEX_POINT ( 'NONE', #526 ) ;
#6801=CARTESIAN_POINT ( 'NONE',  ( 7.188101187499992051, 8.802885111219154394E-16, 1.111552781871753215 ) ) ;
#6802=DIRECTION ( 'NONE',  ( 1.000000000000000000, 0.000000000000000000, 0.000000000000000000 ) ) ;
#6805=CARTESIAN_POINT ( 'NONE',  ( 3.317071493978877683, 8.008118988124991233, 2.044365283940627442 ) ) ;
#6831=CARTESIAN_POINT ( 'NONE',  ( -3.313708498984757167, 7.999999999999991118, 12.54905277982336287 ) ) ;
#6845=CARTESIAN_POINT ( 'NONE',  ( -7.999999999999989342, -3.313708498984762496, 20.48030278432982598 ) ) ;
#6861=DIRECTION ( 'NONE',  ( -0.000000000000000000, -0.000000000000000000, 1.000000000000000000 ) ) ;
#6869=CARTESIAN_POINT ( 'NONE',  ( 5.656854249492374365, 5.656854249492375253, 12.45530278392014623 ) ) ;
#6879=CARTESIAN_POINT ( 'NONE',  ( -4.401442555609577197E-16, 7.188101187499992051, 13.11155278187175277 ) ) ;
#6901=CARTESIAN_POINT ( 'NONE',  ( -2.977408999572647819, -7.188101187499990274, 11.14280278187175455 ) ) ;
#6905=CARTESIAN_POINT ( 'NONE',  ( 1.469576158976822172E-15, -7.999999999999991118, 20.70530277982336642 ) ) ;
#6948=CARTESIAN_POINT ( 'NONE',  ( 1.471067592899761672E-15, -8.008118988124991233, 13.38811528394063011 ) ) ;
#6954=CARTESIAN_POINT ( 'NONE',  ( -7.188101187499992051, 0.000000000000000000, 10.48655278187175455 ) ) ;
#6967=FACE_OUTER_BOUND ( 'NONE', #16124, .T. ) ;
#6968=CARTESIAN_POINT ( 'NONE',  ( -7.999999999999991118, 3.313708498984756723, 2.424052783920144005 ) ) ;
#6985=CARTESIAN_POINT ( 'NONE',  ( -2.977408999572647819, 7.188101187499991163, 18.08030278187175455 ) ) ;
#6990=CARTESIAN_POINT ( 'NONE',  ( 3.313708498984762496, -7.999999999999989342, 19.48655278392014978 ) ) ;
#6994=CARTESIAN_POINT ( 'NONE',  ( -4.401442555609577197E-16, 7.188101187499992051, 28.48655278187175810 ) ) ;
#7013=CARTESIAN_POINT ( 'NONE',  ( 3.313708498984762496, -7.999999999999989342, 14.79905277982336465 ) ) ;
#7024=ADVANCED_FACE ( 'NONE', ( #41242 ), #54419, .F. ) ;
#7031=CARTESIAN_POINT ( 'NONE',  ( 7.999999999999991118, 9.797174393178815797E-16, 9.267802783920146226 ) ) ;
#7078=CARTESIAN_POINT ( 'NONE',  ( 2.977408999572650927, -7.188101187499990274, 4.955302781871753659 ) ) ;
#7104=CARTESIAN_POINT ( 'NONE',  ( 7.188101187499992051, 8.802885111219154394E-16, 5.611552781871753659 ) ) ;
#7119=CARTESIAN_POINT ( 'NONE',  ( -5.656854249492375253, 5.656854249492375253, 26.33030278392014623 ) ) ;
#7135=CARTESIAN_POINT ( 'NONE',  ( 7.999999999999992895, -3.313708498984756279, 12.17405278392014623 ) ) ;
#7140=CARTESIAN_POINT ( 'NONE',  ( 7.188101187499992051, 8.802885111219154394E-16, 26.23655278187175810 ) ) ;
#7143=EDGE_CURVE ( 'NONE', #71548, #55503, #16772, .T. ) ;
#7150=CARTESIAN_POINT ( 'NONE',  ( -3.313708498984757167, 7.999999999999991118, 18.73655278392014623 ) ) ;
#7154=CARTESIAN_POINT ( 'NONE',  ( 0.000000000000000000, 0.000000000000000000, 30.00000000000000000 ) ) ;
#7162=CARTESIAN_POINT ( 'NONE',  ( 5.082755093536320601, -5.082755093536318824, 27.54905278187175455 ) ) ;
#7164=ORIENTED_EDGE ( 'NONE', *, *, #8790, .T. ) ;
#7179=CARTESIAN_POINT ( 'NONE',  ( -5.662595241051935346, 5.662595241051935346, 2.325615283940627442 ) ) ;
#7186=CARTESIAN_POINT ( 'NONE',  ( -5.082755093536319713, 5.082755093536319713, 21.17405278187175455 ) ) ;
#7204=CARTESIAN_POINT ( 'NONE',  ( -5.656854249492375253, 5.656854249492375253, 15.64280277982336642 ) ) ;
#7221=CARTESIAN_POINT ( 'NONE',  ( -5.656854249492375253, 5.656854249492375253, 18.69905278432982243 ) ) ;
#7232=ORIENTED_EDGE ( 'NONE', *, *, #34800, .F. ) ;
#7249=CARTESIAN_POINT ( 'NONE',  ( 2.977408999572646486, 7.188101187499991163, 13.01780278187175277 ) ) ;
#7274=CARTESIAN_POINT ( 'NONE',  ( -5.082755093536317936, -5.082755093536320601, 11.04905278187175455 ) ) ;
#7279=CARTESIAN_POINT ( 'NONE',  ( -7.999999999961189268, -1.665725685002260109E-05, 4.018425631117963803 ) ) ;
#7296=CARTESIAN_POINT ( 'NONE',  ( -5.867882488397293095, -5.445826010587458299, 1.009359473472040802 ) ) ;
#7308=AXIS2_PLACEMENT_3D ( 'NONE', #70543, #18859, #6802 ) ;
#7318=CARTESIAN_POINT ( 'NONE',  ( 5.656854249492376141, -5.656854249492374365, 13.39280277982336465 ) ) ;
#7321=CARTESIAN_POINT ( 'NONE',  ( 8.008118988124991233, 9.807117285998411148E-16, 16.76311528394063188 ) ) ;
#7328=CARTESIAN_POINT ( 'NONE',  ( 1.320432766682872962E-15, -7.188101187499992051, 9.361552781871752771 ) ) ;
#7339=DIRECTION ( 'NONE',  ( -0.000000000000000000, -0.000000000000000000, 1.000000000000000000 ) ) ;
#7340=CARTESIAN_POINT ( 'NONE',  ( -5.656854249492375253, 5.656854249492375253, 3.830302783920144893 ) ) ;
#7341=ORIENTED_EDGE ( 'NONE', *, *, #36737, .T. ) ;
#7351=CARTESIAN_POINT ( 'NONE',  ( -6.062687379811042554, -5.219768740853823807, 2.519839246067225784E-12 ) ) ;
#7355=CARTESIAN_POINT ( 'NONE',  ( 1.320432766682872962E-15, -7.188101187499992051, 12.73655278187175277 ) ) ;
#7358=CARTESIAN_POINT ( 'NONE',  ( 3.313708498984756279, 7.999999999999991118, 2.049052783920143117 ) ) ;
#7382=CARTESIAN_POINT ( 'NONE',  ( 7.999999999932789763, 3.279097096261179525E-05, 13.76780373625499010 ) ) ;
#7383=CARTESIAN_POINT ( 'NONE',  ( -5.656854249492373476, -5.656854249492376141, 13.01780277982336465 ) ) ;
#7385=CARTESIAN_POINT ( 'NONE',  ( 5.656854249492376141, -5.656854249492374365, 18.08030278392014623 ) ) ;
#7439=CARTESIAN_POINT ( 'NONE',  ( -4.898587196589407898E-16, 7.999999999999991118, 6.455302779823365533 ) ) ;
#7450=CARTESIAN_POINT ( 'NONE',  ( -5.272366635369878374, -4.893143551702760163, 0.1656094755204294555 ) ) ;
#7452=ORIENTED_EDGE ( 'NONE', *, *, #70622, .F. ) ;
#7461=VECTOR ( 'NONE', #29279, 1000.000000000000000 ) ;
#7475=CARTESIAN_POINT ( 'NONE',  ( 5.082755093536320601, -5.082755093536318824, 6.924052781871754547 ) ) ;
#7489=CARTESIAN_POINT ( 'NONE',  ( 3.313708498984756279, 7.999999999999991118, 24.54905278392014978 ) ) ;
#7509=CARTESIAN_POINT ( 'NONE',  ( 7.188101187499993827, -2.977408999572645598, 23.14280278187175810 ) ) ;
#7515=( BOUNDED_CURVE ( )  B_SPLINE_CURVE ( 2, ( #19079, #18719, #60179, #13405, #47740, #41728, #12674, #2102, #13765, #53793, #25096 ),
 .UNSPECIFIED., .F., .F. ) 
 B_SPLINE_CURVE_WITH_KNOTS ( ( 3, 2, 2, 2, 2, 3 ),
 ( 0.7412468980011663877, 0.7478651410436197855, 0.7544834166280764975, 0.7611016922125333206, 0.7677199677969902547, 0.7677200384551818857 ),
 .UNSPECIFIED. ) 
 CURVE ( )  GEOMETRIC_REPRESENTATION_ITEM ( )  RATIONAL_B_SPLINE_CURVE ( ( 0.9999992514363272855, 0.9238799067949634569, 1.000000000000000000, 0.9238795325112867385, 1.000000000000000000, 0.9238795325112867385, 1.000000000000000000, 0.9238795325112867385, 1.000000000000000000, 0.9999991873208492477, 0.9999983746590511702 ) ) 
 REPRESENTATION_ITEM ( '' )  );
#7519=CARTESIAN_POINT ( 'NONE',  ( -3.313708498984758943, -7.999999999999989342, 16.29905278392014623 ) ) ;
#7531=CARTESIAN_POINT ( 'NONE',  ( 7.188101187499993827, -2.977408999572645598, 23.14280278187176165 ) ) ;
#7536=CYLINDRICAL_SURFACE ( 'NONE', #28784, 7.999999999999991118 ) ;
#7545=CARTESIAN_POINT ( 'NONE',  ( 7.999999999714877852, 6.754118554053788561E-05, 0.2678047518895779744 ) ) ;
#7548=CARTESIAN_POINT ( 'NONE',  ( 3.317071493978883456, -8.008118988124989457, 1.481865283940630329 ) ) ;
#7555=CARTESIAN_POINT ( 'NONE',  ( 7.188101187499992051, 8.802885111219154394E-16, 22.11155278187175455 ) ) ;
#7573=CARTESIAN_POINT ( 'NONE',  ( 7.999999999999991118, 3.313708498984757611, 16.67405277982336642 ) ) ;
#7580=ORIENTED_EDGE ( 'NONE', *, *, #46814, .T. ) ;
#7586=CARTESIAN_POINT ( 'NONE',  ( 5.656854249492376141, -5.656854249492374365, 19.44905278432982598 ) ) ;
#7614=EDGE_CURVE ( 'NONE', #51761, #852, #39923, .T. ) ;
#7617=CARTESIAN_POINT ( 'NONE',  ( 5.082755093536318824, 5.082755093536319713, 14.42405278187175455 ) ) ;
#7619=EDGE_LOOP ( 'NONE', ( #2747, #3052, #8823, #58480, #46101, #32976, #43074, #46080, #68285, #40839, #30535, #26912, #39345, #19603, #54763, #67083, #6432, #2477, #45947, #61132, #13811, #34969, #12832, #41712, #73812, #13095, #34591, #59082, #22493, #1848, #23392, #19822, #73853, #38875, #15341, #71602, #2520, #48704, #10381, #65206, #3652 ) ) ;
#7643=CARTESIAN_POINT ( 'NONE',  ( 7.188101187499992051, 2.977408999572647819, 8.705302781871752771 ) ) ;
#7649=CARTESIAN_POINT ( 'NONE',  ( 7.999999999999991118, 9.797174393178815797E-16, 3.267802783920144449 ) ) ;
#7672=CARTESIAN_POINT ( 'NONE',  ( 8.000000000000035527, 3.313708498984715423, 9.174052779823362869 ) ) ;
#7687=CARTESIAN_POINT ( 'NONE',  ( 5.662595241051934458, 5.662595241051935346, 7.950615283940629219 ) ) ;
#7693=CARTESIAN_POINT ( 'NONE',  ( 7.188101187499993827, -2.977408999572645598, 6.642802781871754547 ) ) ;
#7707=CARTESIAN_POINT ( 'NONE',  ( -4.898587196589407898E-16, 7.999999999999991118, 0.6428027839201454485 ) ) ;
#7736=CARTESIAN_POINT ( 'NONE',  ( 0.000000000000000000, 0.000000000000000000, 30.00000000000000000 ) ) ;
#7750=CARTESIAN_POINT ( 'NONE',  ( 7.999999999999991118, 3.313708498984757611, 16.67405277982336642 ) ) ;
#7780=CARTESIAN_POINT ( 'NONE',  ( 7.999999999999991118, 0.000000000000000000, 30.00000000000000000 ) ) ;
#7781=CARTESIAN_POINT ( 'NONE',  ( 8.008118988124991233, 9.807117285998411148E-16, 27.26311528394063188 ) ) ;
#7803=CARTESIAN_POINT ( 'NONE',  ( -7.999999999999991118, 9.797174393178815797E-16, 30.00000000000000000 ) ) ;
#7814=CARTESIAN_POINT ( 'NONE',  ( 7.188101187499991163, 2.977408999572648707, 0.8303027818717529929 ) ) ;
#7837=CARTESIAN_POINT ( 'NONE',  ( -5.082755093536319713, 5.082755093536319713, 1.674052781871753659 ) ) ;
#7853=CARTESIAN_POINT ( 'NONE',  ( 3.313708498984762496, -7.999999999999989342, 26.98655278392014623 ) ) ;
#7871=ADVANCED_FACE ( 'NONE', ( #69824 ), #31592, .F. ) ;
#7877=CARTESIAN_POINT ( 'NONE',  ( 7.188101187499993827, -2.977408999572645598, 21.64280278187176165 ) ) ;
#7885=CARTESIAN_POINT ( 'NONE',  ( 1.469576158976822172E-15, -7.999999999999991118, 11.89280278392014445 ) ) ;
#7896=CARTESIAN_POINT ( 'NONE',  ( -7.188101187499992051, 0.000000000000000000, 17.98655278187175455 ) ) ;
#7911=CARTESIAN_POINT ( 'NONE',  ( 3.313708498984762496, -7.999999999999989342, 26.98655278392014623 ) ) ;
#7912=CARTESIAN_POINT ( 'NONE',  ( -7.999999999999991118, 0.000000000000000000, 15.83030277982336642 ) ) ;
#7918=CARTESIAN_POINT ( 'NONE',  ( -2.977408999572648707, -7.188101187499990274, 20.14280278187176165 ) ) ;
#7925=EDGE_LOOP ( 'NONE', ( #36273, #55488, #45018, #8602 ) ) ;
#7928=EDGE_CURVE ( 'NONE', #28973, #59170, #14966, .T. ) ;
#7934=DIRECTION ( 'NONE',  ( 1.000000000000000000, 0.000000000000000000, 0.000000000000000000 ) ) ;
#7937=CARTESIAN_POINT ( 'NONE',  ( 7.999999999999991118, 3.313708498984757611, 13.67405277982336287 ) ) ;
#7952=CARTESIAN_POINT ( 'NONE',  ( -3.313708498984757167, 7.999999999999991118, 20.10530278432982954 ) ) ;
#7983=CARTESIAN_POINT ( 'NONE',  ( -2.977408999572647819, 7.188101187499991163, 8.705302781871752771 ) ) ;
#8004=CARTESIAN_POINT ( 'NONE',  ( -4.401442555609577197E-16, 7.188101187499992051, 13.48655278187175455 ) ) ;
#8008=CARTESIAN_POINT ( 'NONE',  ( -7.999999999999861444, -9.580972845112835701E-07, 13.01783880491507261 ) ) ;
#8010=CARTESIAN_POINT ( 'NONE',  ( 0.000000000000000000, 0.000000000000000000, 30.00000000000000000 ) ) ;
#8011=ORIENTED_EDGE ( 'NONE', *, *, #4710, .F. ) ;
#8027=CARTESIAN_POINT ( 'NONE',  ( 7.999999999999991118, 9.797174393178815797E-16, 24.08030277982336642 ) ) ;
#8039=EDGE_CURVE ( 'NONE', #49310, #44274, #15713, .T. ) ;
#8048=CARTESIAN_POINT ( 'NONE',  ( 1.469576158976822172E-15, -7.999999999999991118, 13.20530277982336465 ) ) ;
#8050=CARTESIAN_POINT ( 'NONE',  ( -8.008118988124991233, 0.000000000000000000, 10.01311528394063011 ) ) ;
#8059=CARTESIAN_POINT ( 'NONE',  ( -4.401442555609577197E-16, 7.188101187499992051, 5.611552781871753659 ) ) ;
#8073=CARTESIAN_POINT ( 'NONE',  ( 5.656854249492376141, -5.656854249492374365, 4.580302783920145338 ) ) ;
#8095=CARTESIAN_POINT ( 'NONE',  ( -8.000000000000033751, -3.313708498984719864, 3.924052779823361092 ) ) ;
#8097=FACE_OUTER_BOUND ( 'NONE', #7925, .T. ) ;
#8103=VERTEX_POINT ( 'NONE', #50055 ) ;
#8114=CARTESIAN_POINT ( 'NONE',  ( -3.313708498984759387, -7.999999999999989342, 13.29905278392014800 ) ) ;
#8115=CARTESIAN_POINT ( 'NONE',  ( -3.313708498984757167, 7.999999999999991118, 14.04905277982336465 ) ) ;
#8138=DIRECTION ( 'NONE',  ( 1.000000000000000000, 0.000000000000000000, 0.000000000000000000 ) ) ;
#8146=CARTESIAN_POINT ( 'NONE',  ( -8.008118988124989457, -3.317071493978883900, 25.10686528394063544 ) ) ;
#8174=CARTESIAN_POINT ( 'NONE',  ( 7.999999999999991118, 0.000000000000000000, 30.00000000000000000 ) ) ;
#8178=CARTESIAN_POINT ( 'NONE',  ( -7.188101187499992051, 0.000000000000000000, 27.36155278187175455 ) ) ;
#8202=CARTESIAN_POINT ( 'NONE',  ( -7.188101187499990274, -2.977408999572651371, 1.955302781871753881 ) ) ;
#8217=CARTESIAN_POINT ( 'NONE',  ( -7.999999999970034636, -1.442163225726577833E-05, 17.51834960462420909 ) ) ;
#8219=CARTESIAN_POINT ( 'NONE',  ( 3.313708498984756279, 7.999999999999991118, 18.54905278392014623 ) ) ;
#8240=CARTESIAN_POINT ( 'NONE',  ( 5.082755093536320601, -5.082755093536318824, 21.54905278187175455 ) ) ;
#8246=CARTESIAN_POINT ( 'NONE',  ( -4.898587196589407898E-16, 7.999999999999991118, 11.14280278392014800 ) ) ;
#8248=ORIENTED_EDGE ( 'NONE', *, *, #22473, .T. ) ;
#8258=CARTESIAN_POINT ( 'NONE',  ( 5.082755093536318824, 5.082755093536319713, 17.42405278187175810 ) ) ;
#8278=CARTESIAN_POINT ( 'NONE',  ( -3.313708498984757167, 7.999999999999991118, 24.73655278392014978 ) ) ;
#8285=CARTESIAN_POINT ( 'NONE',  ( 5.082755093536320601, -5.082755093536318824, 23.42405278187175455 ) ) ;
#8301=CARTESIAN_POINT ( 'NONE',  ( 5.656854249492374365, 5.656854249492375253, 18.26780277982336642 ) ) ;
#8316=CARTESIAN_POINT ( 'NONE',  ( 0.000000000000000000, 0.000000000000000000, 30.00000000000000000 ) ) ;
#8317=CARTESIAN_POINT ( 'NONE',  ( -7.999999999999991118, 3.313708498984756723, 20.29280278432982954 ) ) ;
#8346=CARTESIAN_POINT ( 'NONE',  ( 2.977408999572650927, -7.188101187499990274, 6.455302781871754547 ) ) ;
#8371=CARTESIAN_POINT ( 'NONE',  ( -2.977408999572647819, 7.188101187499992051, 4.580302781871752771 ) ) ;
#8395=CARTESIAN_POINT ( 'NONE',  ( 1.469576158976822172E-15, -7.999999999999991118, 1.205302779823363979 ) ) ;
#8402=CARTESIAN_POINT ( 'NONE',  ( -4.898587196589407898E-16, 7.999999999999991118, 5.142802783920146226 ) ) ;
#8419=CARTESIAN_POINT ( 'NONE',  ( 8.008118988124991233, 3.317071493978879015, 7.856865283940629219 ) ) ;
#8425=CARTESIAN_POINT ( 'NONE',  ( 7.188101187499992051, 8.802885111219154394E-16, 5.236552781871753659 ) ) ;
#8431=EDGE_CURVE ( 'NONE', #51609, #44274, #68784, .T. ) ;
#8437=CARTESIAN_POINT ( 'NONE',  ( 2.977408999572650927, -7.188101187499990274, 25.95530278187175455 ) ) ;
#8442=CARTESIAN_POINT ( 'NONE',  ( 7.999999999999991118, 9.797174393178815797E-16, 10.58030277982336465 ) ) ;
#8446=ADVANCED_FACE ( 'NONE', ( #26195 ), #48096, .F. ) ;
#8456=CARTESIAN_POINT ( 'NONE',  ( -7.999999999994261479, 6.398094505892175214E-06, 25.01756343669228499 ) ) ;
#8462=CARTESIAN_POINT ( 'NONE',  ( -5.082755093536319713, 5.082755093536319713, 25.67405278187175810 ) ) ;
#8480=CARTESIAN_POINT ( 'NONE',  ( 1.469576158976822172E-15, -7.999999999999991118, 13.39280278392014623 ) ) ;
#8481=CARTESIAN_POINT ( 'NONE',  ( 5.656854249492374365, 5.656854249492375253, 10.76780277982336642 ) ) ;
#8483=CARTESIAN_POINT ( 'NONE',  ( -3.313708498984759387, -7.999999999999989342, 17.79905278392014623 ) ) ;
#8491=EDGE_CURVE ( 'NONE', #16032, #31550, #35536, .T. ) ;
#8513=CARTESIAN_POINT ( 'NONE',  ( -3.317071493978880348, -8.008118988124989457, 25.29436528394063544 ) ) ;
#8550=CARTESIAN_POINT ( 'NONE',  ( -2.977408999572648707, -7.188101187499990274, 27.64280278187175810 ) ) ;
#8552=CARTESIAN_POINT ( 'NONE',  ( -7.999999999998400391, 3.416934844025491914E-06, 16.01767659775488184 ) ) ;
#8562=LINE ( 'NONE', #71181, #57928 ) ;
#8575=CARTESIAN_POINT ( 'NONE',  ( -7.188101187499991163, 2.977408999572646930, 6.267802781871754547 ) ) ;
#8592=CARTESIAN_POINT ( 'NONE',  ( -5.656854249492373476, -5.656854249492376141, 17.70530278392014623 ) ) ;
#8593=CYLINDRICAL_SURFACE ( 'NONE', #43281, 7.999999999999991118 ) ;
#8602=ORIENTED_EDGE ( 'NONE', *, *, #22072, .F. ) ;
#8614=CARTESIAN_POINT ( 'NONE',  ( -7.188101187499992051, 2.977408999572646930, 20.89280278187176521 ) ) ;
#8616=CARTESIAN_POINT ( 'NONE',  ( 5.656854249492376141, -5.656854249492374365, 16.58030278392014978 ) ) ;
#8625=( BOUNDED_CURVE ( )  B_SPLINE_CURVE ( 2, ( #42469, #65486, #67353, #15651, #56410, #43966, #38692, #3992, #66975, #60942, #15278 ),
 .UNSPECIFIED., .F., .F. ) 
 B_SPLINE_CURVE_WITH_KNOTS ( ( 3, 2, 2, 2, 2, 3 ),
 ( 0.1588385999027599471, 0.1588386140269634761, 0.1654568896114202992, 0.1720751651958771222, 0.1786934407803339175, 0.1853116620478932886 ),
 .UNSPECIFIED. ) 
 CURVE ( )  GEOMETRIC_REPRESENTATION_ITEM ( )  RATIONAL_B_SPLINE_CURVE ( ( 0.9999996751000569395, 0.9999998375496818026, 1.000000000000000000, 0.9238795325112867385, 1.000000000000000000, 0.9238795325112867385, 1.000000000000000000, 0.9238795325112867385, 1.000000000000000000, 0.9238801572401263984, 0.9999987505525751441 ) ) 
 REPRESENTATION_ITEM ( '' )  );
#8627=CARTESIAN_POINT ( 'NONE',  ( -4.898587196589407898E-16, 7.999999999999991118, 15.64280278392014800 ) ) ;
#8632=CARTESIAN_POINT ( 'NONE',  ( -7.999999999999991118, 0.000000000000000000, 12.83030277982336465 ) ) ;
#8637=CARTESIAN_POINT ( 'NONE',  ( -5.082755093536319713, 5.082755093536319713, 17.79905278187175455 ) ) ;
#8656=CARTESIAN_POINT ( 'NONE',  ( -5.656854249492375253, 5.656854249492375253, 27.83030278392014978 ) ) ;
#8663=CARTESIAN_POINT ( 'NONE',  ( -7.188101187499991163, 2.977408999572646930, 22.76780278187175455 ) ) ;
#8678=CARTESIAN_POINT ( 'NONE',  ( -7.999999999999991118, 0.000000000000000000, 11.33030277982336642 ) ) ;
#8693=FACE_OUTER_BOUND ( 'NONE', #57978, .T. ) ;
#8694=CARTESIAN_POINT ( 'NONE',  ( -5.656854249492375253, 5.656854249492375253, 11.19905278432982243 ) ) ;
#8696=CARTESIAN_POINT ( 'NONE',  ( 1.469576158976822172E-15, -7.999999999999991118, 16.20530277982336287 ) ) ;
#8699=VERTEX_POINT ( 'NONE', #23899 ) ;
#8728=CARTESIAN_POINT ( 'NONE',  ( -4.401442555609577197E-16, 7.188101187499992051, 7.111552781871751883 ) ) ;
#8741=CARTESIAN_POINT ( 'NONE',  ( 7.188101187499993827, -2.977408999572645598, 14.51780278187175455 ) ) ;
#8754=CARTESIAN_POINT ( 'NONE',  ( -7.188101187499992051, 0.000000000000000000, 1.861552781871753881 ) ) ;
#8758=CARTESIAN_POINT ( 'NONE',  ( -7.999999999999991118, 9.797174393178815797E-16, 30.00000000000000000 ) ) ;
#8771=CARTESIAN_POINT ( 'NONE',  ( 5.656854249492374365, 5.656854249492375253, 28.76780277982336642 ) ) ;
#8783=CARTESIAN_POINT ( 'NONE',  ( -4.898587196589407898E-16, 7.999999999999991118, 6.642802783920143561 ) ) ;
#8790=EDGE_CURVE ( 'NONE', #33251, #73315, #27358, .T. ) ;
#8800=CARTESIAN_POINT ( 'NONE',  ( -4.903558642999205574E-16, 8.008118988124991233, 8.138115283940630107 ) ) ;
#8808=CARTESIAN_POINT ( 'NONE',  ( 2.977408999572646486, 7.188101187499992051, 1.017802781871752993 ) ) ;
#8820=CARTESIAN_POINT ( 'NONE',  ( 7.188101187499991163, 2.977408999572648707, 26.33030278187175810 ) ) ;
#8823=ORIENTED_EDGE ( 'NONE', *, *, #37181, .F. ) ;
#8825=CARTESIAN_POINT ( 'NONE',  ( -7.999999999999992895, 4.898587196589407898E-16, 0.000000000000000000 ) ) ;
#8844=CARTESIAN_POINT ( 'NONE',  ( 5.082755093536320601, -5.082755093536318824, 23.42405278187175455 ) ) ;
#8850=CARTESIAN_POINT ( 'NONE',  ( 7.999999999999991118, 3.313708498984758055, 25.67405277982336997 ) ) ;
#8863=CARTESIAN_POINT ( 'NONE',  ( -5.656854249492375253, 5.656854249492375253, 11.14280277982336642 ) ) ;
#8867=CARTESIAN_POINT ( 'NONE',  ( -7.999999999974042098, 1.357258486152048259E-05, 14.51729352187485311 ) ) ;
#8871=CARTESIAN_POINT ( 'NONE',  ( 5.656854249492374365, 5.656854249492375253, 4.955302783920146226 ) ) ;
#8890=FACE_OUTER_BOUND ( 'NONE', #1948, .T. ) ;
#8908=EDGE_CURVE ( 'NONE', #471, #59945, #61066, .T. ) ;
#8911=DIRECTION ( 'NONE',  ( -0.000000000000000000, -0.9659258262890698665, -0.2588190451025146332 ) ) ;
#8924=CARTESIAN_POINT ( 'NONE',  ( -2.977408999572647819, 7.188101187499991163, 1.205302781871753215 ) ) ;
#8950=CARTESIAN_POINT ( 'NONE',  ( 5.082755093536320601, -5.082755093536318824, 0.9240527818717529929 ) ) ;
#8968=CARTESIAN_POINT ( 'NONE',  ( -5.656854249492373476, -5.656854249492376141, 19.20530278392014978 ) ) ;
#8991=CARTESIAN_POINT ( 'NONE',  ( -7.188101187499992051, 0.000000000000000000, 23.98655278187175455 ) ) ;
#9000=CARTESIAN_POINT ( 'NONE',  ( -3.313708498984758943, -7.999999999999989342, 11.79905278392014800 ) ) ;
#9002=CARTESIAN_POINT ( 'NONE',  ( -7.999999999999991118, 0.000000000000000000, 19.01780278392014623 ) ) ;
#9012=CARTESIAN_POINT ( 'NONE',  ( 7.188101187499993827, -2.977408999572645598, 17.14280278187175455 ) ) ;
#9024=AXIS2_PLACEMENT_3D ( 'NONE', #14547, #8911, #30804 ) ;
#9031=CARTESIAN_POINT ( 'NONE',  ( 7.999999999999992895, -3.313708498984756279, 27.17405278392014978 ) ) ;
#9037=CARTESIAN_POINT ( 'NONE',  ( 5.082755093536318824, 5.082755093536319713, 17.79905278187175810 ) ) ;
#9053=CARTESIAN_POINT ( 'NONE',  ( -7.999999999999991118, 3.313708498984756723, 9.736552779823368198 ) ) ;
#9072=CARTESIAN_POINT ( 'NONE',  ( -7.999999999999991118, 0.000000000000000000, 12.88655278432982421 ) ) ;
#9103=CARTESIAN_POINT ( 'NONE',  ( -7.188101187499990274, -2.977408999572651371, 6.080302781871753659 ) ) ;
#9115=CARTESIAN_POINT ( 'NONE',  ( -2.977408999572647819, 7.188101187499991163, 12.08030278187175099 ) ) ;
#9126=CARTESIAN_POINT ( 'NONE',  ( -7.188101187499992051, 2.977408999572646930, 3.267802781871751439 ) ) ;
#9141=CARTESIAN_POINT ( 'NONE',  ( 3.313708498984762496, -7.999999999999989342, 25.29905277982336642 ) ) ;
#9155=CARTESIAN_POINT ( 'NONE',  ( 1.469576158976822172E-15, -7.999999999999991118, 1.392802783920146004 ) ) ;
#9176=CARTESIAN_POINT ( 'NONE',  ( 7.188101187499992051, 2.977408999572647819, 2.330302781871750550 ) ) ;
#9188=CARTESIAN_POINT ( 'NONE',  ( 5.082755093536320601, -5.082755093536318824, 27.54905278187175455 ) ) ;
#9204=EDGE_CURVE ( 'NONE', #26236, #3963, #71197, .T. ) ;
#9214=CARTESIAN_POINT ( 'NONE',  ( 7.188101187499993827, -2.977408999572645598, 25.01780278187175810 ) ) ;
#9216=CARTESIAN_POINT ( 'NONE',  ( -7.999980374704816377, -3.313728124279936349, 22.11155356913438652 ) ) ;
#9233=CARTESIAN_POINT ( 'NONE',  ( -7.999999999999991118, 3.313708498984756723, 9.736552779823368198 ) ) ;
#9262=CARTESIAN_POINT ( 'NONE',  ( -8.008118988124991233, 3.317071493978878127, 23.41936528394063544 ) ) ;
#9269=ORIENTED_EDGE ( 'NONE', *, *, #65422, .F. ) ;
#9297=CARTESIAN_POINT ( 'NONE',  ( 1.320432766682872962E-15, -7.188101187499992051, 26.23655278187175810 ) ) ;
#9317=EDGE_CURVE ( 'NONE', #12693, #30893, #5774, .T. ) ;
#9326=CARTESIAN_POINT ( 'NONE',  ( 3.313708498984762496, -7.999999999999989342, 28.29905277982336997 ) ) ;
#9329=EDGE_LOOP ( 'NONE', ( #12937, #63073, #28781, #27236 ) ) ;
#9330=DIRECTION ( 'NONE',  ( -0.000000000000000000, -0.000000000000000000, 1.000000000000000000 ) ) ;
#9332=CARTESIAN_POINT ( 'NONE',  ( 3.313708498984762496, -7.999999999999989342, 14.79905277982336642 ) ) ;
#9340=CARTESIAN_POINT ( 'NONE',  ( 1.469576158976822172E-15, -7.999999999999991118, 11.70530277982336642 ) ) ;
#9344=CARTESIAN_POINT ( 'NONE',  ( -4.898587196589407898E-16, 7.999999999999991118, 17.14280278392014978 ) ) ;
#9354=CARTESIAN_POINT ( 'NONE',  ( -5.656854249492373476, -5.656854249492376141, 26.70530278392014623 ) ) ;
#9357=DIRECTION ( 'NONE',  ( -0.000000000000000000, -0.000000000000000000, 1.000000000000000000 ) ) ;
#9364=CARTESIAN_POINT ( 'NONE',  ( 2.977408999572650927, -7.188101187499990274, 13.95530278187175455 ) ) ;
#9365=CARTESIAN_POINT ( 'NONE',  ( 7.999999999981424637, 1.723583929636134980E-05, 16.76780327155163874 ) ) ;
#9374=CARTESIAN_POINT ( 'NONE',  ( -3.313708498984758943, -7.999999999999989342, 8.799052783920144449 ) ) ;
#9376=CARTESIAN_POINT ( 'NONE',  ( -5.656854249492375253, 5.656854249492375253, 18.83030278392014623 ) ) ;
#9387=CARTESIAN_POINT ( 'NONE',  ( 2.977408999572646486, 7.188101187499991163, 16.01780278187175455 ) ) ;
#9404=VERTEX_POINT ( 'NONE', #13919 ) ;
#9408=CARTESIAN_POINT ( 'NONE',  ( -3.313708498984758943, -7.999999999999989342, 25.29905278392014623 ) ) ;
#9415=CARTESIAN_POINT ( 'NONE',  ( 2.977408999572646486, 7.188101187499991163, 13.39280278187175455 ) ) ;
#9433=CARTESIAN_POINT ( 'NONE',  ( 1.469576158976822172E-15, -7.999999999999991118, 7.205302779823365533 ) ) ;
#9450=CARTESIAN_POINT ( 'NONE',  ( -7.999999999999991118, 3.313708498984756723, 14.29280278432982598 ) ) ;
#9484=CARTESIAN_POINT ( 'NONE',  ( -7.188101187499991163, 2.977408999572646930, 7.392802781871750994 ) ) ;
#9497=CARTESIAN_POINT ( 'NONE',  ( 2.977408999572650927, -7.188101187499990274, 14.33030278187175277 ) ) ;
#9508=LINE ( 'NONE', #32523, #30149 ) ;
#9512=CARTESIAN_POINT ( 'NONE',  ( 7.188101187499992051, 2.977408999572647819, 7.205302781871755435 ) ) ;
#9528=CARTESIAN_POINT ( 'NONE',  ( -3.313708498984757167, 7.999999999999991118, 29.04905277982337353 ) ) ;
#9541=CARTESIAN_POINT ( 'NONE',  ( -7.999999999999991118, 3.313708498984756723, 2.424052783920144005 ) ) ;
#9562=CARTESIAN_POINT ( 'NONE',  ( -5.082755093536319713, 5.082755093536319713, 2.799052781871750994 ) ) ;
#9575=CARTESIAN_POINT ( 'NONE',  ( -5.082755093536317936, -5.082755093536320601, 25.67405278187175810 ) ) ;
#9592=CARTESIAN_POINT ( 'NONE',  ( -4.898587196589407898E-16, 7.999999999999991118, 24.64280278392014978 ) ) ;
#9598=CARTESIAN_POINT ( 'NONE',  ( 2.977408999572646486, 7.188101187499992051, 23.89280278187175810 ) ) ;
#9608=CARTESIAN_POINT ( 'NONE',  ( -6.062591786044946751, -5.219672483564715471, -0.3118205092643556720 ) ) ;
#9616=CARTESIAN_POINT ( 'NONE',  ( -3.313708498984757167, 7.999999999999991118, 9.549052779823362869 ) ) ;
#9623=CARTESIAN_POINT ( 'NONE',  ( -5.656854249492375253, 5.656854249492375253, 14.33030278392014800 ) ) ;
#9629=CARTESIAN_POINT ( 'NONE',  ( 7.999999999999991118, -2.975320552349488356E-08, 19.76780278304987348 ) ) ;
#9643=ORIENTED_EDGE ( 'NONE', *, *, #9317, .T. ) ;
#9645=CARTESIAN_POINT ( 'NONE',  ( -5.662595241051935346, 5.662595241051935346, 21.82561528394063188 ) ) ;
#9680=CARTESIAN_POINT ( 'NONE',  ( 2.977408999572646486, 7.188101187499991163, 22.39280278187175810 ) ) ;
#9686=DIRECTION ( 'NONE',  ( -0.000000000000000000, -0.9659258262890698665, -0.2588190451025146332 ) ) ;
#9704=CARTESIAN_POINT ( 'NONE',  ( -5.447323953993864265, -4.689931814214729933, 0.5319290643893268555 ) ) ;
#9721=CARTESIAN_POINT ( 'NONE',  ( -7.999999999999991118, 0.000000000000000000, 20.51780278392014623 ) ) ;
#9732=FACE_OUTER_BOUND ( 'NONE', #59974, .T. ) ;
#9742=CARTESIAN_POINT ( 'NONE',  ( -7.188101187499992051, 2.977408999572646930, 13.39280278187175277 ) ) ;
#9753=ORIENTED_EDGE ( 'NONE', *, *, #19987, .T. ) ;
#9756=CARTESIAN_POINT ( 'NONE',  ( 5.656854249492374365, 5.656854249492375253, 6.455302783920143561 ) ) ;
#9761=CARTESIAN_POINT ( 'NONE',  ( 5.656854249492374365, 5.656854249492375253, 12.26780277982336642 ) ) ;
#9767=CARTESIAN_POINT ( 'NONE',  ( 5.082755093536320601, -5.082755093536318824, 12.54905278187175277 ) ) ;
#9773=CARTESIAN_POINT ( 'NONE',  ( 3.313708498984762496, -7.999999999999989342, 23.98655278392014978 ) ) ;
#9790=CARTESIAN_POINT ( 'NONE',  ( -5.082755093536317936, -5.082755093536320601, 14.04905278187175455 ) ) ;
#9806=CARTESIAN_POINT ( 'NONE',  ( -3.313708498984757167, 7.999999999999991118, 8.049052779823362869 ) ) ;
#9807=CARTESIAN_POINT ( 'NONE',  ( -7.999999999999991118, 3.313708498984757167, 21.92405278392014978 ) ) ;
#9819=CARTESIAN_POINT ( 'NONE',  ( -7.999999999999991118, 0.000000000000000000, 14.38655278432982598 ) ) ;
#9849=CARTESIAN_POINT ( 'NONE',  ( -3.313708498984757611, 7.999999999999991118, 17.04905277982336642 ) ) ;
#9853=CARTESIAN_POINT ( 'NONE',  ( 5.082755093536318824, 5.082755093536319713, 27.92405278187175455 ) ) ;
#9857=CARTESIAN_POINT ( 'NONE',  ( 5.656854249492374365, 5.656854249492375253, 19.76780277982336642 ) ) ;
#9865=CARTESIAN_POINT ( 'NONE',  ( -7.188101187499990274, -2.977408999572651371, 12.45530278187175277 ) ) ;
#9879=CARTESIAN_POINT ( 'NONE',  ( 5.082755093536318824, 5.082755093536319713, 7.299052781871751883 ) ) ;
#9894=CARTESIAN_POINT ( 'NONE',  ( -7.999999999999991118, 0.000000000000000000, 27.83030277982336642 ) ) ;
#9904=CARTESIAN_POINT ( 'NONE',  ( -4.898587196589407898E-16, 7.999999999999991118, 0.6428027839201454485 ) ) ;
#9939=CARTESIAN_POINT ( 'NONE',  ( -2.977408999572647819, 7.188101187499991163, 22.20530278187175455 ) ) ;
#9965=CARTESIAN_POINT ( 'NONE',  ( 1.320432766682872962E-15, -7.188101187499992051, 24.73655278187175810 ) ) ;
#9974=CARTESIAN_POINT ( 'NONE',  ( 7.999999999999992895, -9.797174393178815797E-16, 0.000000000000000000 ) ) ;
#9984=CARTESIAN_POINT ( 'NONE',  ( 3.313708498984756279, 7.999999999999991118, 7.861552779823362869 ) ) ;
#9989=CARTESIAN_POINT ( 'NONE',  ( -7.999999999999991118, 1.438550051402736141E-05, 14.51780237693182052 ) ) ;
#9998=CARTESIAN_POINT ( 'NONE',  ( -7.999999999999991118, 0.000000000000000000, 20.51780278392014623 ) ) ;
#10011=ADVANCED_FACE ( 'NONE', ( #38655 ), #46901, .F. ) ;
#10015=CARTESIAN_POINT ( 'NONE',  ( -8.008118988124991233, 3.317071493978878127, 18.91936528394063544 ) ) ;
#10020=CARTESIAN_POINT ( 'NONE',  ( -5.447321192899549303, -4.689935021205116961, 0.1569292013794422458 ) ) ;
#10033=ORIENTED_EDGE ( 'NONE', *, *, #67632, .T. ) ;
#10035=CARTESIAN_POINT ( 'NONE',  ( -7.999999999946576068, -3.313708499038175770, 8.611552783922281407 ) ) ;
#10045=CARTESIAN_POINT ( 'NONE',  ( -4.401442555609577197E-16, 7.188101187499992051, 20.98655278187175455 ) ) ;
#10071=CARTESIAN_POINT ( 'NONE',  ( 3.313708498984762496, -7.999999999999989342, 26.79905277982337353 ) ) ;
#10089=CARTESIAN_POINT ( 'NONE',  ( -7.999999999999991118, 0.000000000000000000, 13.01780278392014623 ) ) ;
#10092=CARTESIAN_POINT ( 'NONE',  ( 0.000000000000000000, 0.000000000000000000, 30.00000000000000000 ) ) ;
#10110=CARTESIAN_POINT ( 'NONE',  ( -5.082755093536319713, 5.082755093536319713, 13.29905278187175277 ) ) ;
#10118=EDGE_LOOP ( 'NONE', ( #37873, #56927, #71962, #20003 ) ) ;
#10125=CARTESIAN_POINT ( 'NONE',  ( 3.313708498984756279, 7.999999999999991118, 12.36155277982336820 ) ) ;
#10131=CARTESIAN_POINT ( 'NONE',  ( 7.188101187499991163, 2.977408999572648707, 11.33030278187175632 ) ) ;
#10136=CARTESIAN_POINT ( 'NONE',  ( 7.999999999999991118, 9.797174393178815797E-16, 18.08030277982336642 ) ) ;
#10138=DIRECTION ( 'NONE',  ( -0.000000000000000000, -0.000000000000000000, 1.000000000000000000 ) ) ;
#10157=CARTESIAN_POINT ( 'NONE',  ( -2.977408999572647819, 7.188101187499991163, 15.08030278187175455 ) ) ;
#10166=EDGE_CURVE ( 'NONE', #73412, #73226, #53316, .T. ) ;
#10174=CARTESIAN_POINT ( 'NONE',  ( -7.999999999999989342, -3.313708498984762496, 8.424052779823362869 ) ) ;
#10175=CARTESIAN_POINT ( 'NONE',  ( -4.898587196589407898E-16, 7.999999999999991118, 21.64280278392014623 ) ) ;
#10190=CARTESIAN_POINT ( 'NONE',  ( 7.999978819527651552, -3.313729679457098065, 3.174051936482769953 ) ) ;
#10192=CARTESIAN_POINT ( 'NONE',  ( -5.656854249492373476, -5.656854249492376141, 10.07405278432982421 ) ) ;
#10216=CARTESIAN_POINT ( 'NONE',  ( 7.999999999999991118, 3.313708498984758055, 9.361552783920146226 ) ) ;
#10222=CARTESIAN_POINT ( 'NONE',  ( 7.188101187499992051, 8.802885111219154394E-16, 27.73655278187175455 ) ) ;
#10235=CARTESIAN_POINT ( 'NONE',  ( 2.977408999572646486, 7.188101187499991163, 4.392802781871752771 ) ) ;
#10249=CARTESIAN_POINT ( 'NONE',  ( -7.188101187499992051, 2.977408999572646930, 1.767802781871753437 ) ) ;
#10266=CARTESIAN_POINT ( 'NONE',  ( -4.898587196589407898E-16, 7.999999999999991118, 28.95530277982336642 ) ) ;
#10278=CARTESIAN_POINT ( 'NONE',  ( 3.313708498984762496, -7.999999999999989342, 26.85530278432982598 ) ) ;
#10311=CARTESIAN_POINT ( 'NONE',  ( -7.188101187499992051, 0.000000000000000000, 19.48655278187175455 ) ) ;
#10336=CARTESIAN_POINT ( 'NONE',  ( 2.977408999572646486, 7.188101187499992051, 14.89280278187175455 ) ) ;
#10355=CARTESIAN_POINT ( 'NONE',  ( 3.313708498984756279, 7.999999999999991118, 4.861552779823364645 ) ) ;
#10356=CARTESIAN_POINT ( 'NONE',  ( 1.469576158976822172E-15, -7.999999999999991118, 20.89280278392014623 ) ) ;
#10381=ORIENTED_EDGE ( 'NONE', *, *, #62110, .F. ) ;
#10383=CARTESIAN_POINT ( 'NONE',  ( 1.471067592899761672E-15, -8.008118988124991233, 19.38811528394063188 ) ) ;
#10395=( BOUNDED_CURVE ( )  B_SPLINE_CURVE ( 2, ( #58824, #54646, #42184, #7135, #24833, #64838, #13871, #30143, #2953, #25943, #31248 ),
 .UNSPECIFIED., .F., .F. ) 
 B_SPLINE_CURVE_WITH_KNOTS ( ( 3, 2, 2, 2, 2, 3 ),
 ( 0.5559351258181921551, 0.5559351490943722496, 0.5625534246788289616, 0.5691717002632856737, 0.5757899758477422747, 0.5824082574719842142 ),
 .UNSPECIFIED. ) 
 CURVE ( )  GEOMETRIC_REPRESENTATION_ITEM ( )  RATIONAL_B_SPLINE_CURVE ( ( 0.9999994645773038204, 0.9999997322877103301, 1.000000000000000000, 0.9238795325112867385, 1.000000000000000000, 0.9238795325112867385, 1.000000000000000000, 0.9238795325112867385, 1.000000000000000000, 0.9238795325112867385, 1.000000000000000000 ) ) 
 REPRESENTATION_ITEM ( '' )  );
#10415=CARTESIAN_POINT ( 'NONE',  ( -4.401442555609577197E-16, 7.188101187499992051, 25.48655278187175810 ) ) ;
#10441=CARTESIAN_POINT ( 'NONE',  ( -5.272366635369878374, -4.893143551702760163, 0.5406094755204297053 ) ) ;
#10448=CARTESIAN_POINT ( 'NONE',  ( -3.313708498984759387, -7.999999999999989342, 8.611552779823364645 ) ) ;
#10458=CARTESIAN_POINT ( 'NONE',  ( 5.656854249492376141, -5.656854249492374365, 12.08030278392014445 ) ) ;
#10480=CARTESIAN_POINT ( 'NONE',  ( 2.977408999572646486, 7.188101187499992051, 16.01780278187175099 ) ) ;
#10492=FACE_OUTER_BOUND ( 'NONE', #62120, .T. ) ;
#10505=CARTESIAN_POINT ( 'NONE',  ( 7.188101187499991163, 2.977408999572648707, 9.830302781871752771 ) ) ;
#10511=CARTESIAN_POINT ( 'NONE',  ( -5.656854249492373476, -5.656854249492376141, 23.70530278392014978 ) ) ;
#10517=CARTESIAN_POINT ( 'NONE',  ( -7.999999999999991118, 9.797174393178815797E-16, 30.00000000000000000 ) ) ;
#10529=CARTESIAN_POINT ( 'NONE',  ( 7.188101187499993827, -2.977408999572645598, 14.51780278187175455 ) ) ;
#10545=CARTESIAN_POINT ( 'NONE',  ( 5.656854249492374365, 5.656854249492375253, 4.767802779823363757 ) ) ;
#10562=CARTESIAN_POINT ( 'NONE',  ( 5.656854249492376141, -5.656854249492374365, 7.449052784329822430 ) ) ;
#10563=CARTESIAN_POINT ( 'NONE',  ( -7.999999999999948486, 3.313708498984799355, 5.236552779823361981 ) ) ;
#10572=EDGE_LOOP ( 'NONE', ( #20197, #49414, #47455, #18746 ) ) ;
#10592=CARTESIAN_POINT ( 'NONE',  ( -7.999999999999991118, 0.000000000000000000, 3.830302779823362869 ) ) ;
#10593=CARTESIAN_POINT ( 'NONE',  ( -7.188101187499990274, -2.977408999572651371, 1.580302781871753437 ) ) ;
#10594=ORIENTED_EDGE ( 'NONE', *, *, #8491, .T. ) ;
#10606=CIRCLE ( 'NONE', #51584, 15.99999999999998579 ) ;
#10608=CARTESIAN_POINT ( 'NONE',  ( -5.082755093536317936, -5.082755093536320601, 6.549052781871754547 ) ) ;
#10618=CYLINDRICAL_SURFACE ( 'NONE', #52026, 7.999999999999991118 ) ;
#10636=CARTESIAN_POINT ( 'NONE',  ( -7.999999999999991118, 0.000000000000000000, 18.83030277982336642 ) ) ;
#10647=CARTESIAN_POINT ( 'NONE',  ( -5.656854249492373476, -5.656854249492376141, 1.205302783920146004 ) ) ;
#10666=CARTESIAN_POINT ( 'NONE',  ( 0.000000000000000000, -16.70329308849007077, 0.000000000000000000 ) ) ;
#10669=CARTESIAN_POINT ( 'NONE',  ( 7.999999999999991118, 9.797174393178815797E-16, 6.080302779823364645 ) ) ;
#10674=EDGE_CURVE ( 'NONE', #25965, #38243, #8625, .T. ) ;
#10680=CARTESIAN_POINT ( 'NONE',  ( -7.188101187499991163, 2.977408999572646930, 16.39280278187175455 ) ) ;
#10701=CARTESIAN_POINT ( 'NONE',  ( 5.082755093536320601, -5.082755093536318824, 18.92405278187175455 ) ) ;
#10750=CARTESIAN_POINT ( 'NONE',  ( 5.662595241051934458, 5.662595241051935346, 18.45061528394063188 ) ) ;
#10784=CARTESIAN_POINT ( 'NONE',  ( -7.188101187499991163, 2.977408999572646930, 21.26780278187175810 ) ) ;
#10811=CARTESIAN_POINT ( 'NONE',  ( 3.313708498984762496, -7.999999999999989342, 22.29905277982336287 ) ) ;
#10817=CARTESIAN_POINT ( 'NONE',  ( 5.656854249492376141, -5.656854249492374365, 8.892802779823364645 ) ) ;
#10826=CARTESIAN_POINT ( 'NONE',  ( 3.313708498984762496, -7.999999999999989342, 11.79905277982336465 ) ) ;
#10829=CARTESIAN_POINT ( 'NONE',  ( 7.999999999999991118, 9.797174393178815797E-16, 15.26780278392014623 ) ) ;
#10878=CARTESIAN_POINT ( 'NONE',  ( 7.188101187499992051, 8.802885111219154394E-16, 11.23655278187175455 ) ) ;
#10884=CARTESIAN_POINT ( 'NONE',  ( 1.469576158976822172E-15, -7.999999999999991118, 23.89280278392014978 ) ) ;
#10903=CARTESIAN_POINT ( 'NONE',  ( 2.977408999572650927, -7.188101187499990274, 8.330302781871752771 ) ) ;
#10907=CARTESIAN_POINT ( 'NONE',  ( 7.999999999999991118, 9.797174393178815797E-16, 1.636552784329821097 ) ) ;
#10918=CARTESIAN_POINT ( 'NONE',  ( -9.121419926064122663, -1.666886344965055722, 0.8643199637478004016 ) ) ;
#10934=CARTESIAN_POINT ( 'NONE',  ( 7.999999999999991118, 9.797174393178815797E-16, 4.636552784329823318 ) ) ;
#10935=EDGE_CURVE ( 'NONE', #471, #22871, #60682, .T. ) ;
#10946=EDGE_CURVE ( 'NONE', #29054, #51609, #950, .T. ) ;
#10966=CARTESIAN_POINT ( 'NONE',  ( -2.977408999572648707, -7.188101187499990274, 1.767802781871753881 ) ) ;
#10981=CARTESIAN_POINT ( 'NONE',  ( -7.188101187499990274, -2.977408999572651371, 7.955302781871752771 ) ) ;
#10996=CARTESIAN_POINT ( 'NONE',  ( 0.000000000000000000, 130.3999865490244190, 45.94057108883949070 ) ) ;
#11010=CARTESIAN_POINT ( 'NONE',  ( -7.999999999999989342, -3.313708498984762496, 20.42405277982336642 ) ) ;
#11018=CARTESIAN_POINT ( 'NONE',  ( 7.999999999999991118, 9.797174393178815797E-16, 0.2678027839201451155 ) ) ;
#11024=CARTESIAN_POINT ( 'NONE',  ( 7.999999999999991118, 9.797174393178815797E-16, 21.13655278432982243 ) ) ;
#11032=CARTESIAN_POINT ( 'NONE',  ( 8.000000000000001776, 3.313708498984747397, 24.17405277982336997 ) ) ;
#11058=CARTESIAN_POINT ( 'NONE',  ( 1.320432766682872962E-15, -7.188101187499992051, 19.86155278187175455 ) ) ;
#11077=CARTESIAN_POINT ( 'NONE',  ( -7.999999999999976019, -3.611371706259009353E-07, 26.51781575558936055 ) ) ;
#11081=CARTESIAN_POINT ( 'NONE',  ( -5.082755093536317936, -5.082755093536320601, 18.54905278187175455 ) ) ;
#11100=CIRCLE ( 'NONE', #21959, 20.00000000000000355 ) ;
#11104=CARTESIAN_POINT ( 'NONE',  ( -7.999999999999989342, -3.313708498984762496, 3.924052779823362425 ) ) ;
#11108=CARTESIAN_POINT ( 'NONE',  ( -7.999999999999991118, 0.000000000000000000, 11.33030277982336642 ) ) ;
#11132=CARTESIAN_POINT ( 'NONE',  ( 8.008118988124991233, 3.317071493978879015, 18.35686528394063188 ) ) ;
#11149=CARTESIAN_POINT ( 'NONE',  ( -4.898587196589407898E-16, 7.999999999999991118, 5.142802783920146226 ) ) ;
#11164=CARTESIAN_POINT ( 'NONE',  ( -7.188101187499991163, 2.977408999572646930, 19.76780278187175455 ) ) ;
#11188=CARTESIAN_POINT ( 'NONE',  ( 5.656854249492376141, -5.656854249492374365, 22.39280277982336997 ) ) ;
#11193=CARTESIAN_POINT ( 'NONE',  ( -7.999999999999991118, 0.000000000000000000, 8.330302779823362869 ) ) ;
#11205=CARTESIAN_POINT ( 'NONE',  ( -3.313708498984757167, 7.999999999999991118, 11.23655278392014445 ) ) ;
#11209=ADVANCED_FACE ( 'NONE', ( #10492 ), #4844, .T. ) ;
#11252=CARTESIAN_POINT ( 'NONE',  ( 2.977408999572646486, 7.188101187499991163, 11.51780278187175810 ) ) ;
#11276=CARTESIAN_POINT ( 'NONE',  ( -5.082755093536317936, -5.082755093536320601, 12.54905278187175277 ) ) ;
#11280=CARTESIAN_POINT ( 'NONE',  ( 7.999999999999991118, 9.797174393178815797E-16, 0.1365527843298230681 ) ) ;
#11291=CARTESIAN_POINT ( 'NONE',  ( 3.313708498984756279, 7.999999999999991118, 1.861552779823364423 ) ) ;
#11301=ORIENTED_EDGE ( 'NONE', *, *, #5155, .T. ) ;
#11308=CARTESIAN_POINT ( 'NONE',  ( -3.313708498984758943, -7.999999999999989342, 8.667802784329824206 ) ) ;
#11315=CARTESIAN_POINT ( 'NONE',  ( 2.977408999572650927, -7.188101187499990274, 27.45530278187175455 ) ) ;
#11317=EDGE_CURVE ( 'NONE', #30893, #64535, #18769, .T. ) ;
#11330=CARTESIAN_POINT ( 'NONE',  ( -4.898587196589407898E-16, 7.999999999999991118, 9.642802783920146226 ) ) ;
#11335=CARTESIAN_POINT ( 'NONE',  ( -2.977408999572648707, -7.188101187499990274, 0.2678027818717523822 ) ) ;
#11349=CARTESIAN_POINT ( 'NONE',  ( -7.188101187499991163, 2.977408999572646930, 4.767802781871753659 ) ) ;
#11359=CARTESIAN_POINT ( 'NONE',  ( -2.977408999572648707, -7.188101187499990274, 27.64280278187175810 ) ) ;
#11378=CARTESIAN_POINT ( 'NONE',  ( -3.313708498984758943, -7.999999999999989342, 20.61155277982337353 ) ) ;
#11384=CARTESIAN_POINT ( 'NONE',  ( 7.999999999714877852, 6.754118554053788561E-05, 0.2678047518895779744 ) ) ;
#11391=CARTESIAN_POINT ( 'NONE',  ( -3.313708498984757167, 7.999999999999991118, 21.60530278432982954 ) ) ;
#11411=DIRECTION ( 'NONE',  ( 1.000000000000000000, 0.000000000000000000, -0.000000000000000000 ) ) ;
#11413=PRODUCT ( 'clamping lever', 'clamping lever', '', ( #62923 ) ) ;
#11422=DIRECTION ( 'NONE',  ( 0.000000000000000000, 0.000000000000000000, 1.000000000000000000 ) ) ;
#11425=CARTESIAN_POINT ( 'NONE',  ( 5.082755093536318824, 5.082755093536319713, 17.42405278187175810 ) ) ;
#11426=VERTEX_POINT ( 'NONE', #24409 ) ;
#11450=CARTESIAN_POINT ( 'NONE',  ( -7.188101187499992051, 2.977408999572646930, 15.26780278187175455 ) ) ;
#11472=CARTESIAN_POINT ( 'NONE',  ( -5.656854249492373476, -5.656854249492376141, 4.017802779823362869 ) ) ;
#11498=CARTESIAN_POINT ( 'NONE',  ( 7.999999999999991118, 3.313708498984758055, 7.861552783920144449 ) ) ;
#11499=CARTESIAN_POINT ( 'NONE',  ( -8.008118988124989457, -3.317071493978883900, 13.10686528394062833 ) ) ;
#11519=CARTESIAN_POINT ( 'NONE',  ( 5.656854249492376141, -5.656854249492374365, 7.580302783920144449 ) ) ;
#11531=CARTESIAN_POINT ( 'NONE',  ( 7.188101187499992051, 8.802885111219154394E-16, 16.11155278187175455 ) ) ;
#11534=DIRECTION ( 'NONE',  ( 1.000000000000000000, -0.000000000000000000, 0.000000000000000000 ) ) ;
#11548=CARTESIAN_POINT ( 'NONE',  ( -4.264261133003372173, -6.795089700395649857, -0.000000000000000000 ) ) ;
#11554=CARTESIAN_POINT ( 'NONE',  ( -3.313708498984758943, -7.999999999999989342, 22.11155277982336997 ) ) ;
#11572=CARTESIAN_POINT ( 'NONE',  ( 7.999999999999992895, -3.313708498984756279, 10.67405278392014623 ) ) ;
#11587=CARTESIAN_POINT ( 'NONE',  ( 0.000000000000000000, 0.000000000000000000, 29.33030277982336642 ) ) ;
#11621=CARTESIAN_POINT ( 'NONE',  ( 7.188101187499991163, 2.977408999572648707, 6.830302781871755435 ) ) ;
#11646=CARTESIAN_POINT ( 'NONE',  ( -7.188101187499991163, 2.977408999572646930, 10.76780278187175632 ) ) ;
#11649=CARTESIAN_POINT ( 'NONE',  ( -7.999999999999991118, 3.313708498984756723, 2.292802784329821986 ) ) ;
#11659=CARTESIAN_POINT ( 'NONE',  ( 1.469576158976822172E-15, -7.999999999999991118, 1.205302779823363979 ) ) ;
#11673=CARTESIAN_POINT ( 'NONE',  ( 7.999999999999991118, 3.313708498984757611, 4.730302784329824206 ) ) ;
#11680=CARTESIAN_POINT ( 'NONE',  ( -2.977408999572647819, 7.188101187499992051, 28.20530278187175810 ) ) ;
#11692=CARTESIAN_POINT ( 'NONE',  ( 7.999999999999992895, -3.313708498984756279, 21.17405278392015333 ) ) ;
#11701=CARTESIAN_POINT ( 'NONE',  ( -5.082755093536319713, 5.082755093536319713, 23.79905278187175455 ) ) ;
#11715=CARTESIAN_POINT ( 'NONE',  ( 5.082755093536318824, 5.082755093536319713, 2.799052781871750994 ) ) ;
#11722=CARTESIAN_POINT ( 'NONE',  ( 1.471067592899761672E-15, -8.008118988124991233, 2.888115283940627886 ) ) ;
#11729=CARTESIAN_POINT ( 'NONE',  ( -7.188101187499991163, 2.977408999572646930, 27.26780278187175099 ) ) ;
#11748=CARTESIAN_POINT ( 'NONE',  ( -7.999999999999991118, 0.000000000000000000, 21.83030277982336997 ) ) ;
#11762=CARTESIAN_POINT ( 'NONE',  ( -5.656854249492375253, 5.656854249492375253, 24.69905278432982598 ) ) ;
#11794=CARTESIAN_POINT ( 'NONE',  ( -5.082755093536317936, -5.082755093536320601, 18.17405278187175455 ) ) ;
#11818=CARTESIAN_POINT ( 'NONE',  ( 1.320432766682872962E-15, -7.188101187499992051, 18.73655278187175455 ) ) ;
#11839=CARTESIAN_POINT ( 'NONE',  ( 3.313708498984756279, 7.999999999999991118, 1.861552779823364423 ) ) ;
#11853=CARTESIAN_POINT ( 'NONE',  ( 5.622403371994028731, -5.703161834202245650, -0.000000000000000000 ) ) ;
#11867=CARTESIAN_POINT ( 'NONE',  ( 8.008118988124993010, -3.317071493978877239, 16.66936528394062833 ) ) ;
#11873=CARTESIAN_POINT ( 'NONE',  ( 7.188101187499992051, 2.977408999572647819, 12.83030278187175277 ) ) ;
#11888=CARTESIAN_POINT ( 'NONE',  ( -3.313708498984758943, -7.999999999999989342, 5.799052783920146226 ) ) ;
#11903=CARTESIAN_POINT ( 'NONE',  ( -5.082755093536317936, -5.082755093536320601, 20.04905278187175455 ) ) ;
#11909=DIRECTION ( 'NONE',  ( -0.000000000000000000, -0.000000000000000000, 1.000000000000000000 ) ) ;
#11927=CARTESIAN_POINT ( 'NONE',  ( -5.656854249492375253, 5.656854249492375253, 21.64280277982336997 ) ) ;
#11946=CARTESIAN_POINT ( 'NONE',  ( 5.656854249492376141, -5.656854249492374365, 4.580302783920145338 ) ) ;
#11991=EDGE_LOOP ( 'NONE', ( #565, #29255, #31544, #5118 ) ) ;
#11993=CARTESIAN_POINT ( 'NONE',  ( 7.188101187499992051, 8.802885111219154394E-16, 8.236552781871752771 ) ) ;
#12018=CARTESIAN_POINT ( 'NONE',  ( 2.977408999572650927, -7.188101187499990274, 9.830302781871752771 ) ) ;
#12021=CARTESIAN_POINT ( 'NONE',  ( 5.656854249492376141, -5.656854249492374365, 1.449052784329824428 ) ) ;
#12031=CARTESIAN_POINT ( 'NONE',  ( 1.469576158976822172E-15, -7.999999999999991118, 5.705302779823364645 ) ) ;
#12052=CARTESIAN_POINT ( 'NONE',  ( -5.082755093536317936, -5.082755093536320601, 25.67405278187175810 ) ) ;
#12061=CARTESIAN_POINT ( 'NONE',  ( 5.656854249492376141, -5.656854249492374365, 18.08030278392014623 ) ) ;
#12071=CARTESIAN_POINT ( 'NONE',  ( -7.188101187499990274, -2.977408999572651371, 25.58030278187175810 ) ) ;
#12088=CARTESIAN_POINT ( 'NONE',  ( 3.317071493978877683, 8.008118988124991233, 0.5443652839406293298 ) ) ;
#12092=CARTESIAN_POINT ( 'NONE',  ( 5.656854249492376141, -5.656854249492374365, 7.392802779823366421 ) ) ;
#12095=CARTESIAN_POINT ( 'NONE',  ( -5.082755093536319713, 5.082755093536319713, 25.67405278187175810 ) ) ;
#12102=CARTESIAN_POINT ( 'NONE',  ( -5.656854249492375253, 5.656854249492375253, 29.14280277982336642 ) ) ;
#12113=CARTESIAN_POINT ( 'NONE',  ( -4.898587196589407898E-16, 7.999999999999991118, 19.95530277982336642 ) ) ;
#12126=CARTESIAN_POINT ( 'NONE',  ( -7.999999999999991118, 0.000000000000000000, 26.38655278432982243 ) ) ;
#12132=EDGE_CURVE ( 'NONE', #6596, #4443, #51505, .T. ) ;
#12155=CARTESIAN_POINT ( 'NONE',  ( 0.000000000000000000, 0.000000000000000000, 30.00000000000000000 ) ) ;
#12161=CARTESIAN_POINT ( 'NONE',  ( 7.188101187499992051, 8.802885111219154394E-16, 15.73655278187175632 ) ) ;
#12182=CARTESIAN_POINT ( 'NONE',  ( 2.977408999572650927, -7.188101187499990274, 11.33030278187175455 ) ) ;
#12186=CARTESIAN_POINT ( 'NONE',  ( 7.999999999999991118, 9.797174393178815797E-16, 21.08030277982336642 ) ) ;
#12214=VECTOR ( 'NONE', #48757, 1000.000000000000000 ) ;
#12230=CARTESIAN_POINT ( 'NONE',  ( -8.008118988124991233, 3.317071493978878127, 11.41936528394062833 ) ) ;
#12237=CARTESIAN_POINT ( 'NONE',  ( 2.977408999572646486, 7.188101187499992051, 8.517802781871756324 ) ) ;
#12242=DIRECTION ( 'NONE',  ( -0.000000000000000000, -0.000000000000000000, 1.000000000000000000 ) ) ;
#12252=CARTESIAN_POINT ( 'NONE',  ( -7.999999999999991118, 3.313708498984756723, 0.9240527839201456706 ) ) ;
#12268=CARTESIAN_POINT ( 'NONE',  ( -2.977408999572648707, -7.188101187499990274, 17.14280278187175455 ) ) ;
#12277=CARTESIAN_POINT ( 'NONE',  ( -2.977408999572647819, -7.188101187499990274, 26.14280278187176165 ) ) ;
#12287=EDGE_CURVE ( 'NONE', #63012, #29054, #18332, .T. ) ;
#12294=DIRECTION ( 'NONE',  ( 1.000000000000000000, 0.000000000000000000, 0.000000000000000000 ) ) ;
#12295=CARTESIAN_POINT ( 'NONE',  ( 7.999999999999992895, -3.313708498984756279, 23.98655277982336642 ) ) ;
#12298=ORIENTED_EDGE ( 'NONE', *, *, #30125, .F. ) ;
#12315=CARTESIAN_POINT ( 'NONE',  ( 7.999999999999991118, 9.797174393178815797E-16, 6.267802783920147114 ) ) ;
#12332=CARTESIAN_POINT ( 'NONE',  ( -4.898587196589407898E-16, 7.999999999999991118, 11.14280278392014800 ) ) ;
#12360=CARTESIAN_POINT ( 'NONE',  ( -7.188101187499990274, -2.977408999572651371, 9.080302781871752771 ) ) ;
#12383=CARTESIAN_POINT ( 'NONE',  ( -5.082755093536319713, 5.082755093536319713, 9.174052781871752771 ) ) ;
#12388=CARTESIAN_POINT ( 'NONE',  ( 5.656854249492376141, -5.656854249492374365, -0.05094721567017711228 ) ) ;
#12398=CARTESIAN_POINT ( 'NONE',  ( -7.999999999999989342, -3.313708498984762496, 22.11155278392014623 ) ) ;
#12417=CARTESIAN_POINT ( 'NONE',  ( -7.999999999961178609, -1.665943300379353739E-05, 2.518425711869641592 ) ) ;
#12425=CARTESIAN_POINT ( 'NONE',  ( -7.999999999999991118, 0.000000000000000000, 20.51780278392014623 ) ) ;
#12437=CARTESIAN_POINT ( 'NONE',  ( 5.082755093536320601, -5.082755093536318824, 26.04905278187175810 ) ) ;
#12457=CARTESIAN_POINT ( 'NONE',  ( 3.317071493978883456, -8.008118988124989457, 4.481865283940629219 ) ) ;
#12463=CARTESIAN_POINT ( 'NONE',  ( 7.188101187499991163, 2.977408999572648707, 26.70530278187175455 ) ) ;
#12469=DIRECTION ( 'NONE',  ( -1.000000000000000000, -1.224646799147353207E-16, 0.000000000000000000 ) ) ;
#12480=CARTESIAN_POINT ( 'NONE',  ( -5.656854249492373476, -5.656854249492376141, 13.01780277982336465 ) ) ;
#12496=CARTESIAN_POINT ( 'NONE',  ( 1.469576158976822172E-15, -7.999999999999991118, 26.76155278432982598 ) ) ;
#12528=CARTESIAN_POINT ( 'NONE',  ( 1.320432766682872962E-15, -7.188101187499992051, 10.86155278187175455 ) ) ;
#12553=CARTESIAN_POINT ( 'NONE',  ( -7.188101187499992051, 2.977408999572646930, 12.26780278187175455 ) ) ;
#12582=CARTESIAN_POINT ( 'NONE',  ( 5.656854249492374365, 5.656854249492375253, 9.267802779823364645 ) ) ;
#12584=DIRECTION ( 'NONE',  ( -0.000000000000000000, -0.000000000000000000, 1.000000000000000000 ) ) ;
#12600=CARTESIAN_POINT ( 'NONE',  ( -5.662595241051935346, 5.662595241051935346, 17.32561528394063188 ) ) ;
#12605=CARTESIAN_POINT ( 'NONE',  ( 7.188101187499992051, 2.977408999572647819, 9.830302781871754547 ) ) ;
#12617=CARTESIAN_POINT ( 'NONE',  ( -6.062598230945730471, -5.219664997883827873, -0.3118207965721654928 ) ) ;
#12631=CARTESIAN_POINT ( 'NONE',  ( 2.977408999572646486, 7.188101187499991163, 16.39280278187175455 ) ) ;
#12636=CARTESIAN_POINT ( 'NONE',  ( -5.656854249492373476, -5.656854249492376141, 19.20530278392014978 ) ) ;
#12644=CARTESIAN_POINT ( 'NONE',  ( -7.999999999999991118, 0.000000000000000000, 26.33030277982336997 ) ) ;
#12656=CARTESIAN_POINT ( 'NONE',  ( 7.999999999999992895, -3.313708498984756279, 16.48655277982336642 ) ) ;
#12672=CARTESIAN_POINT ( 'NONE',  ( 3.313708498984756279, 7.999999999999991118, 9.549052783920146226 ) ) ;
#12674=CARTESIAN_POINT ( 'NONE',  ( 5.656854249492374365, 5.656854249492375253, 6.455302783920143561 ) ) ;
#12693=VERTEX_POINT ( 'NONE', #50680 ) ;
#12706=( BOUNDED_CURVE ( )  B_SPLINE_CURVE ( 2, ( #12644, #42420, #58690, #70008, #18317, #41330, #64340, #8850, #49198 ),
 .UNSPECIFIED., .F., .F. ) 
 B_SPLINE_CURVE_WITH_KNOTS ( ( 3, 2, 2, 2, 3 ),
 ( 0.1052631578947368085, 0.1118421052631578816, 0.1184210526315789269, 0.1250000000000000000, 0.1315789473684210453 ),
 .UNSPECIFIED. ) 
 CURVE ( )  GEOMETRIC_REPRESENTATION_ITEM ( )  RATIONAL_B_SPLINE_CURVE ( ( 1.000000000000000222, 0.9238795325112864054, 1.000000000000000000, 0.9238795325112867385, 1.000000000000000000, 0.9238795325112867385, 1.000000000000000000, 0.9238795325112867385, 1.000000000000000000 ) ) 
 REPRESENTATION_ITEM ( '' )  );
#12720=CARTESIAN_POINT ( 'NONE',  ( 5.082755093536318824, 5.082755093536319713, 6.924052781871750994 ) ) ;
#12748=CARTESIAN_POINT ( 'NONE',  ( 7.188101187499991163, 2.977408999572648707, 5.705302781871753659 ) ) ;
#12750=CARTESIAN_POINT ( 'NONE',  ( 0.000000000000000000, -16.70329308849007077, 0.000000000000000000 ) ) ;
#12761=CARTESIAN_POINT ( 'NONE',  ( 1.469576158976822172E-15, -7.999999999999991118, 22.39280278392014623 ) ) ;
#12780=CARTESIAN_POINT ( 'NONE',  ( -2.977408999572647819, 7.188101187499992051, 25.20530278187175810 ) ) ;
#12792=CARTESIAN_POINT ( 'NONE',  ( -5.656854249492375253, 5.656854249492375253, 20.33030278392014623 ) ) ;
#12795=FACE_OUTER_BOUND ( 'NONE', #45192, .T. ) ;
#12803=CARTESIAN_POINT ( 'NONE',  ( -2.977408999572647819, 7.188101187499991163, 23.70530278187175810 ) ) ;
#12818=CARTESIAN_POINT ( 'NONE',  ( -3.317071493978880348, -8.008118988124989457, 4.294365283940629219 ) ) ;
#12832=ORIENTED_EDGE ( 'NONE', *, *, #57616, .F. ) ;
#12841=CARTESIAN_POINT ( 'NONE',  ( 1.469576158976822172E-15, -7.999999999999991118, 13.20530277982336465 ) ) ;
#12855=CARTESIAN_POINT ( 'NONE',  ( -3.313708498984758943, -7.999999999999989342, 17.66780278432982598 ) ) ;
#12872=CARTESIAN_POINT ( 'NONE',  ( -7.999999999999991118, 9.797174393178815797E-16, 30.00000000000000000 ) ) ;
#12890=CARTESIAN_POINT ( 'NONE',  ( -2.977408999572648707, -7.188101187499990274, 13.76780278187175455 ) ) ;
#12913=CARTESIAN_POINT ( 'NONE',  ( 5.082755093536320601, -5.082755093536318824, 9.924052781871754547 ) ) ;
#12937=ORIENTED_EDGE ( 'NONE', *, *, #2739, .T. ) ;
#12957=CARTESIAN_POINT ( 'NONE',  ( 3.317071493978883456, -8.008118988124989457, 13.48186528394063011 ) ) ;
#12964=CARTESIAN_POINT ( 'NONE',  ( -5.082755093536317936, -5.082755093536320601, 9.174052781871752771 ) ) ;
#12978=CARTESIAN_POINT ( 'NONE',  ( -4.401442555609577197E-16, 7.188101187499992051, 28.11155278187175455 ) ) ;
#12979=ORIENTED_EDGE ( 'NONE', *, *, #20996, .T. ) ;
#12993=CARTESIAN_POINT ( 'NONE',  ( 5.082755093536320601, -5.082755093536318824, 12.92405278187175277 ) ) ;
#13009=VECTOR ( 'NONE', #30650, 1000.000000000000000 ) ;
#13019=CARTESIAN_POINT ( 'NONE',  ( 5.656854249492374365, 5.656854249492375253, 16.76780277982336287 ) ) ;
#13021=CARTESIAN_POINT ( 'NONE',  ( 7.999999999521839378, -8.746674989952265200E-05, 18.26780030933659305 ) ) ;
#13023=( BOUNDED_CURVE ( )  B_SPLINE_CURVE ( 2, ( #20166, #44319, #20544, #33022, #56024, #4333, #54525, #49602, #55652 ),
 .UNSPECIFIED., .F., .F. ) 
 B_SPLINE_CURVE_WITH_KNOTS ( ( 3, 2, 2, 2, 3 ),
 ( 0.9473684210526316374, 0.9539473684210527660, 0.9605263157894736725, 0.9671052631578946901, 0.9736842105263158187 ),
 .UNSPECIFIED. ) 
 CURVE ( )  GEOMETRIC_REPRESENTATION_ITEM ( )  RATIONAL_B_SPLINE_CURVE ( ( 0.9999999999999986677, 0.9238795325112880708, 1.000000000000000000, 0.9238795325112867385, 1.000000000000000000, 0.9238795325112867385, 1.000000000000000000, 0.9238795325112867385, 1.000000000000000000 ) ) 
 REPRESENTATION_ITEM ( '' )  );
#13047=EDGE_LOOP ( 'NONE', ( #69119, #36007, #68372, #55199 ) ) ;
#13085=CARTESIAN_POINT ( 'NONE',  ( -7.188101187499992051, 0.000000000000000000, 8.986552781871752771 ) ) ;
#13094=DIRECTION ( 'NONE',  ( -0.000000000000000000, -0.000000000000000000, 1.000000000000000000 ) ) ;
#13095=ORIENTED_EDGE ( 'NONE', *, *, #53528, .F. ) ;
#13109=CARTESIAN_POINT ( 'NONE',  ( 7.188101187499991163, 2.977408999572648707, 2.705302781871750994 ) ) ;
#13123=CARTESIAN_POINT ( 'NONE',  ( 5.656854249492376141, -5.656854249492374365, 24.08030278392014978 ) ) ;
#13145=CARTESIAN_POINT ( 'NONE',  ( 7.188101187499992051, 2.977408999572647819, 21.83030278187175810 ) ) ;
#13155=CARTESIAN_POINT ( 'NONE',  ( -3.313708498984758943, -7.999999999999989342, 13.29905278392014800 ) ) ;
#13162=CARTESIAN_POINT ( 'NONE',  ( -7.999999999961182162, -1.665870058181487338E-05, 5.518425684709454160 ) ) ;
#13166=CARTESIAN_POINT ( 'NONE',  ( 5.082755093536320601, -5.082755093536318824, 23.04905278187175455 ) ) ;
#13180=CARTESIAN_POINT ( 'NONE',  ( 3.313708498984756279, 7.999999999999991118, 0.5490527839201453375 ) ) ;
#13183=CARTESIAN_POINT ( 'NONE',  ( 5.662595241051934458, 5.662595241051935346, 3.450615283940628775 ) ) ;
#13189=CARTESIAN_POINT ( 'NONE',  ( 5.082755093536318824, 5.082755093536319713, 23.79905278187175455 ) ) ;
#13207=CARTESIAN_POINT ( 'NONE',  ( -3.313708498984757167, 7.999999999999991118, 14.04905277982336465 ) ) ;
#13224=CARTESIAN_POINT ( 'NONE',  ( 5.656854249492376141, -5.656854249492374365, 17.94905278432982243 ) ) ;
#13239=ORIENTED_EDGE ( 'NONE', *, *, #41291, .F. ) ;
#13244=B_SPLINE_CURVE_WITH_KNOTS ( 'NONE', 3,
 ( #22476, #46617, #69264, #46244, #11548, #34206, #30016, #35681, #70014, #45874, #18322, #57209, #46982, #68887, #58334, #23236, #23606, #17199, #58696, #16815 ),
 .UNSPECIFIED., .F., .F.,
 ( 4, 2, 1, 2, 2, 1, 2, 2, 1, 1, 2, 4 ),
 ( 0.6132134907475605967, 0.6391986578402925057, 0.6651838249330244146, 0.6781764084793903136, 0.6911689920257563235, 0.7171541591184882325, 0.7431393262112202525, 0.7561319097575862624, 0.7691244933039521614, 0.7951096603966840703, 0.8081022439430500803, 0.8210948274894160903 ),
 .UNSPECIFIED. ) ;
#13257=CARTESIAN_POINT ( 'NONE',  ( 7.188101187499991163, 2.977408999572648707, 14.33030278187175277 ) ) ;
#13258=EDGE_LOOP ( 'NONE', ( #43486, #36018, #72952, #20851 ) ) ;
#13277=CARTESIAN_POINT ( 'NONE',  ( -5.082755093536319713, 5.082755093536319713, 12.17405278187175277 ) ) ;
#13283=DIRECTION ( 'NONE',  ( -0.000000000000000000, -0.000000000000000000, 1.000000000000000000 ) ) ;
#13294=EDGE_CURVE ( 'NONE', #29130, #63012, #9508, .T. ) ;
#13301=CARTESIAN_POINT ( 'NONE',  ( 5.656854249492376141, -5.656854249492374365, 23.89280277982336642 ) ) ;
#13304=EDGE_CURVE ( 'NONE', #41375, #33835, #27004, .T. ) ;
#13323=CARTESIAN_POINT ( 'NONE',  ( 5.662595241051936235, -5.662595241051934458, 7.575615283940628331 ) ) ;
#13330=CARTESIAN_POINT ( 'NONE',  ( 2.977408999572646486, 7.188101187499992051, 11.51780278187175632 ) ) ;
#13342=CARTESIAN_POINT ( 'NONE',  ( 3.313708498984762496, -7.999999999999989342, 1.486552783920146448 ) ) ;
#13364=CARTESIAN_POINT ( 'NONE',  ( -8.000000000000033751, -3.313708498984719864, 5.424052779823364645 ) ) ;
#13366=CARTESIAN_POINT ( 'NONE',  ( -7.999999999999991118, 0.000000000000000000, 3.830302779823362869 ) ) ;
#13378=CARTESIAN_POINT ( 'NONE',  ( 3.313708498984762496, -7.999999999999989342, 25.29905277982336287 ) ) ;
#13386=CARTESIAN_POINT ( 'NONE',  ( -3.313708498984757167, 7.999999999999991118, 17.04905277982336642 ) ) ;
#13395=EDGE_LOOP ( 'NONE', ( #66669, #29494, #40711, #51000, #47428 ) ) ;
#13405=CARTESIAN_POINT ( 'NONE',  ( -3.313708498984757611, 7.999999999999991118, 6.736552783920143561 ) ) ;
#13417=CARTESIAN_POINT ( 'NONE',  ( 5.662595241051934458, 5.662595241051935346, 27.45061528394063188 ) ) ;
#13437=LINE ( 'NONE', #7803, #48913 ) ;
#13447=CARTESIAN_POINT ( 'NONE',  ( -1.450627696953363260E-15, 11.84527406565996621, 27.11488387514485154 ) ) ;
#13448=ORIENTED_EDGE ( 'NONE', *, *, #31951, .T. ) ;
#13450=CARTESIAN_POINT ( 'NONE',  ( -7.188101187499990274, -2.977408999572651371, 1.580302781871753437 ) ) ;
#13467=ADVANCED_FACE ( 'NONE', ( #62289 ), #10618, .F. ) ;
#13476=CARTESIAN_POINT ( 'NONE',  ( 7.188101187499991163, 2.977408999572648707, 4.205302781871751883 ) ) ;
#13484=ORIENTED_EDGE ( 'NONE', *, *, #16881, .F. ) ;
#13492=CARTESIAN_POINT ( 'NONE',  ( -5.656854249492373476, -5.656854249492376141, 23.70530278392014978 ) ) ;
#13510=CARTESIAN_POINT ( 'NONE',  ( -7.188101187499992051, 2.977408999572646930, 22.39280278187175810 ) ) ;
#13519=CARTESIAN_POINT ( 'NONE',  ( 7.999999999999991118, 9.797174393178815797E-16, 13.76780278392014623 ) ) ;
#13530=CARTESIAN_POINT ( 'NONE',  ( -2.977408999572648707, -7.188101187499990274, 18.26780278187175455 ) ) ;
#13549=CARTESIAN_POINT ( 'NONE',  ( -5.656854249492373476, -5.656854249492376141, 26.70530278392014623 ) ) ;
#13556=CARTESIAN_POINT ( 'NONE',  ( 2.977408999572646486, 7.188101187499991163, 20.89280278187176521 ) ) ;
#13562=CARTESIAN_POINT ( 'NONE',  ( 1.530808498934191719E-15, 11.84527406565996976, 27.11488387514484444 ) ) ;
#13574=CARTESIAN_POINT ( 'NONE',  ( 7.999999999999992895, -3.313708498984756279, 13.48655277982336465 ) ) ;
#13592=CARTESIAN_POINT ( 'NONE',  ( -7.999999999999991118, 3.313708498984756723, 15.79280278432982421 ) ) ;
#13623=CARTESIAN_POINT ( 'NONE',  ( -7.188101187499992051, 0.000000000000000000, 13.48655278187175455 ) ) ;
#13646=CARTESIAN_POINT ( 'NONE',  ( -7.188101187499990274, -2.977408999572651815, 9.455302781871752771 ) ) ;
#13688=CARTESIAN_POINT ( 'NONE',  ( 8.008118988124991233, 9.807117285998411148E-16, 7.763115283940629219 ) ) ;
#13694=CARTESIAN_POINT ( 'NONE',  ( -7.188101187499992051, 2.977408999572646930, 2.892802781871751439 ) ) ;
#13706=CARTESIAN_POINT ( 'NONE',  ( -7.188101187499992051, 0.000000000000000000, 28.48655278187175810 ) ) ;
#13708=EDGE_CURVE ( 'NONE', #51761, #34174, #31367, .T. ) ;
#13729=CARTESIAN_POINT ( 'NONE',  ( 5.082755093536318824, 5.082755093536319713, 26.79905278187175455 ) ) ;
#13749=CARTESIAN_POINT ( 'NONE',  ( -5.656854249492375253, 5.656854249492375253, 17.14280277982336287 ) ) ;
#13756=VERTEX_POINT ( 'NONE', #39107 ) ;
#13757=CARTESIAN_POINT ( 'NONE',  ( -7.999999999999991118, 3.313708498984757167, 5.424052783920146226 ) ) ;
#13765=CARTESIAN_POINT ( 'NONE',  ( 7.999999999999991118, 9.797174393178815797E-16, 6.267802783920147114 ) ) ;
#13777=CARTESIAN_POINT ( 'NONE',  ( 3.317071493978883456, -8.008118988124989457, 26.98186528394063188 ) ) ;
#13799=VECTOR ( 'NONE', #58032, 1000.000000000000000 ) ;
#13811=ORIENTED_EDGE ( 'NONE', *, *, #67745, .F. ) ;
#13813=CARTESIAN_POINT ( 'NONE',  ( 7.188101187499992051, 8.802885111219154394E-16, 28.11155278187175455 ) ) ;
#13836=CARTESIAN_POINT ( 'NONE',  ( -7.188101187499992051, 0.000000000000000000, 3.361552781871751883 ) ) ;
#13842=FACE_OUTER_BOUND ( 'NONE', #9329, .T. ) ;
#13853=CARTESIAN_POINT ( 'NONE',  ( -7.999999999999991118, 3.313708498984756723, 17.42405278392014623 ) ) ;
#13871=CARTESIAN_POINT ( 'NONE',  ( 1.469576158976822172E-15, -7.999999999999991118, 11.89280278392014445 ) ) ;
#13874=CARTESIAN_POINT ( 'NONE',  ( 7.188101187499992051, 8.802885111219154394E-16, 18.73655278187175455 ) ) ;
#13876=CARTESIAN_POINT ( 'NONE',  ( -7.999999999998400391, 3.416934844025491914E-06, 16.01767659775488184 ) ) ;
#13887=CARTESIAN_POINT ( 'NONE',  ( 3.313708498984756279, 7.999999999999991118, 14.04905278392014978 ) ) ;
#13888=CARTESIAN_POINT ( 'NONE',  ( 7.999999999999991118, -4.373337617987190320E-05, 18.26780154663448386 ) ) ;
#13899=CARTESIAN_POINT ( 'NONE',  ( 5.082755093536320601, -5.082755093536318824, 21.54905278187175455 ) ) ;
#13911=CARTESIAN_POINT ( 'NONE',  ( -4.898587196589407898E-16, 7.999999999999991118, 15.45530277982336642 ) ) ;
#13915=CARTESIAN_POINT ( 'NONE',  ( 7.999999999999991118, 3.313708498984757611, 27.36155278392014978 ) ) ;
#13919=CARTESIAN_POINT ( 'NONE',  ( 7.999999999999992895, -7.224685084787812073E-14, 27.26780278391845513 ) ) ;
#13922=CARTESIAN_POINT ( 'NONE',  ( -7.188101187499990274, -2.977408999572651371, 24.45530278187175455 ) ) ;
#13938=CARTESIAN_POINT ( 'NONE',  ( -5.656854249492375253, 5.656854249492375253, 12.64280277982336287 ) ) ;
#13952=CARTESIAN_POINT ( 'NONE',  ( 3.313708498984756279, 7.999999999999991118, 18.41780278432982598 ) ) ;
#13968=EDGE_CURVE ( 'NONE', #34597, #6793, #47188, .T. ) ;
#13983=EDGE_CURVE ( 'NONE', #19989, #74609, #19471, .T. ) ;
#13986=CARTESIAN_POINT ( 'NONE',  ( 7.188101187499992051, 8.802885111219154394E-16, 9.736552781871754547 ) ) ;
#14013=CARTESIAN_POINT ( 'NONE',  ( -5.082755093536317936, -5.082755093536320601, 6.549052781871754547 ) ) ;
#14043=CARTESIAN_POINT ( 'NONE',  ( 1.469576158976822172E-15, -7.999999999999991118, 8.892802783920146226 ) ) ;
#14061=CARTESIAN_POINT ( 'NONE',  ( 3.317071493978877683, 8.008118988124991233, 9.544365283940628331 ) ) ;
#14068=CARTESIAN_POINT ( 'NONE',  ( 1.320432766682872962E-15, -7.188101187499992051, 0.3615527818717524378 ) ) ;
#14081=CARTESIAN_POINT ( 'NONE',  ( -7.188101187499991163, 2.977408999572646930, 22.39280278187175810 ) ) ;
#14085=ORIENTED_EDGE ( 'NONE', *, *, #10935, .T. ) ;
#14099=CARTESIAN_POINT ( 'NONE',  ( 7.999999999999991118, 3.313708498984758055, 24.36155278392014978 ) ) ;
#14107=CARTESIAN_POINT ( 'NONE',  ( 7.188101187499992051, 8.802885111219154394E-16, 22.11155278187175455 ) ) ;
#14126=CARTESIAN_POINT ( 'NONE',  ( 5.656854249492374365, 5.656854249492375253, 13.76780277982336465 ) ) ;
#14131=CARTESIAN_POINT ( 'NONE',  ( 7.999999999932789763, 3.279097096261179525E-05, 13.76780373625499010 ) ) ;
#14158=CARTESIAN_POINT ( 'NONE',  ( 3.317071493978877683, 8.008118988124991233, 26.04436528394063188 ) ) ;
#14187=EDGE_LOOP ( 'NONE', ( #28377, #69634, #41304, #37667 ) ) ;
#14190=CARTESIAN_POINT ( 'NONE',  ( 1.320432766682872962E-15, -7.188101187499992051, 1.861552781871753881 ) ) ;
#14203=EDGE_LOOP ( 'NONE', ( #74379, #60112, #4285, #40440 ) ) ;
#14215=CARTESIAN_POINT ( 'NONE',  ( -2.977408999572647819, 7.188101187499991163, 6.080302781871753659 ) ) ;
#14230=CARTESIAN_POINT ( 'NONE',  ( 3.313708498984762496, -7.999999999999989342, 19.48655278392014978 ) ) ;
#14231=VECTOR ( 'NONE', #6624, 1000.000000000000000 ) ;
#14233=FACE_OUTER_BOUND ( 'NONE', #50818, .T. ) ;
#14257=CARTESIAN_POINT ( 'NONE',  ( 5.082755093536318824, 5.082755093536319713, 23.42405278187175455 ) ) ;
#14264=CARTESIAN_POINT ( 'NONE',  ( -7.999999999999989342, -3.313708498984762496, 14.61155278392014800 ) ) ;
#14266=CARTESIAN_POINT ( 'NONE',  ( 7.999999999999991118, 3.313708498984758055, 18.36155278392014623 ) ) ;
#14275=CARTESIAN_POINT ( 'NONE',  ( 7.188101187499991163, 2.977408999572648707, 18.83030278187175099 ) ) ;
#14294=CARTESIAN_POINT ( 'NONE',  ( -5.656854249492375253, 5.656854249492375253, 26.33030278392014623 ) ) ;
#14301=CARTESIAN_POINT ( 'NONE',  ( 7.188101187499993827, -2.977408999572645598, 25.01780278187175455 ) ) ;
#14317=CARTESIAN_POINT ( 'NONE',  ( -5.656854249492375253, 5.656854249492375253, 6.642802779823365533 ) ) ;
#14336=CARTESIAN_POINT ( 'NONE',  ( 7.999999999999991118, 3.313708498984757611, 19.73030278432982598 ) ) ;
#14337=CARTESIAN_POINT ( 'NONE',  ( 7.999999999999950262, -3.313708498984798467, 16.48655277982336287 ) ) ;
#14367=CARTESIAN_POINT ( 'NONE',  ( -7.188101187499992051, 0.000000000000000000, 8.986552781871752771 ) ) ;
#14380=CARTESIAN_POINT ( 'NONE',  ( 1.320432766682872962E-15, -7.188101187499992051, 11.23655278187175455 ) ) ;
#14393=CARTESIAN_POINT ( 'NONE',  ( 2.977408999572646486, 7.188101187499992051, 2.892802781871751439 ) ) ;
#14407=LINE ( 'NONE', #66855, #16543 ) ;
#14410=CARTESIAN_POINT ( 'NONE',  ( -5.656854249492375253, 5.656854249492375253, 26.14280277982336997 ) ) ;
#14421=CARTESIAN_POINT ( 'NONE',  ( -3.313708498984758943, -7.999999999999989342, 5.799052783920146226 ) ) ;
#14437=CARTESIAN_POINT ( 'NONE',  ( -4.903558642999205574E-16, 8.008118988124991233, 9.638115283940630107 ) ) ;
#14443=CARTESIAN_POINT ( 'NONE',  ( -7.188101187499992051, 0.000000000000000000, 5.986552781871753659 ) ) ;
#14456=CARTESIAN_POINT ( 'NONE',  ( -2.977408999572647819, 7.188101187499991163, 26.70530278187175455 ) ) ;
#14480=CARTESIAN_POINT ( 'NONE',  ( -7.188101187499992051, 0.000000000000000000, 22.86155278187175455 ) ) ;
#14498=CARTESIAN_POINT ( 'NONE',  ( -4.898587196589407898E-16, 7.999999999999991118, 7.955302779823362869 ) ) ;
#14508=CARTESIAN_POINT ( 'NONE',  ( -5.656854249492375253, 5.656854249492375253, 5.330302783920146226 ) ) ;
#14529=CARTESIAN_POINT ( 'NONE',  ( 5.662595241051934458, 5.662595241051935346, 25.95061528394063188 ) ) ;
#14547=CARTESIAN_POINT ( 'NONE',  ( 0.000000000000000000, 15.08051212944140218, 15.04081104653146994 ) ) ;
#14549=( BOUNDED_CURVE ( )  B_SPLINE_CURVE ( 2, ( #23595, #28885, #46604, #48447, #29634, #65055, #18312, #8095, #13366 ),
 .UNSPECIFIED., .F., .F. ) 
 B_SPLINE_CURVE_WITH_KNOTS ( ( 3, 2, 2, 2, 3 ),
 ( 0.8684210526315789824, 0.8750000000000000000, 0.8815789473684210176, 0.8881578947368422572, 0.8947368421052632748 ),
 .UNSPECIFIED. ) 
 CURVE ( )  GEOMETRIC_REPRESENTATION_ITEM ( )  RATIONAL_B_SPLINE_CURVE ( ( 1.000000000000000000, 0.9238795325112867385, 1.000000000000000000, 0.9238795325112867385, 1.000000000000000000, 0.9238795325112867385, 1.000000000000000000, 0.9238795325112854062, 1.000000000000001332 ) ) 
 REPRESENTATION_ITEM ( '' )  );
#14565=CARTESIAN_POINT ( 'NONE',  ( -5.082755093536319713, 5.082755093536319713, 1.299052781871753215 ) ) ;
#14591=CARTESIAN_POINT ( 'NONE',  ( 5.656854249492376141, -5.656854249492374365, 28.39280277982336642 ) ) ;
#14598=CARTESIAN_POINT ( 'NONE',  ( 7.999999999999991118, 9.797174393178815797E-16, 15.08030277982336642 ) ) ;
#14610=CARTESIAN_POINT ( 'NONE',  ( 5.656854249492376141, -5.656854249492374365, 18.08030278392014623 ) ) ;
#14614=CARTESIAN_POINT ( 'NONE',  ( -7.999999999999991118, 0.000000000000000000, 14.33030277982336465 ) ) ;
#14630=CARTESIAN_POINT ( 'NONE',  ( 2.977408999572650927, -7.188101187499990274, 19.95530278187175455 ) ) ;
#14638=CARTESIAN_POINT ( 'NONE',  ( 7.999999999999991118, 3.313708498984757611, 15.36155278392014623 ) ) ;
#14642=ORIENTED_EDGE ( 'NONE', *, *, #59880, .T. ) ;
#14650=CARTESIAN_POINT ( 'NONE',  ( 5.082755093536318824, 5.082755093536319713, 20.42405278187175455 ) ) ;
#14666=CARTESIAN_POINT ( 'NONE',  ( -4.898587196589407898E-16, 7.999999999999991118, 0.6428027839201454485 ) ) ;
#14670=CARTESIAN_POINT ( 'NONE',  ( 8.008118988124993010, -3.317071493978877239, 0.1693652839406289412 ) ) ;
#14677=CARTESIAN_POINT ( 'NONE',  ( 2.977408999572646486, 7.188101187499991163, 17.89280278187175455 ) ) ;
#14692=CARTESIAN_POINT ( 'NONE',  ( -5.656854249492373476, -5.656854249492376141, 8.517802779823362869 ) ) ;
#14711=CARTESIAN_POINT ( 'NONE',  ( 5.656854249492374365, 5.656854249492375253, 13.82405278432982421 ) ) ;
#14716=VECTOR ( 'NONE', #49802, 1000.000000000000000 ) ;
#14742=CARTESIAN_POINT ( 'NONE',  ( 7.188101187499993827, -2.977408999572645598, 8.142802781871750994 ) ) ;
#14755=CARTESIAN_POINT ( 'NONE',  ( -2.977408999572647819, 7.188101187499991163, 9.080302781871752771 ) ) ;
#14756=VERTEX_POINT ( 'NONE', #36236 ) ;
#14767=CARTESIAN_POINT ( 'NONE',  ( 1.320432766682872962E-15, -7.188101187499992051, 6.736552781871754547 ) ) ;
#14783=CARTESIAN_POINT ( 'NONE',  ( -3.313708498984758943, -7.999999999999989342, 28.11155277982336642 ) ) ;
#14788=DIRECTION ( 'NONE',  ( -0.000000000000000000, -0.000000000000000000, 1.000000000000000000 ) ) ;
#14795=CARTESIAN_POINT ( 'NONE',  ( 5.656854249492376141, -5.656854249492374365, 1.580302783920146226 ) ) ;
#14817=CARTESIAN_POINT ( 'NONE',  ( -7.188101187499990274, -2.977408999572651815, 3.080302781871751439 ) ) ;
#14830=CARTESIAN_POINT ( 'NONE',  ( 1.320432766682872962E-15, -7.188101187499992051, 24.36155278187175810 ) ) ;
#14849=CARTESIAN_POINT ( 'NONE',  ( -7.999999999999989342, -3.313708498984762496, 21.92405277982336642 ) ) ;
#14854=CARTESIAN_POINT ( 'NONE',  ( -7.188101187499990274, -2.977408999572651815, 21.45530278187175810 ) ) ;
#14865=CARTESIAN_POINT ( 'NONE',  ( -6.062687379811042554, -5.219768740853823807, 2.519839246067225784E-12 ) ) ;
#14874=CARTESIAN_POINT ( 'NONE',  ( -3.313708498984758943, -7.999999999999989342, 10.11155277982336820 ) ) ;
#14894=AXIS2_PLACEMENT_3D ( 'NONE', #56796, #12242, #68472 ) ;
#14903=CARTESIAN_POINT ( 'NONE',  ( -5.662595241051933570, -5.662595241051936235, 23.70061528394063188 ) ) ;
#14923=VERTEX_POINT ( 'NONE', #55450 ) ;
#14938=CARTESIAN_POINT ( 'NONE',  ( -5.447323953993864265, -4.689931814214729933, 0.1569290643893266057 ) ) ;
#14965=CARTESIAN_POINT ( 'NONE',  ( 5.656854249492374365, 5.656854249492375253, 28.76780277982336642 ) ) ;
#14966=LINE ( 'NONE', #6462, #66437 ) ;
#14982=CARTESIAN_POINT ( 'NONE',  ( 3.313708498984762496, -7.999999999999989342, 16.48655278392014623 ) ) ;
#15004=CARTESIAN_POINT ( 'NONE',  ( 7.188101187499992051, 8.802885111219154394E-16, 17.23655278187175810 ) ) ;
#15016=CARTESIAN_POINT ( 'NONE',  ( -7.999999999999991118, 3.313708498984756723, 6.924052783920144449 ) ) ;
#15019=DIRECTION ( 'NONE',  ( -0.000000000000000000, -0.000000000000000000, 1.000000000000000000 ) ) ;
#15030=CARTESIAN_POINT ( 'NONE',  ( -4.401442555609577197E-16, 7.188101187499992051, 16.11155278187175455 ) ) ;
#15048=CARTESIAN_POINT ( 'NONE',  ( -7.999999999999991118, 0.000000000000000000, 23.51780278392014978 ) ) ;
#15055=CARTESIAN_POINT ( 'NONE',  ( 2.977408999572646486, 7.188101187499991163, 14.89280278187175455 ) ) ;
#15070=CARTESIAN_POINT ( 'NONE',  ( -7.999999999999989342, -3.313708498984762496, 9.924052779823364645 ) ) ;
#15075=EDGE_LOOP ( 'NONE', ( #3715, #19547, #43187, #28655 ) ) ;
#15086=CARTESIAN_POINT ( 'NONE',  ( -5.656854249492373476, -5.656854249492376141, 11.57405278432982243 ) ) ;
#15090=ORIENTED_EDGE ( 'NONE', *, *, #28200, .F. ) ;
#15120=CARTESIAN_POINT ( 'NONE',  ( -7.188101187499990274, -2.977408999572651371, 4.580302781871752771 ) ) ;
#15132=CARTESIAN_POINT ( 'NONE',  ( 7.188101187499991163, 2.977408999572648707, 11.70530278187175455 ) ) ;
#15146=CARTESIAN_POINT ( 'NONE',  ( 7.188101187499993827, -2.977408999572645598, 7.017802781871754547 ) ) ;
#15163=CARTESIAN_POINT ( 'NONE',  ( 7.999999999999991118, 9.797174393178815797E-16, 27.08030277982336642 ) ) ;
#15176=CARTESIAN_POINT ( 'NONE',  ( -9.121419926064122663, -1.666886344965055722, -0.4481800321554205713 ) ) ;
#15179=CARTESIAN_POINT ( 'NONE',  ( 0.000000000000000000, 0.000000000000000000, 30.00000000000000000 ) ) ;
#15199=CARTESIAN_POINT ( 'NONE',  ( -7.188101187499992051, 0.000000000000000000, 2.986552781871751439 ) ) ;
#15209=CARTESIAN_POINT ( 'NONE',  ( 7.188101187499993827, -2.977408999572645598, 26.14280278187175455 ) ) ;
#15228=CARTESIAN_POINT ( 'NONE',  ( -3.313708498984759387, -7.999999999999989342, 22.11155277982336997 ) ) ;
#15234=CARTESIAN_POINT ( 'NONE',  ( 7.188101187499992051, 2.977408999572647819, 23.70530278187175455 ) ) ;
#15250=CARTESIAN_POINT ( 'NONE',  ( -3.313708498984758943, -7.999999999999989342, 8.611552779823366421 ) ) ;
#15263=CARTESIAN_POINT ( 'NONE',  ( -3.313708498984757611, 7.999999999999991118, 20.23655278392014978 ) ) ;
#15269=ORIENTED_EDGE ( 'NONE', *, *, #20477, .F. ) ;
#15277=CARTESIAN_POINT ( 'NONE',  ( 3.317071493978877683, 8.008118988124991233, 23.04436528394063544 ) ) ;
#15278=CARTESIAN_POINT ( 'NONE',  ( 7.999999999842164478, 5.025161467855852442E-05, 22.76780420562571905 ) ) ;
#15309=CARTESIAN_POINT ( 'NONE',  ( 7.188101187499991163, 2.977408999572648707, 23.70530278187175810 ) ) ;
#15337=CARTESIAN_POINT ( 'NONE',  ( 1.469576158976822172E-15, -7.999999999999991118, 25.20530277982336642 ) ) ;
#15341=ORIENTED_EDGE ( 'NONE', *, *, #18006, .F. ) ;
#15349=EDGE_CURVE ( 'NONE', #54725, #3504, #61731, .T. ) ;
#15353=DIRECTION ( 'NONE',  ( -0.000000000000000000, -0.000000000000000000, 1.000000000000000000 ) ) ;
#15356=CARTESIAN_POINT ( 'NONE',  ( 1.469576158976822172E-15, -7.999999999999991118, 20.89280278392014623 ) ) ;
#15367=CARTESIAN_POINT ( 'NONE',  ( -8.000000000000005329, -3.313708498984745621, 27.92405277982336287 ) ) ;
#15378=CARTESIAN_POINT ( 'NONE',  ( -2.977408999572647819, 7.188101187499992051, 13.20530278187175277 ) ) ;
#15389=CARTESIAN_POINT ( 'NONE',  ( 7.999999999999992895, -3.313708498984756279, 7.674052783920145338 ) ) ;
#15399=CARTESIAN_POINT ( 'NONE',  ( -7.188101187499990274, -2.977408999572651371, 10.58030278187175455 ) ) ;
#15423=CARTESIAN_POINT ( 'NONE',  ( 1.320432766682872962E-15, -7.188101187499992051, 14.23655278187175455 ) ) ;
#15426=ADVANCED_FACE ( 'NONE', ( #13842 ), #65916, .T. ) ;
#15430=ORIENTED_EDGE ( 'NONE', *, *, #51754, .F. ) ;
#15438=CARTESIAN_POINT ( 'NONE',  ( 0.000000000000000000, 0.000000000000000000, 30.00000000000000000 ) ) ;
#15441=CARTESIAN_POINT ( 'NONE',  ( -3.313708498984758943, -7.999999999999989342, 8.611552779823366421 ) ) ;
#15458=CARTESIAN_POINT ( 'NONE',  ( 3.313708498984762496, -7.999999999999989342, 11.85530278432982243 ) ) ;
#15488=CARTESIAN_POINT ( 'NONE',  ( -7.999999999999927169, 3.313708498984821116, 17.23655277982336642 ) ) ;
#15504=CARTESIAN_POINT ( 'NONE',  ( -4.401442555609577197E-16, 7.188101187499992051, 8.986552781871752771 ) ) ;
#15514=CARTESIAN_POINT ( 'NONE',  ( -5.447319899895621376, -4.689936522885654213, 0.2819290645437558807 ) ) ;
#15517=CARTESIAN_POINT ( 'NONE',  ( -2.977408999572647819, -7.188101187499990274, 2.142802781871754103 ) ) ;
#15533=CARTESIAN_POINT ( 'NONE',  ( 7.999999999999991118, 9.797174393178815797E-16, 28.58030277982336642 ) ) ;
#15545=CARTESIAN_POINT ( 'NONE',  ( -5.656854249492375253, 5.656854249492375253, 0.8303027839201455595 ) ) ;
#15580=CARTESIAN_POINT ( 'NONE',  ( 5.082755093536320601, -5.082755093536318824, 23.04905278187175455 ) ) ;
#15605=CARTESIAN_POINT ( 'NONE',  ( -7.188101187499992051, 2.977408999572646930, 21.26780278187175810 ) ) ;
#15623=CARTESIAN_POINT ( 'NONE',  ( 3.313708498984762496, -7.999999999999989342, 10.29905277982336465 ) ) ;
#15632=ORIENTED_EDGE ( 'NONE', *, *, #10674, .T. ) ;
#15633=CARTESIAN_POINT ( 'NONE',  ( 7.999999999667481099, -7.293937043860970585E-05, 4.767800658666735636 ) ) ;
#15650=CARTESIAN_POINT ( 'NONE',  ( -8.008118988124989457, -3.317071493978883900, 17.60686528394063188 ) ) ;
#15651=CARTESIAN_POINT ( 'NONE',  ( -7.999999999999991118, 3.313708498984757167, 23.42405278392015333 ) ) ;
#15671=B_SPLINE_CURVE_WITH_KNOTS ( 'NONE', 1,
 ( #17225, #57996 ),
 .UNSPECIFIED., .F., .F.,
 ( 2, 2 ),
 ( 0.000000000000000000, 1.000000000000000000 ),
 .UNSPECIFIED. ) ;
#15687=CARTESIAN_POINT ( 'NONE',  ( -7.188101187499992051, 0.000000000000000000, 25.86155278187175810 ) ) ;
#15702=ORIENTED_EDGE ( 'NONE', *, *, #41485, .T. ) ;
#15711=CARTESIAN_POINT ( 'NONE',  ( -3.313708498984758943, -7.999999999999989342, 25.11155277982337353 ) ) ;
#15713=LINE ( 'NONE', #61379, #1425 ) ;
#15729=CARTESIAN_POINT ( 'NONE',  ( 7.999999999999991118, 3.313708498984757611, 12.36155278392014445 ) ) ;
#15733=EDGE_CURVE ( 'NONE', #14756, #49450, #71848, .T. ) ;
#15741=CARTESIAN_POINT ( 'NONE',  ( -7.999999999961167951, -1.666173683171983354E-05, 1.018425797410095646 ) ) ;
#15748=CARTESIAN_POINT ( 'NONE',  ( 1.320432766682872962E-15, -7.188101187499992051, 16.86155278187175810 ) ) ;
#15756=EDGE_CURVE ( 'NONE', #14923, #58023, #58878, .T. ) ;
#15776=CARTESIAN_POINT ( 'NONE',  ( -2.977408999572647819, 7.188101187499991163, 14.70530278187175455 ) ) ;
#15800=CARTESIAN_POINT ( 'NONE',  ( -5.082755093536317936, -5.082755093536320601, 17.04905278187175810 ) ) ;
#15815=CARTESIAN_POINT ( 'NONE',  ( 5.656854249492376141, -5.656854249492374365, 11.89280277982336642 ) ) ;
#15816=CARTESIAN_POINT ( 'NONE',  ( -5.656854249492375253, 5.656854249492375253, 21.83030278392014623 ) ) ;
#15831=CARTESIAN_POINT ( 'NONE',  ( 7.999999999999991118, 3.313708498984757611, 10.73030278432982598 ) ) ;
#15854=CARTESIAN_POINT ( 'NONE',  ( 7.999999999996472155, 7.505344305739403062E-06, 9.267802996260090964 ) ) ;
#15857=( NAMED_UNIT ( * ) SI_UNIT ( $, .STERADIAN. ) SOLID_ANGLE_UNIT ( ) );
#15862=CARTESIAN_POINT ( 'NONE',  ( -5.447321192899549303, -4.689935021205116961, 0.1569292013794422458 ) ) ;
#15865=ORIENTED_EDGE ( 'NONE', *, *, #15756, .T. ) ;
#15875=CARTESIAN_POINT ( 'NONE',  ( -5.082755093536317936, -5.082755093536320601, 5.049052781871752771 ) ) ;
#15906=CARTESIAN_POINT ( 'NONE',  ( -7.999999999999991118, 0.000000000000000000, 29.33030277982336642 ) ) ;
#15918=CARTESIAN_POINT ( 'NONE',  ( 7.999999999999992895, -3.313708498984756279, 0.1740527839201450044 ) ) ;
#15955=CARTESIAN_POINT ( 'NONE',  ( -4.401442555609577197E-16, 7.188101187499992051, 17.61155278187175810 ) ) ;
#15970=CARTESIAN_POINT ( 'NONE',  ( -7.999999999999948486, 3.313708498984799355, 8.236552779823361092 ) ) ;
#15978=CARTESIAN_POINT ( 'NONE',  ( 1.320432766682872962E-15, -7.188101187499992051, 17.23655278187175810 ) ) ;
#15997=CARTESIAN_POINT ( 'NONE',  ( -7.999999999999991118, 3.313708498984756723, 2.236552779823365533 ) ) ;
#15998=CARTESIAN_POINT ( 'NONE',  ( 5.656854249492376141, -5.656854249492374365, 21.08030278392014623 ) ) ;
#16024=CARTESIAN_POINT ( 'NONE',  ( 8.008118988124991233, 9.807117285998411148E-16, 19.76311528394062833 ) ) ;
#16032=VERTEX_POINT ( 'NONE', #53414 ) ;
#16054=ORIENTED_EDGE ( 'NONE', *, *, #15349, .F. ) ;
#16056=CARTESIAN_POINT ( 'NONE',  ( 7.188101187499991163, 2.977408999572648707, 25.20530278187175810 ) ) ;
#16079=CARTESIAN_POINT ( 'NONE',  ( 5.656854249492374365, 5.656854249492375253, 27.26780277982336642 ) ) ;
#16085=CARTESIAN_POINT ( 'NONE',  ( -8.000000000000033751, -3.313708498984719864, 14.42405277982336465 ) ) ;
#16093=CARTESIAN_POINT ( 'NONE',  ( -3.313708498984759387, -7.999999999999989342, 11.61155277982336820 ) ) ;
#16096=CARTESIAN_POINT ( 'NONE',  ( -3.313708498984758943, -7.999999999999989342, 14.79905278392014978 ) ) ;
#16107=CARTESIAN_POINT ( 'NONE',  ( 1.469576158976822172E-15, -7.999999999999991118, 28.20530277982336642 ) ) ;
#16116=CARTESIAN_POINT ( 'NONE',  ( -2.977408999572647819, -7.188101187499990274, 16.76780278187175455 ) ) ;
#16124=EDGE_LOOP ( 'NONE', ( #9643, #72361, #16054, #56494 ) ) ;
#16136=CARTESIAN_POINT ( 'NONE',  ( -2.977408999572648707, -7.188101187499990274, 12.26780278187175455 ) ) ;
#16161=CARTESIAN_POINT ( 'NONE',  ( -5.082755093536319713, 5.082755093536319713, 16.67405278187175810 ) ) ;
#16176=CARTESIAN_POINT ( 'NONE',  ( -7.999999999999991118, 0.000000000000000000, 28.01780278392014978 ) ) ;
#16192=CARTESIAN_POINT ( 'NONE',  ( -5.656854249492373476, -5.656854249492376141, 2.705302783920143561 ) ) ;
#16194=CARTESIAN_POINT ( 'NONE',  ( 7.999999999999992895, -3.313708498984756279, 4.542802784329823318 ) ) ;
#16201=ORIENTED_EDGE ( 'NONE', *, *, #15349, .T. ) ;
#16241=CARTESIAN_POINT ( 'NONE',  ( -2.977408999572648707, -7.188101187499990274, 3.642802781871751883 ) ) ;
#16254=CARTESIAN_POINT ( 'NONE',  ( 7.188101187499992051, 8.802885111219154394E-16, 1.111552781871753215 ) ) ;
#16259=CARTESIAN_POINT ( 'NONE',  ( 7.999999999999991118, 9.797174393178815797E-16, 28.58030277982336642 ) ) ;
#16261=EDGE_CURVE ( 'NONE', #73165, #33251, #13023, .T. ) ;
#16270=CARTESIAN_POINT ( 'NONE',  ( -7.999999999999989342, -3.313708498984762496, 18.92405277982336642 ) ) ;
#16281=CARTESIAN_POINT ( 'NONE',  ( -7.999999999999991118, 3.313708498984756723, 0.9240527839201456706 ) ) ;
#16309=EDGE_CURVE ( 'NONE', #70218, #71597, #5337, .T. ) ;
#16316=CARTESIAN_POINT ( 'NONE',  ( -5.082755093536319713, 5.082755093536319713, 17.79905278187175455 ) ) ;
#16340=CARTESIAN_POINT ( 'NONE',  ( 2.977408999572650927, -7.188101187499990274, 14.33030278187175277 ) ) ;
#16349=CARTESIAN_POINT ( 'NONE',  ( -7.999999999999992895, -1.544684865728715588E-05, 17.51780322093567577 ) ) ;
#16357=CARTESIAN_POINT ( 'NONE',  ( -4.898587196589407898E-16, 7.999999999999991118, 1.955302779823364645 ) ) ;
#16358=CARTESIAN_POINT ( 'NONE',  ( 3.313708498984762496, -7.999999999999989342, 20.98655278392014978 ) ) ;
#16386=CARTESIAN_POINT ( 'NONE',  ( 5.662595241051936235, -5.662595241051934458, 19.57561528394063188 ) ) ;
#16417=CARTESIAN_POINT ( 'NONE',  ( -5.656854249492373476, -5.656854249492376141, 2.517802779823365089 ) ) ;
#16419=CARTESIAN_POINT ( 'NONE',  ( -8.000072035430726203, -0.9604724192222298118, 0.000000000000000000 ) ) ;
#16423=CARTESIAN_POINT ( 'NONE',  ( 7.188101187499993827, -2.977408999572645598, 23.51780278187175455 ) ) ;
#16430=DIRECTION ( 'NONE',  ( 1.000000000000000000, 0.000000000000000000, 0.000000000000000000 ) ) ;
#16449=CARTESIAN_POINT ( 'NONE',  ( -7.999999999999991118, 3.313708498984756723, 23.23655277982336642 ) ) ;
#16450=CARTESIAN_POINT ( 'NONE',  ( 3.499857865026532622, -7.193933550196781823, 0.0006324257780546024528 ) ) ;
#16468=CARTESIAN_POINT ( 'NONE',  ( 7.999999999999991118, 9.797174393178815797E-16, 13.76780278392014623 ) ) ;
#16482=CARTESIAN_POINT ( 'NONE',  ( -7.999999999999991118, 0.000000000000000000, 27.83030277982336642 ) ) ;
#16494=ORIENTED_EDGE ( 'NONE', *, *, #5155, .F. ) ;
#16514=CARTESIAN_POINT ( 'NONE',  ( -5.082755093536319713, 5.082755093536319713, 11.79905278187175277 ) ) ;
#16536=CARTESIAN_POINT ( 'NONE',  ( -2.977408999572647819, 7.188101187499991163, 9.080302781871752771 ) ) ;
#16538=( BOUNDED_CURVE ( )  B_SPLINE_CURVE ( 2, ( #47697, #64697, #1709, #30365, #69621, #36767, #24326, #17935, #58678 ),
 .UNSPECIFIED., .F., .F. ) 
 B_SPLINE_CURVE_WITH_KNOTS ( ( 3, 2, 2, 2, 3 ),
 ( 0.8947368421052632748, 0.9013157894736842923, 0.9078947368421054209, 0.9144736842105264385, 0.9210526315789474561 ),
 .UNSPECIFIED. ) 
 CURVE ( )  GEOMETRIC_REPRESENTATION_ITEM ( )  RATIONAL_B_SPLINE_CURVE ( ( 0.9999999999999986677, 0.9238795325112880708, 1.000000000000000000, 0.9238795325112867385, 1.000000000000000000, 0.9238795325112867385, 1.000000000000000000, 0.9238795325112854062, 1.000000000000001332 ) ) 
 REPRESENTATION_ITEM ( '' )  );
#16540=CARTESIAN_POINT ( 'NONE',  ( 3.313708498984762496, -7.999999999999989342, 1.486552783920146448 ) ) ;
#16543=VECTOR ( 'NONE', #72515, 1000.000000000000000 ) ;
#16553=CARTESIAN_POINT ( 'NONE',  ( 3.313708498984762496, -7.999999999999989342, 4.299052779823363757 ) ) ;
#16570=CARTESIAN_POINT ( 'NONE',  ( -4.898587196589407898E-16, 7.999999999999991118, 5.011552784329824206 ) ) ;
#16600=CARTESIAN_POINT ( 'NONE',  ( -7.188101187499992051, 0.000000000000000000, 28.48655278187175810 ) ) ;
#16604=CARTESIAN_POINT ( 'NONE',  ( -4.898587196589407898E-16, 7.999999999999991118, 19.95530277982336642 ) ) ;
#16615=CARTESIAN_POINT ( 'NONE',  ( -7.188101187499992051, 0.000000000000000000, 3.361552781871751883 ) ) ;
#16627=CARTESIAN_POINT ( 'NONE',  ( -5.082755093536317936, -5.082755093536320601, 0.5490527818717526598 ) ) ;
#16643=CARTESIAN_POINT ( 'NONE',  ( -3.313708498984758943, -7.999999999999989342, 22.11155277982336997 ) ) ;
#16655=CARTESIAN_POINT ( 'NONE',  ( -3.313708498984757167, 7.999999999999991118, 26.10530278432982598 ) ) ;
#16688=CARTESIAN_POINT ( 'NONE',  ( -7.188101187499990274, -2.977408999572651371, 21.08030278187175810 ) ) ;
#16704=CARTESIAN_POINT ( 'NONE',  ( -5.656854249492375253, 5.656854249492375253, 8.142802779823362869 ) ) ;
#16711=CARTESIAN_POINT ( 'NONE',  ( -4.401442555609577197E-16, 7.188101187499992051, 16.48655278187175810 ) ) ;
#16718=VECTOR ( 'NONE', #6861, 1000.000000000000000 ) ;
#16761=CARTESIAN_POINT ( 'NONE',  ( -5.656854249492375253, 5.656854249492375253, 8.330302783920144449 ) ) ;
#16762=CARTESIAN_POINT ( 'NONE',  ( 8.008118988124993010, -3.317071493978877239, 21.16936528394063899 ) ) ;
#16772=( BOUNDED_CURVE ( )  B_SPLINE_CURVE ( 2, ( #7279, #30286, #2352, #64974, #24975, #1631, #18962, #24611, #41965, #36323, #7649, #42333, #65715 ),
 .UNSPECIFIED., .F., .F. ) 
 B_SPLINE_CURVE_WITH_KNOTS ( ( 3, 2, 2, 2, 2, 2, 3 ),
 ( 0.8471392367758522335, 0.8471392748104720205, 0.8537575503949288436, 0.8603758259793856666, 0.8669941015638423787, 0.8736123771482992018, 0.8736124324192364732 ),
 .UNSPECIFIED. ) 
 CURVE ( )  GEOMETRIC_REPRESENTATION_ITEM ( )  RATIONAL_B_SPLINE_CURVE ( ( 0.9999991250904070039, 0.9999995625426895129, 1.000000000000000000, 0.9238795325112867385, 1.000000000000000000, 0.9238795325112867385, 1.000000000000000000, 0.9238795325112867385, 1.000000000000000000, 0.9238795325112867385, 1.000000000000000000, 0.9999993642982181186, 0.9999987286070540771 ) ) 
 REPRESENTATION_ITEM ( '' )  );
#16782=CARTESIAN_POINT ( 'NONE',  ( -7.999999999999991118, 3.313708498984756723, 5.424052783920145338 ) ) ;
#16796=CARTESIAN_POINT ( 'NONE',  ( 5.082755093536320601, -5.082755093536318824, 20.42405278187175810 ) ) ;
#16799=SPHERICAL_SURFACE ( 'NONE', #2601, 15.99999999999998579 ) ;
#16807=CARTESIAN_POINT ( 'NONE',  ( -3.313708498984757611, 7.999999999999991118, 27.73655278392014978 ) ) ;
#16815=CARTESIAN_POINT ( 'NONE',  ( 3.459103461385761413, -7.213501455148458419, -0.0001169852011744028255 ) ) ;
#16822=CARTESIAN_POINT ( 'NONE',  ( 0.000000000000000000, 0.000000000000000000, 30.00000000000000000 ) ) ;
#16823=CARTESIAN_POINT ( 'NONE',  ( 7.999999999999991118, 9.797174393178815797E-16, 24.08030277982336642 ) ) ;
#16840=CARTESIAN_POINT ( 'NONE',  ( -8.000000000000033751, -3.313708498984719864, 11.42405277982336642 ) ) ;
#16843=CARTESIAN_POINT ( 'NONE',  ( -5.656854249492375253, 5.656854249492375253, 11.33030278392014445 ) ) ;
#16881=EDGE_CURVE ( 'NONE', #13756, #70510, #21210, .T. ) ;
#16896=CARTESIAN_POINT ( 'NONE',  ( -2.977408999572648707, -7.188101187499990274, 15.26780278187175455 ) ) ;
#16912=ORIENTED_EDGE ( 'NONE', *, *, #21736, .T. ) ;
#16923=CARTESIAN_POINT ( 'NONE',  ( -4.401442555609577197E-16, 7.188101187499992051, 10.48655278187175455 ) ) ;
#16926=CARTESIAN_POINT ( 'NONE',  ( -3.313708498984757167, 7.999999999999991118, 2.105302784329821542 ) ) ;
#16937=CARTESIAN_POINT ( 'NONE',  ( -7.999999999999991118, 0.000000000000000000, 2.330302779823365089 ) ) ;
#16954=CARTESIAN_POINT ( 'NONE',  ( -4.898587196589407898E-16, 7.999999999999991118, 6.511552784329821542 ) ) ;
#16981=CARTESIAN_POINT ( 'NONE',  ( 5.082755093536320601, -5.082755093536318824, 3.549052781871751883 ) ) ;
#16996=CARTESIAN_POINT ( 'NONE',  ( 7.188101187499992051, 8.802885111219154394E-16, 5.611552781871753659 ) ) ;
#17025=CARTESIAN_POINT ( 'NONE',  ( 5.656854249492376141, -5.656854249492374365, 23.89280277982336642 ) ) ;
#17039=CARTESIAN_POINT ( 'NONE',  ( 5.656854249492374365, 5.656854249492375253, 25.82405278432982243 ) ) ;
#17047=EDGE_CURVE ( 'NONE', #60780, #51815, #66391, .T. ) ;
#17057=AXIS2_PLACEMENT_3D ( 'NONE', #51914, #63591, #6272 ) ;
#17073=CARTESIAN_POINT ( 'NONE',  ( 5.082755093536318824, 5.082755093536319713, 18.92405278187175455 ) ) ;
#17089=CARTESIAN_POINT ( 'NONE',  ( -5.656854249492375253, 5.656854249492375253, 26.33030278392014623 ) ) ;
#17094=CARTESIAN_POINT ( 'NONE',  ( -2.977408999572647819, -7.188101187499990274, 17.14280278187175455 ) ) ;
#17109=( BOUNDED_CURVE ( )  B_SPLINE_CURVE ( 2, ( #65050, #54121, #65797, #31092, #48071, #43155, #20139, #7358, #53750, #42780, #25425, #71444, #47338 ),
 .UNSPECIFIED., .F., .F. ) 
 B_SPLINE_CURVE_WITH_KNOTS ( ( 3, 2, 2, 2, 2, 2, 3 ),
 ( 0.9000854414465758735, 0.9000854794861264940, 0.9067037550705827620, 0.9133220306550392520, 0.9199403062394955199, 0.9265585818239518989, 0.9265586498208127075 ),
 .UNSPECIFIED. ) 
 CURVE ( )  GEOMETRIC_REPRESENTATION_ITEM ( )  RATIONAL_B_SPLINE_CURVE ( ( 0.9999991249769839552, 0.9999995624859773224, 1.000000000000000000, 0.9238795325112867385, 1.000000000000000000, 0.9238795325112867385, 1.000000000000000000, 0.9238795325112867385, 1.000000000000000000, 0.9238795325112867385, 1.000000000000000000, 0.9999992179302951145, 0.9999984358766603743 ) ) 
 REPRESENTATION_ITEM ( '' )  );
#17116=CARTESIAN_POINT ( 'NONE',  ( -3.313708498984757167, 7.999999999999991118, 5.049052779823364645 ) ) ;
#17143=CARTESIAN_POINT ( 'NONE',  ( 5.662595241051936235, -5.662595241051934458, 12.07561528394063011 ) ) ;
#17166=CARTESIAN_POINT ( 'NONE',  ( 5.656854249492374365, 5.656854249492375253, 4.955302783920146226 ) ) ;
#17179=CARTESIAN_POINT ( 'NONE',  ( -5.082755093536317936, -5.082755093536320601, 17.04905278187175810 ) ) ;
#17182=FACE_OUTER_BOUND ( 'NONE', #50859, .T. ) ;
#17185=CARTESIAN_POINT ( 'NONE',  ( 7.999999999999991118, 9.797174393178815797E-16, 24.08030277982336642 ) ) ;
#17199=CARTESIAN_POINT ( 'NONE',  ( 3.058894802626711318, -7.395264550195966180, -0.000000000000000000 ) ) ;
#17204=FACE_OUTER_BOUND ( 'NONE', #38005, .T. ) ;
#17205=CARTESIAN_POINT ( 'NONE',  ( -5.656854249492373476, -5.656854249492376141, 20.51780277982336642 ) ) ;
#17209=( BOUNDED_CURVE ( )  B_SPLINE_CURVE ( 2, ( #73916, #22220, #45247, #68259, #5268, #73177, #21485, #38851, #61855 ),
 .UNSPECIFIED., .F., .F. ) 
 B_SPLINE_CURVE_WITH_KNOTS ( ( 3, 2, 2, 2, 3 ),
 ( 0.8206662513146789628, 0.8272844480571014403, 0.8339027236415583744, 0.8405209992260151974, 0.8471392367758522335 ),
 .UNSPECIFIED. ) 
 CURVE ( )  GEOMETRIC_REPRESENTATION_ITEM ( )  RATIONAL_B_SPLINE_CURVE ( ( 0.9999981864094533712, 0.9238804393173626339, 1.000000000000000000, 0.9238795325112867385, 1.000000000000000000, 0.9238795325112867385, 1.000000000000000000, 0.9238799699685972255, 0.9999991250904070039 ) ) 
 REPRESENTATION_ITEM ( '' )  );
#17223=CARTESIAN_POINT ( 'NONE',  ( -5.656854249492375253, 5.656854249492375253, 15.83030278392014800 ) ) ;
#17225=CARTESIAN_POINT ( 'NONE',  ( -7.999999999999991118, 0.000000000000000000, 28.01780278392014978 ) ) ;
#17255=ADVANCED_FACE ( 'NONE', ( #8693 ), #71309, .F. ) ;
#17258=ORIENTED_EDGE ( 'NONE', *, *, #7928, .F. ) ;
#17274=CARTESIAN_POINT ( 'NONE',  ( 5.082755093536318824, 5.082755093536319713, 8.424052781871752771 ) ) ;
#17298=CARTESIAN_POINT ( 'NONE',  ( -2.977408999572647819, 7.188101187499991163, 7.580302781871751883 ) ) ;
#17310=CARTESIAN_POINT ( 'NONE',  ( -3.313708498984758943, -7.999999999999989342, 2.611552779823365977 ) ) ;
#17325=CARTESIAN_POINT ( 'NONE',  ( 3.313708498984762496, -7.999999999999989342, 5.855302784329825094 ) ) ;
#17333=CARTESIAN_POINT ( 'NONE',  ( 7.188101187499992051, 2.977408999572647819, 26.33030278187176165 ) ) ;
#17346=CARTESIAN_POINT ( 'NONE',  ( 7.999999999999991118, 3.313708498984757611, 19.86155278392014978 ) ) ;
#17356=CARTESIAN_POINT ( 'NONE',  ( 5.082755093536318824, 5.082755093536319713, 23.42405278187175455 ) ) ;
#17369=CARTESIAN_POINT ( 'NONE',  ( -4.401442555609577197E-16, 7.188101187499992051, 2.986552781871751439 ) ) ;
#17374=CARTESIAN_POINT ( 'NONE',  ( 8.008118988124991233, 9.807117285998411148E-16, 3.263115283940628331 ) ) ;
#17378=CARTESIAN_POINT ( 'NONE',  ( -7.999999999999989342, -3.313708498984762496, 6.924052779823365533 ) ) ;
#17398=CARTESIAN_POINT ( 'NONE',  ( 5.656854249492374365, 5.656854249492375253, 19.76780277982336642 ) ) ;
#17412=CARTESIAN_POINT ( 'NONE',  ( 5.656854249492376141, -5.656854249492374365, 23.94905278432982598 ) ) ;
#17446=CARTESIAN_POINT ( 'NONE',  ( -7.188101187499991163, 2.977408999572646930, 19.39280278187176165 ) ) ;
#17459=EDGE_CURVE ( 'NONE', #37555, #70218, #28018, .T. ) ;
#17470=CARTESIAN_POINT ( 'NONE',  ( -2.977408999572647819, 7.188101187499992051, 15.08030278187175455 ) ) ;
#17493=CARTESIAN_POINT ( 'NONE',  ( -3.313708498984758943, -7.999999999999989342, 2.611552779823365977 ) ) ;
#17520=CARTESIAN_POINT ( 'NONE',  ( 5.662595241051936235, -5.662595241051934458, 13.57561528394063011 ) ) ;
#17526=CARTESIAN_POINT ( 'NONE',  ( -2.977408999572647819, -7.188101187499990274, 13.76780278187175455 ) ) ;
#17540=CARTESIAN_POINT ( 'NONE',  ( 3.313708498984756279, 7.999999999999991118, 8.049052783920146226 ) ) ;
#17552=ORIENTED_EDGE ( 'NONE', *, *, #26417, .T. ) ;
#17555=CARTESIAN_POINT ( 'NONE',  ( -5.082755093536319713, 5.082755093536319713, 15.17405278187175455 ) ) ;
#17581=CARTESIAN_POINT ( 'NONE',  ( 7.999999999999991118, 9.797174393178815797E-16, 19.58030277982336642 ) ) ;
#17600=CARTESIAN_POINT ( 'NONE',  ( 5.656854249492374365, 5.656854249492375253, 4.955302783920146226 ) ) ;
#17645=CARTESIAN_POINT ( 'NONE',  ( 1.320432766682872962E-15, -7.188101187499992051, 9.361552781871752771 ) ) ;
#17672=CARTESIAN_POINT ( 'NONE',  ( 2.977408999572646486, 7.188101187499991163, 8.892802781871754547 ) ) ;
#17676=CARTESIAN_POINT ( 'NONE',  ( 3.313708498984756279, 7.999999999999991118, 0.4178027843298233734 ) ) ;
#17686=CARTESIAN_POINT ( 'NONE',  ( -3.313708498984758943, -7.999999999999989342, 4.111552779823362869 ) ) ;
#17699=CARTESIAN_POINT ( 'NONE',  ( -3.313708498984758943, -7.999999999999989342, 5.667802784329825094 ) ) ;
#17708=CARTESIAN_POINT ( 'NONE',  ( -7.188101187499992051, 2.977408999572646930, 26.89280278187175455 ) ) ;
#17718=CARTESIAN_POINT ( 'NONE',  ( 3.313708498984762496, -7.999999999999989342, 17.98655278392014978 ) ) ;
#17728=CARTESIAN_POINT ( 'NONE',  ( 2.977408999572646486, 7.188101187499991163, 23.51780278187175455 ) ) ;
#17749=CARTESIAN_POINT ( 'NONE',  ( 8.008118988124991233, 3.317071493978879015, 1.856865283940626998 ) ) ;
#17756=CARTESIAN_POINT ( 'NONE',  ( 7.188101187499992051, 8.802885111219154394E-16, 25.11155278187175810 ) ) ;
#17763=CARTESIAN_POINT ( 'NONE',  ( -3.313708498984757611, 7.999999999999991118, 29.04905277982336997 ) ) ;
#17773=CARTESIAN_POINT ( 'NONE',  ( 7.999999999999991118, 3.313708498984757611, 21.17405277982336642 ) ) ;
#17790=CARTESIAN_POINT ( 'NONE',  ( 7.999999999999991118, 9.797174393178815797E-16, 25.63655278432982954 ) ) ;
#17813=CARTESIAN_POINT ( 'NONE',  ( -7.999999999999861444, -9.580972845112835701E-07, 13.01783880491507261 ) ) ;
#17816=CYLINDRICAL_SURFACE ( 'NONE', #34342, 7.999999999999991118 ) ;
#17824=CARTESIAN_POINT ( 'NONE',  ( 5.082755093536320601, -5.082755093536318824, 15.54905278187175455 ) ) ;
#17847=CARTESIAN_POINT ( 'NONE',  ( -4.401442555609577197E-16, 7.188101187499992051, 8.986552781871752771 ) ) ;
#17897=CARTESIAN_POINT ( 'NONE',  ( 1.471067592899761672E-15, -8.008118988124991233, 16.38811528394063188 ) ) ;
#17903=CARTESIAN_POINT ( 'NONE',  ( 2.977408999572650927, -7.188101187499990274, 10.95530278187175455 ) ) ;
#17917=CARTESIAN_POINT ( 'NONE',  ( 3.313708498984762496, -7.999999999999989342, 2.986552783920144449 ) ) ;
#17933=CARTESIAN_POINT ( 'NONE',  ( 2.977408999572650927, -7.188101187499990274, 20.33030278187175455 ) ) ;
#17935=CARTESIAN_POINT ( 'NONE',  ( 8.000000000000035527, 3.313708498984715423, 3.174052779823360648 ) ) ;
#17957=CARTESIAN_POINT ( 'NONE',  ( -5.656854249492375253, 5.656854249492375253, 23.14280277982336642 ) ) ;
#17962=CARTESIAN_POINT ( 'NONE',  ( -7.999999999999991118, 9.797174393178815797E-16, 30.00000000000000000 ) ) ;
#17974=CARTESIAN_POINT ( 'NONE',  ( 7.999999999999991118, 3.313708498984757611, 7.861552783920145338 ) ) ;
#18006=EDGE_CURVE ( 'NONE', #6793, #471, #56020, .T. ) ;
#18024=AXIS2_PLACEMENT_3D ( 'NONE', #31100, #47707, #36042 ) ;
#18026=CARTESIAN_POINT ( 'NONE',  ( -5.082755093536317936, -5.082755093536320601, 7.674052781871751883 ) ) ;
#18050=CARTESIAN_POINT ( 'NONE',  ( -7.188101187499990274, -2.977408999572651371, 12.45530278187175277 ) ) ;
#18053=CARTESIAN_POINT ( 'NONE',  ( 3.313708498984762496, -7.999999999999989342, 2.855302784329822430 ) ) ;
#18055=CARTESIAN_POINT ( 'NONE',  ( -3.313708498984759387, -7.999999999999989342, 7.299052783920144449 ) ) ;
#18063=CARTESIAN_POINT ( 'NONE',  ( 5.656854249492374365, 5.656854249492375253, 24.45530278392014978 ) ) ;
#18097=CARTESIAN_POINT ( 'NONE',  ( -7.999999999999991118, 0.000000000000000000, 22.01780278392014623 ) ) ;
#18100=CYLINDRICAL_SURFACE ( 'NONE', #29450, 7.999999999999991118 ) ;
#18108=CARTESIAN_POINT ( 'NONE',  ( -2.977408999572647819, 7.188101187499991163, 26.70530278187175455 ) ) ;
#18121=CARTESIAN_POINT ( 'NONE',  ( 7.188101187499992051, 8.802885111219154394E-16, 2.611552781871750994 ) ) ;
#18126=CARTESIAN_POINT ( 'NONE',  ( 8.008118988124991233, 9.807117285998411148E-16, 6.263115283940630995 ) ) ;
#18133=CARTESIAN_POINT ( 'NONE',  ( -2.977408999572647819, 7.188101187499991163, 27.08030278187175810 ) ) ;
#18140=CARTESIAN_POINT ( 'NONE',  ( 0.000000000000000000, 0.000000000000000000, 30.00000000000000000 ) ) ;
#18151=CARTESIAN_POINT ( 'NONE',  ( 1.469576158976822172E-15, -7.999999999999991118, 14.70530277982336642 ) ) ;
#18165=CARTESIAN_POINT ( 'NONE',  ( -4.898587196589407898E-16, 7.999999999999991118, 21.51155278432982243 ) ) ;
#18199=CARTESIAN_POINT ( 'NONE',  ( -7.188101187499991163, 2.977408999572646930, 14.89280278187175455 ) ) ;
#18222=CARTESIAN_POINT ( 'NONE',  ( 2.977408999572646486, 7.188101187499992051, 11.89280278187175810 ) ) ;
#18264=ORIENTED_EDGE ( 'NONE', *, *, #13708, .T. ) ;
#18267=CARTESIAN_POINT ( 'NONE',  ( 5.662595241051934458, 5.662595241051935346, 13.95061528394063011 ) ) ;
#18273=CARTESIAN_POINT ( 'NONE',  ( 1.320432766682872962E-15, -7.188101187499992051, 10.86155278187175455 ) ) ;
#18288=CARTESIAN_POINT ( 'NONE',  ( -7.999999999999989342, -3.313708498984762496, 1.111552783920146004 ) ) ;
#18302=CARTESIAN_POINT ( 'NONE',  ( -5.082755093536319713, 5.082755093536319713, 18.17405278187175455 ) ) ;
#18312=CARTESIAN_POINT ( 'NONE',  ( -5.656854249492373476, -5.656854249492376141, 4.017802779823362869 ) ) ;
#18317=CARTESIAN_POINT ( 'NONE',  ( -4.898587196589407898E-16, 7.999999999999991118, 25.95530277982336997 ) ) ;
#18322=CARTESIAN_POINT ( 'NONE',  ( -0.7855267195163277982, -7.974084888391890225, -0.000000000000000000 ) ) ;
#18328=CARTESIAN_POINT ( 'NONE',  ( 7.999999999999991118, 3.313708498984757611, 13.67405277982336287 ) ) ;
#18332=( BOUNDED_CURVE ( )  B_SPLINE_CURVE ( 2, ( #29630, #58681, #57952, #6990, #1712, #58319, #12636, #59052, #46600 ),
 .UNSPECIFIED., .F., .F. ) 
 B_SPLINE_CURVE_WITH_KNOTS ( ( 3, 2, 2, 2, 3 ),
 ( 0.2912041257482609335, 0.2978224013005510984, 0.3044406768850113632, 0.3110589524694716279, 0.3176771498271482308 ),
 .UNSPECIFIED. ) 
 CURVE ( )  GEOMETRIC_REPRESENTATION_ITEM ( )  RATIONAL_B_SPLINE_CURVE ( ( 1.000000000000000000, 0.9238795325112867385, 1.000000000000000000, 0.9238795325112867385, 1.000000000000000000, 0.9238795325112867385, 1.000000000000000000, 0.9238804322410221204, 0.9999982005617984449 ) ) 
 REPRESENTATION_ITEM ( '' )  );
#18347=CARTESIAN_POINT ( 'NONE',  ( -7.999999999999989342, -3.313708498984762496, 7.111552783920144449 ) ) ;
#18362=CARTESIAN_POINT ( 'NONE',  ( 7.999999999999967137, -3.313708498984783368, 26.98655277982336997 ) ) ;
#18384=ORIENTED_EDGE ( 'NONE', *, *, #22072, .T. ) ;
#18396=CARTESIAN_POINT ( 'NONE',  ( 2.977408999572650927, -7.188101187499990274, 7.955302781871752771 ) ) ;
#18406=ORIENTED_EDGE ( 'NONE', *, *, #24158, .T. ) ;
#18421=CARTESIAN_POINT ( 'NONE',  ( 5.082755093536320601, -5.082755093536318824, 3.924052781871752327 ) ) ;
#18434=CARTESIAN_POINT ( 'NONE',  ( 1.469576158976822172E-15, -7.999999999999991118, 26.89280278392014623 ) ) ;
#18453=CARTESIAN_POINT ( 'NONE',  ( 7.999999999999991118, 0.000000000000000000, 30.00000000000000000 ) ) ;
#18457=CARTESIAN_POINT ( 'NONE',  ( -2.977408999572647819, -7.188101187499990274, 25.76780278187175810 ) ) ;
#18466=CARTESIAN_POINT ( 'NONE',  ( 7.999999999999991118, 3.313708498984757611, 21.36155278392014978 ) ) ;
#18468=ORIENTED_EDGE ( 'NONE', *, *, #19433, .F. ) ;
#18478=CARTESIAN_POINT ( 'NONE',  ( -5.082755093536319713, 5.082755093536319713, 25.29905278187175810 ) ) ;
#18492=CYLINDRICAL_SURFACE ( 'NONE', #3707, 7.999999999999991118 ) ;
#18495=CARTESIAN_POINT ( 'NONE',  ( -5.662595241051933570, -5.662595241051936235, 2.700615283940627886 ) ) ;
#18502=CARTESIAN_POINT ( 'NONE',  ( -4.401442555609577197E-16, 7.188101187499992051, 28.48655278187175810 ) ) ;
#18521=CARTESIAN_POINT ( 'NONE',  ( -4.898587196589407898E-16, 7.999999999999991118, 16.95530277982336287 ) ) ;
#18536=CARTESIAN_POINT ( 'NONE',  ( -7.999999999999989342, -3.313708498984762496, 17.48030278432982598 ) ) ;
#18568=CARTESIAN_POINT ( 'NONE',  ( -2.977408999572647819, 7.188101187499991163, 14.70530278187175455 ) ) ;
#18591=CARTESIAN_POINT ( 'NONE',  ( -7.188101187499990274, -2.977408999572651815, 10.95530278187175455 ) ) ;
#18595=CARTESIAN_POINT ( 'NONE',  ( -5.656854249492373476, -5.656854249492376141, 20.51780277982336642 ) ) ;
#18628=VERTEX_POINT ( 'NONE', #12417 ) ;
#18640=CARTESIAN_POINT ( 'NONE',  ( 8.008118988124993010, -3.317071493978877239, 12.16936528394062833 ) ) ;
#18646=CARTESIAN_POINT ( 'NONE',  ( -7.188101187499992051, 2.977408999572646930, 10.39280278187175632 ) ) ;
#18659=CARTESIAN_POINT ( 'NONE',  ( -7.188101187499991163, 2.977408999572646930, 28.39280278187175810 ) ) ;
#18674=CARTESIAN_POINT ( 'NONE',  ( -5.082755093536317936, -5.082755093536320601, 11.04905278187175455 ) ) ;
#18681=EDGE_CURVE ( 'NONE', #2593, #33835, #46306, .T. ) ;
#18685=CARTESIAN_POINT ( 'NONE',  ( 5.082755093536320601, -5.082755093536318824, 27.92405278187175455 ) ) ;
#18702=CARTESIAN_POINT ( 'NONE',  ( -5.656854249492373476, -5.656854249492376141, 16.01780277982336642 ) ) ;
#18719=CARTESIAN_POINT ( 'NONE',  ( -7.999987529518498341, 3.313720969466249500, 6.924052284972249005 ) ) ;
#18743=ADVANCED_FACE ( 'NONE', ( #73666 ), #67272, .T. ) ;
#18746=ORIENTED_EDGE ( 'NONE', *, *, #2836, .F. ) ;
#18766=CARTESIAN_POINT ( 'NONE',  ( -4.401442555609577197E-16, 7.188101187499992051, 7.111552781871751883 ) ) ;
#18769=( BOUNDED_CURVE ( )  B_SPLINE_CURVE ( 2, ( #46678, #51980, #41764, #1782, #7439, #40281, #57651, #63658, #41399 ),
 .UNSPECIFIED., .F., .F. ) 
 B_SPLINE_CURVE_WITH_KNOTS ( ( 3, 2, 2, 2, 3 ),
 ( 0.7894736842105263275, 0.7960526315789473450, 0.8026315789473685847, 0.8092105263157896022, 0.8157894736842106198 ),
 .UNSPECIFIED. ) 
 CURVE ( )  GEOMETRIC_REPRESENTATION_ITEM ( )  RATIONAL_B_SPLINE_CURVE ( ( 1.000000000000000000, 0.9238795325112867385, 1.000000000000000000, 0.9238795325112867385, 1.000000000000000000, 0.9238795325112867385, 1.000000000000000000, 0.9238795325112854062, 1.000000000000001332 ) ) 
 REPRESENTATION_ITEM ( '' )  );
#18781=( GEOMETRIC_REPRESENTATION_CONTEXT ( 3 ) GLOBAL_UNCERTAINTY_ASSIGNED_CONTEXT ( ( #23933 ) ) GLOBAL_UNIT_ASSIGNED_CONTEXT ( ( #53643, #69881, #15857 ) ) REPRESENTATION_CONTEXT ( 'NONE', 'WORKASPACE' ) );
#18793=CARTESIAN_POINT ( 'NONE',  ( 5.082755093536318824, 5.082755093536319713, 2.799052781871750994 ) ) ;
#18795=ADVANCED_FACE ( 'NONE', ( #45363, #40082 ), #57447, .F. ) ;
#18796=DIRECTION ( 'NONE',  ( 1.224646799147353207E-16, -1.000000000000000000, 0.000000000000000000 ) ) ;
#18807=CARTESIAN_POINT ( 'NONE',  ( 3.313708498984756279, 7.999999999999991118, 27.54905278392014623 ) ) ;
#18827=CARTESIAN_POINT ( 'NONE',  ( -2.977408999572647819, -7.188101187499990274, 18.26780278187175455 ) ) ;
#18835=CARTESIAN_POINT ( 'NONE',  ( 3.313708498984756279, 7.999999999999991118, 17.04905278392014623 ) ) ;
#18845=CARTESIAN_POINT ( 'NONE',  ( -5.082755093536317936, -5.082755093536320601, 25.67405278187175810 ) ) ;
#18857=CARTESIAN_POINT ( 'NONE',  ( -5.082755093536317936, -5.082755093536320601, 0.5490527818717526598 ) ) ;
#18858=( BOUNDED_CURVE ( )  B_SPLINE_CURVE ( 2, ( #21020, #61015, #67802, #10826, #9340, #16093, #32739, #16840, #39128 ),
 .UNSPECIFIED., .F., .F. ) 
 B_SPLINE_CURVE_WITH_KNOTS ( ( 3, 2, 2, 2, 3 ),
 ( 0.6052631578947368363, 0.6118421052631578538, 0.6184210526315789824, 0.6250000000000001110, 0.6315789473684211286 ),
 .UNSPECIFIED. ) 
 CURVE ( )  GEOMETRIC_REPRESENTATION_ITEM ( )  RATIONAL_B_SPLINE_CURVE ( ( 1.000000000000000000, 0.9238795325112867385, 1.000000000000000000, 0.9238795325112867385, 1.000000000000000000, 0.9238795325112867385, 1.000000000000000000, 0.9238795325112854062, 1.000000000000001332 ) ) 
 REPRESENTATION_ITEM ( '' )  );
#18859=DIRECTION ( 'NONE',  ( -0.000000000000000000, -0.000000000000000000, 1.000000000000000000 ) ) ;
#18862=CARTESIAN_POINT ( 'NONE',  ( -8.008118988124991233, 0.000000000000000000, 1.013115283940629663 ) ) ;
#18869=CARTESIAN_POINT ( 'NONE',  ( 1.320432766682872962E-15, -7.188101187499992051, 23.23655278187175455 ) ) ;
#18887=CARTESIAN_POINT ( 'NONE',  ( -7.999999999999989342, -3.313708498984762496, 14.42405277982336465 ) ) ;
#18901=CARTESIAN_POINT ( 'NONE',  ( -7.999999999999991118, 3.313708498984756723, 18.79280278432982598 ) ) ;
#18923=CARTESIAN_POINT ( 'NONE',  ( 7.999999999971009856, 2.153409470846384379E-05, 12.26780339315719814 ) ) ;
#18933=CARTESIAN_POINT ( 'NONE',  ( 7.188101187499993827, -2.977408999572645598, 15.64280278187175277 ) ) ;
#18956=CARTESIAN_POINT ( 'NONE',  ( -2.977408999572647819, 7.188101187499992051, 9.080302781871752771 ) ) ;
#18962=CARTESIAN_POINT ( 'NONE',  ( -4.898587196589407898E-16, 7.999999999999991118, 3.642802783920144449 ) ) ;
#18978=CARTESIAN_POINT ( 'NONE',  ( 3.313708498984762496, -7.999999999999989342, 23.79905277982336287 ) ) ;
#19000=CARTESIAN_POINT ( 'NONE',  ( 5.662595241051934458, 5.662595241051935346, 6.450615283940627442 ) ) ;
#19006=CARTESIAN_POINT ( 'NONE',  ( -7.188101187499992051, 0.000000000000000000, 7.486552781871751883 ) ) ;
#19019=DIRECTION ( 'NONE',  ( 1.000000000000000000, 0.000000000000000000, 0.000000000000000000 ) ) ;
#19020=CARTESIAN_POINT ( 'NONE',  ( 7.999999999999991118, 3.313708498984757611, 4.861552783920145338 ) ) ;
#19036=CARTESIAN_POINT ( 'NONE',  ( -5.082755093536317936, -5.082755093536320601, 12.54905278187175277 ) ) ;
#19044=CARTESIAN_POINT ( 'NONE',  ( 7.188101187499993827, -2.977408999572645598, 28.01780278187175455 ) ) ;
#19058=CYLINDRICAL_SURFACE ( 'NONE', #37761, 7.999999999999991118 ) ;
#19063=CARTESIAN_POINT ( 'NONE',  ( -5.656854249492373476, -5.656854249492376141, 17.51780277982336287 ) ) ;
#19079=CARTESIAN_POINT ( 'NONE',  ( -7.999999999971585396, 1.424435121157765920E-05, 7.017269882810325932 ) ) ;
#19080=EDGE_LOOP ( 'NONE', ( #67479, #60827, #17552, #53333 ) ) ;
#19083=DIRECTION ( 'NONE',  ( -0.000000000000000000, -0.000000000000000000, 1.000000000000000000 ) ) ;
#19096=CARTESIAN_POINT ( 'NONE',  ( 7.999999999521839378, -8.746674989952265200E-05, 18.26780030933659305 ) ) ;
#19123=CARTESIAN_POINT ( 'NONE',  ( -5.082755093536317936, -5.082755093536320601, 3.174052781871751439 ) ) ;
#19126=EDGE_CURVE ( 'NONE', #28973, #64740, #14549, .T. ) ;
#19127=ORIENTED_EDGE ( 'NONE', *, *, #56468, .T. ) ;
#19149=CARTESIAN_POINT ( 'NONE',  ( -7.188101187499990274, -2.977408999572651371, 4.955302781871753659 ) ) ;
#19153=ORIENTED_EDGE ( 'NONE', *, *, #35751, .T. ) ;
#19165=CARTESIAN_POINT ( 'NONE',  ( 7.999999999999992895, -3.313708498984756279, 27.17405278392014978 ) ) ;
#19186=CARTESIAN_POINT ( 'NONE',  ( 2.977408999572650927, -7.188101187499990274, 22.95530278187175455 ) ) ;
#19188=EDGE_CURVE ( 'NONE', #69617, #41375, #44992, .T. ) ;
#19197=CARTESIAN_POINT ( 'NONE',  ( -5.656854249492375253, 5.656854249492375253, 12.83030278392014623 ) ) ;
#19209=CARTESIAN_POINT ( 'NONE',  ( 2.977408999572650927, -7.188101187499990274, 18.45530278187175455 ) ) ;
#19220=CARTESIAN_POINT ( 'NONE',  ( 2.977408999572646486, 7.188101187499991163, 1.392802781871753437 ) ) ;
#19225=CARTESIAN_POINT ( 'NONE',  ( 7.999999999999991118, 9.797174393178815797E-16, 27.26780278392014978 ) ) ;
#19231=CARTESIAN_POINT ( 'NONE',  ( -4.401442555609577197E-16, 7.188101187499992051, 23.98655278187175455 ) ) ;
#19246=CARTESIAN_POINT ( 'NONE',  ( 7.999999999999991118, 9.797174393178815797E-16, 16.58030277982336287 ) ) ;
#19261=CARTESIAN_POINT ( 'NONE',  ( 7.999999999999991118, 9.797174393178815797E-16, 19.63655278432982243 ) ) ;
#19293=CARTESIAN_POINT ( 'NONE',  ( -5.082755093536319713, 5.082755093536319713, 11.79905278187175277 ) ) ;
#19315=CARTESIAN_POINT ( 'NONE',  ( 1.320432766682872962E-15, -7.188101187499992051, 8.236552781871752771 ) ) ;
#19347=DIRECTION ( 'NONE',  ( -0.000000000000000000, -0.000000000000000000, 1.000000000000000000 ) ) ;
#19351=CYLINDRICAL_SURFACE ( 'NONE', #50495, 7.999999999999991118 ) ;
#19361=CARTESIAN_POINT ( 'NONE',  ( -5.662595241051935346, 5.662595241051935346, 9.825615283940630107 ) ) ;
#19367=CARTESIAN_POINT ( 'NONE',  ( 7.188101187499992051, 2.977408999572647819, 6.830302781871754547 ) ) ;
#19379=CARTESIAN_POINT ( 'NONE',  ( -3.313708498984758943, -7.999999999999989342, -0.2009472160798553009 ) ) ;
#19410=ORIENTED_EDGE ( 'NONE', *, *, #40554, .T. ) ;
#19423=CARTESIAN_POINT ( 'NONE',  ( 3.313708498984756279, 7.999999999999991118, 12.36155277982336820 ) ) ;
#19433=EDGE_CURVE ( 'NONE', #27289, #51761, #30316, .T. ) ;
#19453=VERTEX_POINT ( 'NONE', #64158 ) ;
#19455=CARTESIAN_POINT ( 'NONE',  ( -4.903558642999205574E-16, 8.008118988124991233, 27.63811528394063188 ) ) ;
#19471=CIRCLE ( 'NONE', #36184, 16.70329308849007077 ) ;
#19487=CARTESIAN_POINT ( 'NONE',  ( 5.082755093536318824, 5.082755093536319713, 0.9240527818717529929 ) ) ;
#19512=CARTESIAN_POINT ( 'NONE',  ( -2.977408999572647819, 7.188101187499991163, 4.580302781871752771 ) ) ;
#19520=ORIENTED_EDGE ( 'NONE', *, *, #28114, .F. ) ;
#19527=CARTESIAN_POINT ( 'NONE',  ( 7.999999999999991118, 9.797174393178815797E-16, 24.26780278392014978 ) ) ;
#19547=ORIENTED_EDGE ( 'NONE', *, *, #46194, .T. ) ;
#19550=CARTESIAN_POINT ( 'NONE',  ( 2.977408999572650927, -7.188101187499990274, 21.45530278187175810 ) ) ;
#19561=CARTESIAN_POINT ( 'NONE',  ( -4.898587196589407898E-16, 7.999999999999991118, 12.64280278392014623 ) ) ;
#19562=CARTESIAN_POINT ( 'NONE',  ( 3.313708498984756279, 7.999999999999991118, 18.54905278392014623 ) ) ;
#19571=CARTESIAN_POINT ( 'NONE',  ( 5.082755093536320601, -5.082755093536318824, 20.04905278187175455 ) ) ;
#19588=CARTESIAN_POINT ( 'NONE',  ( -4.898587196589407898E-16, 7.999999999999991118, 24.64280278392014978 ) ) ;
#19595=CARTESIAN_POINT ( 'NONE',  ( -2.977408999572647819, 7.188101187499991163, 22.58030278187175099 ) ) ;
#19603=ORIENTED_EDGE ( 'NONE', *, *, #15756, .F. ) ;
#19614=CARTESIAN_POINT ( 'NONE',  ( -7.999999999999991118, 0.000000000000000000, 12.83030277982336465 ) ) ;
#19630=CARTESIAN_POINT ( 'NONE',  ( 1.469576158976822172E-15, -7.999999999999991118, 19.26155278432982598 ) ) ;
#19631=CARTESIAN_POINT ( 'NONE',  ( -5.857508853935765814, -5.043084890513333640, 0.8444290630237344386 ) ) ;
#19661=CARTESIAN_POINT ( 'NONE',  ( -5.082755093536317936, -5.082755093536320601, 7.674052781871751883 ) ) ;
#19687=CARTESIAN_POINT ( 'NONE',  ( -7.188101187499992051, 2.977408999572646930, 7.767802781871751883 ) ) ;
#19715=CARTESIAN_POINT ( 'NONE',  ( -7.999999999999991118, 3.313708498984756723, 5.424052783920145338 ) ) ;
#19734=CARTESIAN_POINT ( 'NONE',  ( 5.662595241051934458, 5.662595241051935346, 10.95061528394063188 ) ) ;
#19740=CARTESIAN_POINT ( 'NONE',  ( 2.977408999572650927, -7.188101187499990274, 0.4553027818717525488 ) ) ;
#19750=EDGE_CURVE ( 'NONE', #52951, #73226, #58020, .T. ) ;
#19754=CARTESIAN_POINT ( 'NONE',  ( -7.188101187499992051, 0.000000000000000000, 22.48655278187175455 ) ) ;
#19763=AXIS2_PLACEMENT_3D ( 'NONE', #27842, #28213, #50848 ) ;
#19777=CARTESIAN_POINT ( 'NONE',  ( -7.188101187499992051, 0.000000000000000000, 27.36155278187175455 ) ) ;
#19796=CARTESIAN_POINT ( 'NONE',  ( 3.313708498984756279, 7.999999999999991118, 16.86155277982336642 ) ) ;
#19822=ORIENTED_EDGE ( 'NONE', *, *, #46470, .F. ) ;
#19824=CARTESIAN_POINT ( 'NONE',  ( -8.008118988124989457, -3.317071493978883900, 23.60686528394063188 ) ) ;
#19859=CARTESIAN_POINT ( 'NONE',  ( 5.082755093536318824, 5.082755093536319713, 28.29905278187175810 ) ) ;
#19871=CARTESIAN_POINT ( 'NONE',  ( 0.000000000000000000, 0.000000000000000000, 30.00000000000000000 ) ) ;
#19884=CARTESIAN_POINT ( 'NONE',  ( 5.082755093536320601, -5.082755093536318824, 2.424052781871754103 ) ) ;
#19901=CARTESIAN_POINT ( 'NONE',  ( -5.656854249492375253, 5.656854249492375253, 21.83030278392014623 ) ) ;
#19921=CARTESIAN_POINT ( 'NONE',  ( -7.188101187499992051, 0.000000000000000000, 19.48655278187175455 ) ) ;
#19929=CARTESIAN_POINT ( 'NONE',  ( 7.999999999999991118, 3.313708498984757611, 16.86155278392014623 ) ) ;
#19943=CARTESIAN_POINT ( 'NONE',  ( 7.188101187499992051, 8.802885111219154394E-16, 15.73655278187175632 ) ) ;
#19962=CARTESIAN_POINT ( 'NONE',  ( -5.656854249492373476, -5.656854249492376141, 25.20530278392014978 ) ) ;
#19969=CARTESIAN_POINT ( 'NONE',  ( 5.082755093536320601, -5.082755093536318824, 24.92405278187175810 ) ) ;
#19974=ORIENTED_EDGE ( 'NONE', *, *, #30782, .F. ) ;
#19984=CARTESIAN_POINT ( 'NONE',  ( -5.656854249492373476, -5.656854249492376141, 11.51780277982336642 ) ) ;
#19987=EDGE_CURVE ( 'NONE', #34174, #4709, #11100, .T. ) ;
#19989=VERTEX_POINT ( 'NONE', #12750 ) ;
#19994=CARTESIAN_POINT ( 'NONE',  ( -7.999999999999991118, -1.288204405367768053E-10, 8.517802783929960597 ) ) ;
#20000=CARTESIAN_POINT ( 'NONE',  ( 3.313708498984762496, -7.999999999999989342, 19.35530278432982954 ) ) ;
#20003=ORIENTED_EDGE ( 'NONE', *, *, #10674, .F. ) ;
#20028=CARTESIAN_POINT ( 'NONE',  ( -5.082755093536319713, 5.082755093536319713, 5.799052781871753659 ) ) ;
#20051=CARTESIAN_POINT ( 'NONE',  ( 7.188101187499992051, 8.802885111219154394E-16, 5.611552781871753659 ) ) ;
#20075=CARTESIAN_POINT ( 'NONE',  ( 7.999999999999992895, -3.313708498984756279, 1.486552779823364201 ) ) ;
#20082=CARTESIAN_POINT ( 'NONE',  ( -3.313708498984758943, -7.999999999999989342, 8.799052783920144449 ) ) ;
#20099=CARTESIAN_POINT ( 'NONE',  ( -3.317071493978880348, -8.008118988124989457, 10.29436528394063011 ) ) ;
#20105=CARTESIAN_POINT ( 'NONE',  ( -12.18025451098408318, 1.885907279315492735, 0.7279601535489274022 ) ) ;
#20108=CARTESIAN_POINT ( 'NONE',  ( -4.401442555609577197E-16, 7.188101187499992051, 1.111552781871753215 ) ) ;
#20121=CARTESIAN_POINT ( 'NONE',  ( -5.082755093536317936, -5.082755093536320601, 22.67405278187175455 ) ) ;
#20139=CARTESIAN_POINT ( 'NONE',  ( -4.898587196589407898E-16, 7.999999999999991118, 2.142802783920143117 ) ) ;
#20144=CARTESIAN_POINT ( 'NONE',  ( 2.977408999572650927, -7.188101187499990274, 23.33030278187175455 ) ) ;
#20151=ORIENTED_EDGE ( 'NONE', *, *, #72166, .F. ) ;
#20160=CARTESIAN_POINT ( 'NONE',  ( 7.999999999999991118, 1.639585202047151108E-05, 13.76780324778446385 ) ) ;
#20161=CARTESIAN_POINT ( 'NONE',  ( 3.313708498984762496, -7.999999999999989342, 7.299052779823365533 ) ) ;
#20165=LINE ( 'NONE', #43182, #26788 ) ;
#20166=CARTESIAN_POINT ( 'NONE',  ( -7.999999999999991118, 0.000000000000000000, 2.330302779823365089 ) ) ;
#20189=CARTESIAN_POINT ( 'NONE',  ( 5.662595241051936235, -5.662595241051934458, 25.57561528394063544 ) ) ;
#20197=ORIENTED_EDGE ( 'NONE', *, *, #10166, .F. ) ;
#20225=CARTESIAN_POINT ( 'NONE',  ( -7.188101187499992051, 0.000000000000000000, 2.986552781871751439 ) ) ;
#20227=CYLINDRICAL_SURFACE ( 'NONE', #58692, 7.999999999999991118 ) ;
#20249=CARTESIAN_POINT ( 'NONE',  ( 3.313708498984756279, 7.999999999999991118, 28.86155277982336642 ) ) ;
#20261=FACE_OUTER_BOUND ( 'NONE', #70560, .T. ) ;
#20264=CARTESIAN_POINT ( 'NONE',  ( 5.656854249492376141, -5.656854249492374365, 19.58030278392014978 ) ) ;
#20289=CARTESIAN_POINT ( 'NONE',  ( -2.977408999572647819, -7.188101187499990274, 19.76780278187175455 ) ) ;
#20299=CARTESIAN_POINT ( 'NONE',  ( -7.999999999999989342, -3.313708498984762496, 16.11155278392014267 ) ) ;
#20311=CARTESIAN_POINT ( 'NONE',  ( -7.188101187499991163, 2.977408999572646930, 17.89280278187175455 ) ) ;
#20316=CARTESIAN_POINT ( 'NONE',  ( -3.313708498984759387, -7.999999999999989342, 5.799052783920146226 ) ) ;
#20330=CARTESIAN_POINT ( 'NONE',  ( 5.656854249492374365, 5.656854249492375253, 22.95530278392014623 ) ) ;
#20336=CARTESIAN_POINT ( 'NONE',  ( 7.188101187499993827, -2.977408999572645598, 22.01780278187175810 ) ) ;
#20352=CARTESIAN_POINT ( 'NONE',  ( 5.656854249492376141, -5.656854249492374365, 7.392802779823366421 ) ) ;
#20369=CARTESIAN_POINT ( 'NONE',  ( -7.999999999999991118, 3.313708498984756723, 9.792802784329825982 ) ) ;
#20403=CARTESIAN_POINT ( 'NONE',  ( -2.977408999572648707, -7.188101187499990274, 6.267802781871754547 ) ) ;
#20415=CARTESIAN_POINT ( 'NONE',  ( -7.188101187499992051, 0.000000000000000000, 9.361552781871752771 ) ) ;
#20427=CARTESIAN_POINT ( 'NONE',  ( 1.320432766682872962E-15, -7.188101187499992051, 5.236552781871753659 ) ) ;
#20435=AXIS2_PLACEMENT_3D ( 'NONE', #16822, #34958, #12294 ) ;
#20444=CARTESIAN_POINT ( 'NONE',  ( 5.656854249492374365, 5.656854249492375253, 27.26780277982336642 ) ) ;
#20454=CARTESIAN_POINT ( 'NONE',  ( -12.18025451098408318, 1.885907279315492735, -0.5845398423542953470 ) ) ;
#20475=CARTESIAN_POINT ( 'NONE',  ( -5.082755093536317936, -5.082755093536320601, 3.174052781871751439 ) ) ;
#20477=EDGE_CURVE ( 'NONE', #71023, #72561, #37279, .T. ) ;
#20490=CARTESIAN_POINT ( 'NONE',  ( 5.082755093536320601, -5.082755093536318824, 24.54905278187175810 ) ) ;
#20509=CARTESIAN_POINT ( 'NONE',  ( 7.999999999999991118, 9.797174393178815797E-16, 24.26780278392014978 ) ) ;
#20516=CARTESIAN_POINT ( 'NONE',  ( 2.977408999572650927, -7.188101187499990274, 24.83030278187175455 ) ) ;
#20518=CARTESIAN_POINT ( 'NONE',  ( 7.999999999842164478, 5.025161467855852442E-05, 22.76780420562571905 ) ) ;
#20528=CARTESIAN_POINT ( 'NONE',  ( -5.656854249492375253, 5.656854249492375253, 17.33030278392014623 ) ) ;
#20537=CARTESIAN_POINT ( 'NONE',  ( -3.313708498984757167, 7.999999999999991118, 11.04905277982336642 ) ) ;
#20544=CARTESIAN_POINT ( 'NONE',  ( -5.656854249492375253, 5.656854249492375253, 2.142802779823364645 ) ) ;
#20566=ORIENTED_EDGE ( 'NONE', *, *, #4747, .F. ) ;
#20569=CARTESIAN_POINT ( 'NONE',  ( 8.008118988124993010, -3.317071493978877239, 25.66936528394063188 ) ) ;
#20574=CARTESIAN_POINT ( 'NONE',  ( -5.857492637593530560, -5.043103725236133705, -0.1555707967503436318 ) ) ;
#20582=CARTESIAN_POINT ( 'NONE',  ( 3.313708498984756279, 7.999999999999991118, 21.36155277982336642 ) ) ;
#20588=CARTESIAN_POINT ( 'NONE',  ( -5.656854249492375253, 5.656854249492375253, 14.14280277982336465 ) ) ;
#20602=CARTESIAN_POINT ( 'NONE',  ( 7.188101187499993827, -2.977408999572645598, 0.6428027818717528818 ) ) ;
#20606=FACE_OUTER_BOUND ( 'NONE', #861, .T. ) ;
#20631=CARTESIAN_POINT ( 'NONE',  ( -3.313708498984758943, -7.999999999999989342, 26.61155277982337708 ) ) ;
#20647=DIRECTION ( 'NONE',  ( 1.000000000000000000, 0.000000000000000000, 0.000000000000000000 ) ) ;
#20650=CARTESIAN_POINT ( 'NONE',  ( 7.999999999999991118, 3.313708498984757611, 16.86155278392014623 ) ) ;
#20653=CARTESIAN_POINT ( 'NONE',  ( 7.999999999999706901, -2.135495361439877059E-06, 10.76780272350167245 ) ) ;
#20670=CARTESIAN_POINT ( 'NONE',  ( 5.082755093536320601, -5.082755093536318824, 17.04905278187175810 ) ) ;
#20680=CARTESIAN_POINT ( 'NONE',  ( 7.999999999999991118, 9.797174393178815797E-16, 12.26780278392014623 ) ) ;
#20681=CARTESIAN_POINT ( 'NONE',  ( 7.999999999521839378, -8.746674989952265200E-05, 18.26780030933659305 ) ) ;
#20694=CARTESIAN_POINT ( 'NONE',  ( -7.188101187499992051, 0.000000000000000000, 20.98655278187175455 ) ) ;
#20712=CARTESIAN_POINT ( 'NONE',  ( 7.999999999999991118, 3.313708498984757611, 25.86155278392014623 ) ) ;
#20718=CARTESIAN_POINT ( 'NONE',  ( 2.977408999572650927, -7.188101187499990274, 15.83030278187175277 ) ) ;
#20734=CARTESIAN_POINT ( 'NONE',  ( 3.313708498984756279, 7.999999999999991118, 9.361552779823366421 ) ) ;
#20735=DIRECTION ( 'NONE',  ( 1.000000000000000000, 0.000000000000000000, 0.000000000000000000 ) ) ;
#20752=CARTESIAN_POINT ( 'NONE',  ( -5.656854249492373476, -5.656854249492376141, 13.07405278432982421 ) ) ;
#20783=CARTESIAN_POINT ( 'NONE',  ( 1.320432766682872962E-15, -7.188101187499992051, 4.861552781871752771 ) ) ;
#20798=CARTESIAN_POINT ( 'NONE',  ( 5.082755093536318824, 5.082755093536319713, 8.799052781871752771 ) ) ;
#20810=CARTESIAN_POINT ( 'NONE',  ( 7.188101187499992051, 2.977408999572647819, 4.205302781871752771 ) ) ;
#20827=CARTESIAN_POINT ( 'NONE',  ( -4.898587196589407898E-16, 7.999999999999991118, 24.45530277982336642 ) ) ;
#20832=CARTESIAN_POINT ( 'NONE',  ( 1.469576158976822172E-15, -7.999999999999991118, 25.39280278392014978 ) ) ;
#20838=CARTESIAN_POINT ( 'NONE',  ( -3.313708498984757167, 7.999999999999991118, 3.736552783920145338 ) ) ;
#20851=ORIENTED_EDGE ( 'NONE', *, *, #22674, .F. ) ;
#20859=CARTESIAN_POINT ( 'NONE',  ( -5.082755093536319713, 5.082755093536319713, 4.299052781871752771 ) ) ;
#20872=CARTESIAN_POINT ( 'NONE',  ( 7.188101187499992051, 8.802885111219154394E-16, 24.73655278187175810 ) ) ;
#20886=ORIENTED_EDGE ( 'NONE', *, *, #30782, .T. ) ;
#20896=CARTESIAN_POINT ( 'NONE',  ( -4.401442555609577197E-16, 7.188101187499992051, 23.98655278187175455 ) ) ;
#20908=CARTESIAN_POINT ( 'NONE',  ( 5.656854249492374365, 5.656854249492375253, 16.95530278392014978 ) ) ;
#20916=CARTESIAN_POINT ( 'NONE',  ( 7.999999999999992895, -3.313708498984756279, 8.986552779823366421 ) ) ;
#20944=CARTESIAN_POINT ( 'NONE',  ( 8.008118988124991233, 3.317071493978879015, 27.35686528394063544 ) ) ;
#20956=CARTESIAN_POINT ( 'NONE',  ( -3.313708498984757611, 7.999999999999991118, 21.54905277982336642 ) ) ;
#20972=DIRECTION ( 'NONE',  ( 0.000000000000000000, -0.9480053216942907479, -0.3182544737145173164 ) ) ;
#20978=CARTESIAN_POINT ( 'NONE',  ( 7.188101187499993827, -2.977408999572645598, 26.51780278187175455 ) ) ;
#20981=CARTESIAN_POINT ( 'NONE',  ( 5.656854249492374365, 5.656854249492375253, 15.45530278392014623 ) ) ;
#20996=EDGE_CURVE ( 'NONE', #60631, #73412, #47296, .T. ) ;
#21003=CARTESIAN_POINT ( 'NONE',  ( 1.320432766682872962E-15, -7.188101187499992051, 0.7365527818717527708 ) ) ;
#21020=CARTESIAN_POINT ( 'NONE',  ( 7.999999999999991118, 9.797174393178815797E-16, 12.08030277982336642 ) ) ;
#21023=CARTESIAN_POINT ( 'NONE',  ( 1.469576158976822172E-15, -7.999999999999991118, 17.89280278392014623 ) ) ;
#21045=CARTESIAN_POINT ( 'NONE',  ( 7.188101187499992051, 2.977408999572647819, 17.33030278187175455 ) ) ;
#21048=VERTEX_POINT ( 'NONE', #8442 ) ;
#21057=CARTESIAN_POINT ( 'NONE',  ( -7.999999999999991118, 3.313708498984756723, 8.424052783920146226 ) ) ;
#21066=( BOUNDED_CURVE ( )  B_SPLINE_CURVE ( 2, ( #33174, #43717, #26348, #9773, #10884, #61818, #10511, #4116, #67108 ),
 .UNSPECIFIED., .F., .F. ) 
 B_SPLINE_CURVE_WITH_KNOTS ( ( 3, 2, 2, 2, 3 ),
 ( 0.1323655657721681533, 0.1389837872735831814, 0.1456020628580432796, 0.1522203384425033779, 0.1588385999027599471 ),
 .UNSPECIFIED. ) 
 CURVE ( )  GEOMETRIC_REPRESENTATION_ITEM ( )  RATIONAL_B_SPLINE_CURVE ( ( 0.9999987559318189723, 0.9238801545504604640, 1.000000000000000000, 0.9238795325112867385, 1.000000000000000000, 0.9238795325112867385, 1.000000000000000000, 0.9238796949616049359, 0.9999996751000569395 ) ) 
 REPRESENTATION_ITEM ( '' )  );
#21067=VERTEX_POINT ( 'NONE', #68028 ) ;
#21069=CARTESIAN_POINT ( 'NONE',  ( -5.082755093536319713, 5.082755093536319713, 14.79905278187175455 ) ) ;
#21076=CARTESIAN_POINT ( 'NONE',  ( 3.313708498984762496, -7.999999999999989342, 17.79905277982336997 ) ) ;
#21096=CARTESIAN_POINT ( 'NONE',  ( 7.188101187499991163, 2.977408999572648707, 13.20530278187175277 ) ) ;
#21103=ORIENTED_EDGE ( 'NONE', *, *, #73063, .T. ) ;
#21113=CARTESIAN_POINT ( 'NONE',  ( 7.999999999999991118, 3.313708498984757611, 9.174052779823364645 ) ) ;
#21127=CARTESIAN_POINT ( 'NONE',  ( 5.656854249492376141, -5.656854249492374365, 8.949052784329824206 ) ) ;
#21156=CARTESIAN_POINT ( 'NONE',  ( 1.320432766682872962E-15, -7.188101187499992051, 7.861552781871751883 ) ) ;
#21169=CARTESIAN_POINT ( 'NONE',  ( -5.082755093536319713, 5.082755093536319713, 12.17405278187175277 ) ) ;
#21183=CARTESIAN_POINT ( 'NONE',  ( 2.977408999572650927, -7.188101187499990274, 2.330302781871754991 ) ) ;
#21199=CARTESIAN_POINT ( 'NONE',  ( 1.469576158976822172E-15, -7.999999999999991118, 28.20530277982336642 ) ) ;
#21210=LINE ( 'NONE', #25736, #12214 ) ;
#21211=CARTESIAN_POINT ( 'NONE',  ( 7.999999999999991118, 3.313708498984757611, 0.3615527839201451710 ) ) ;
#21223=CARTESIAN_POINT ( 'NONE',  ( -7.999999999961167951, -1.666173683171983354E-05, 1.018425797410095646 ) ) ;
#21234=CARTESIAN_POINT ( 'NONE',  ( 2.977408999572650927, -7.188101187499990274, 1.955302781871753881 ) ) ;
#21246=CARTESIAN_POINT ( 'NONE',  ( -7.999999999999989342, -3.313708498984762496, 9.924052779823364645 ) ) ;
#21247=CARTESIAN_POINT ( 'NONE',  ( -7.188101187499990274, -2.977408999572651371, 24.08030278187175455 ) ) ;
#21269=CARTESIAN_POINT ( 'NONE',  ( 5.082755093536320601, -5.082755093536318824, 24.92405278187175810 ) ) ;
#21279=CARTESIAN_POINT ( 'NONE',  ( 7.999999999999991118, 9.797174393178815797E-16, 21.08030277982336642 ) ) ;
#21288=CARTESIAN_POINT ( 'NONE',  ( 7.999999999999991118, 9.797174393178815797E-16, 10.58030277982336465 ) ) ;
#21290=CARTESIAN_POINT ( 'NONE',  ( -7.999999999995399236, -5.826008446853342637E-06, 20.51801720710344767 ) ) ;
#21317=ORIENTED_EDGE ( 'NONE', *, *, #13983, .F. ) ;
#21319=CARTESIAN_POINT ( 'NONE',  ( -8.008118988124989457, -3.317071493978883900, 20.60686528394063188 ) ) ;
#21351=CARTESIAN_POINT ( 'NONE',  ( -7.188101187499990274, -2.977408999572651371, 22.95530278187175455 ) ) ;
#21357=FACE_OUTER_BOUND ( 'NONE', #35036, .T. ) ;
#21375=CARTESIAN_POINT ( 'NONE',  ( -7.999999999999991118, 3.313708498984756723, 29.23655277982336642 ) ) ;
#21395=CARTESIAN_POINT ( 'NONE',  ( -3.313708498984758943, -7.999999999999989342, 19.29905278392014978 ) ) ;
#21417=CARTESIAN_POINT ( 'NONE',  ( -2.977408999572647819, -7.188101187499990274, 15.26780278187175455 ) ) ;
#21441=CARTESIAN_POINT ( 'NONE',  ( 7.188101187499991163, 2.977408999572648707, 14.33030278187175277 ) ) ;
#21466=CARTESIAN_POINT ( 'NONE',  ( -4.401442555609577197E-16, 7.188101187499992051, 17.98655278187175810 ) ) ;
#21483=CARTESIAN_POINT ( 'NONE',  ( -3.313708498984758943, -7.999999999999989342, 10.11155277982336820 ) ) ;
#21485=CARTESIAN_POINT ( 'NONE',  ( -5.656854249492373476, -5.656854249492376141, 4.205302783920145338 ) ) ;
#21500=CARTESIAN_POINT ( 'NONE',  ( -3.313708498984757167, 7.999999999999991118, 11.10530278432982065 ) ) ;
#21530=CARTESIAN_POINT ( 'NONE',  ( 1.320432766682872962E-15, -7.188101187499992051, 1.861552781871753881 ) ) ;
#21531=ORIENTED_EDGE ( 'NONE', *, *, #20477, .T. ) ;
#21542=CARTESIAN_POINT ( 'NONE',  ( 7.188101187499992051, 8.802885111219154394E-16, 7.111552781871754547 ) ) ;
#21555=DIRECTION ( 'NONE',  ( -1.000000000000000000, 0.000000000000000000, 0.000000000000000000 ) ) ;
#21570=CARTESIAN_POINT ( 'NONE',  ( -7.999999999999991118, 3.313708498984756723, 27.73655277982336642 ) ) ;
#21582=CARTESIAN_POINT ( 'NONE',  ( 7.999999999999991118, 3.313708498984757611, 3.361552783920145338 ) ) ;
#21602=CARTESIAN_POINT ( 'NONE',  ( -5.447321192899549303, -4.689935021205116961, 0.1569292013794422458 ) ) ;
#21616=CARTESIAN_POINT ( 'NONE',  ( -5.082755093536317936, -5.082755093536320601, 19.67405278187175455 ) ) ;
#21617=ORIENTED_EDGE ( 'NONE', *, *, #39191, .T. ) ;
#21641=CARTESIAN_POINT ( 'NONE',  ( -7.188101187499992051, 0.000000000000000000, 18.36155278187175455 ) ) ;
#21643=CARTESIAN_POINT ( 'NONE',  ( 7.999999999999920064, -1.061780717098090627E-06, 7.767802753882760314 ) ) ;
#21659=CARTESIAN_POINT ( 'NONE',  ( 5.656854249492374365, 5.656854249492375253, 6.267802779823364645 ) ) ;
#21660=CARTESIAN_POINT ( 'NONE',  ( -3.313708498984759387, -7.999999999999989342, 20.79905278392014978 ) ) ;
#21686=CARTESIAN_POINT ( 'NONE',  ( -5.662595241051933570, -5.662595241051936235, 19.20061528394063188 ) ) ;
#21719=CARTESIAN_POINT ( 'NONE',  ( 7.188101187499991163, 2.977408999572648707, 20.70530278187175455 ) ) ;
#21721=CARTESIAN_POINT ( 'NONE',  ( -4.898587196589407898E-16, 7.999999999999991118, 15.64280278392014800 ) ) ;
#21726=CARTESIAN_POINT ( 'NONE',  ( 0.000000000000000000, 0.000000000000000000, 30.00000000000000000 ) ) ;
#21736=EDGE_CURVE ( 'NONE', #30305, #29130, #45419, .T. ) ;
#21745=CARTESIAN_POINT ( 'NONE',  ( 7.999999999999991118, 3.313708498984757611, 24.17405277982336642 ) ) ;
#21752=CARTESIAN_POINT ( 'NONE',  ( -3.313708498984759387, -7.999999999999989342, 14.61155277982336465 ) ) ;
#21761=CARTESIAN_POINT ( 'NONE',  ( -7.999999999999960032, 3.313708498984789141, 23.23655277982336642 ) ) ;
#21764=CARTESIAN_POINT ( 'NONE',  ( -7.999999999999989342, -3.313708498984762496, 14.61155278392014800 ) ) ;
#21783=CARTESIAN_POINT ( 'NONE',  ( 5.082755093536318824, 5.082755093536319713, 15.92405278187175632 ) ) ;
#21805=CARTESIAN_POINT ( 'NONE',  ( 2.977408999572646486, 7.188101187499991163, 10.01780278187175632 ) ) ;
#21830=CARTESIAN_POINT ( 'NONE',  ( 5.082755093536320601, -5.082755093536318824, 15.92405278187175632 ) ) ;
#21848=CARTESIAN_POINT ( 'NONE',  ( -7.999999999999991118, -9.344071862984236532, 28.28216120211630624 ) ) ;
#21866=CARTESIAN_POINT ( 'NONE',  ( -7.999999999999989342, -3.313708498984762496, 12.98030278432982243 ) ) ;
#21869=CARTESIAN_POINT ( 'NONE',  ( -7.999999999999991118, 0.000000000000000000, 5.330302779823363757 ) ) ;
#21901=CARTESIAN_POINT ( 'NONE',  ( 7.999999999999991118, 9.797174393178815797E-16, 19.58030277982336642 ) ) ;
#21909=CARTESIAN_POINT ( 'NONE',  ( 1.320432766682872962E-15, -7.188101187499992051, 5.236552781871753659 ) ) ;
#21923=CARTESIAN_POINT ( 'NONE',  ( 7.188101187499993827, -2.977408999572645598, 1.017802781871752993 ) ) ;
#21939=CARTESIAN_POINT ( 'NONE',  ( -5.656854249492373476, -5.656854249492376141, 26.51780277982336997 ) ) ;
#21953=CARTESIAN_POINT ( 'NONE',  ( -3.313708498984758943, -7.999999999999989342, 1.299052783920146448 ) ) ;
#21959=AXIS2_PLACEMENT_3D ( 'NONE', #52017, #36147, #18796 ) ;
#21987=DIRECTION ( 'NONE',  ( -0.000000000000000000, -0.000000000000000000, 1.000000000000000000 ) ) ;
#21990=CARTESIAN_POINT ( 'NONE',  ( -2.977408999572647819, 7.188101187499991163, 19.20530278187175810 ) ) ;
#22005=CARTESIAN_POINT ( 'NONE',  ( -3.313708498984757611, 7.999999999999991118, 8.049052779823362869 ) ) ;
#22014=CARTESIAN_POINT ( 'NONE',  ( 7.188101187499992051, 8.802885111219154394E-16, 17.61155278187175810 ) ) ;
#22031=CARTESIAN_POINT ( 'NONE',  ( -7.999999999999989342, -3.313708498984762496, 5.424052779823364645 ) ) ;
#22033=ORIENTED_EDGE ( 'NONE', *, *, #47309, .F. ) ;
#22043=CARTESIAN_POINT ( 'NONE',  ( 7.588356073042825223, -2.561989435426024198, 0.000000000000000000 ) ) ;
#22056=CARTESIAN_POINT ( 'NONE',  ( -3.317071493978880348, -8.008118988124989457, 22.29436528394063188 ) ) ;
#22063=ADVANCED_FACE ( 'NONE', ( #50402 ), #61727, .F. ) ;
#22072=EDGE_CURVE ( 'NONE', #3266, #37555, #29568, .T. ) ;
#22077=ADVANCED_FACE ( 'NONE', ( #67012 ), #20227, .F. ) ;
#22091=CARTESIAN_POINT ( 'NONE',  ( 5.082755093536318824, 5.082755093536319713, 22.29905278187175455 ) ) ;
#22092=CARTESIAN_POINT ( 'NONE',  ( 0.000000000000000000, 0.000000000000000000, 30.00000000000000000 ) ) ;
#22116=CARTESIAN_POINT ( 'NONE',  ( 5.656854249492376141, -5.656854249492374365, 20.89280277982336642 ) ) ;
#22117=DIRECTION ( 'NONE',  ( -0.000000000000000000, -0.000000000000000000, 1.000000000000000000 ) ) ;
#22133=CARTESIAN_POINT ( 'NONE',  ( -3.313708498984757167, 7.999999999999991118, 12.73655278392014623 ) ) ;
#22181=CARTESIAN_POINT ( 'NONE',  ( 2.977408999572646486, 7.188101187499991163, 14.51780278187175455 ) ) ;
#22205=CARTESIAN_POINT ( 'NONE',  ( -2.977408999572647819, 7.188101187499991163, 13.58030278187175277 ) ) ;
#22210=CARTESIAN_POINT ( 'NONE',  ( 7.999999999999992895, -3.313708498984756279, 7.674052783920143561 ) ) ;
#22219=CARTESIAN_POINT ( 'NONE',  ( -7.999999999999989342, -3.313708498984762496, 2.424052779823365533 ) ) ;
#22220=CARTESIAN_POINT ( 'NONE',  ( 7.999969786815256612, -3.313738712169494338, 4.674051575081102250 ) ) ;
#22236=CARTESIAN_POINT ( 'NONE',  ( -7.999999999999991118, 0.000000000000000000, 6.886552784329822430 ) ) ;
#22265=CARTESIAN_POINT ( 'NONE',  ( 2.977408999572650927, -7.188101187499990274, 3.455302781871751439 ) ) ;
#22280=CARTESIAN_POINT ( 'NONE',  ( -7.188101187499990274, -2.977408999572651371, 3.455302781871751439 ) ) ;
#22296=CARTESIAN_POINT ( 'NONE',  ( -7.999999999999991118, 0.000000000000000000, 29.33030277982336642 ) ) ;
#22306=CARTESIAN_POINT ( 'NONE',  ( -7.999999999999991118, 3.313708498984756723, 23.23655277982336642 ) ) ;
#22317=CARTESIAN_POINT ( 'NONE',  ( -3.313708498984758943, -7.999999999999989342, 25.16780278432982954 ) ) ;
#22320=VECTOR ( 'NONE', #72254, 1000.000000000000000 ) ;
#22325=CARTESIAN_POINT ( 'NONE',  ( -4.898587196589407898E-16, 7.999999999999991118, 24.45530277982336642 ) ) ;
#22349=CARTESIAN_POINT ( 'NONE',  ( 7.188101187499993827, -2.977408999572645598, 20.14280278187176165 ) ) ;
#22374=CARTESIAN_POINT ( 'NONE',  ( 7.188101187499992051, 2.977408999572647819, 14.70530278187175455 ) ) ;
#22393=CARTESIAN_POINT ( 'NONE',  ( 3.313708498984756279, 7.999999999999991118, 3.361552779823362425 ) ) ;
#22397=CARTESIAN_POINT ( 'NONE',  ( -4.898587196589407898E-16, 7.999999999999991118, 10.95530277982336642 ) ) ;
#22398=CARTESIAN_POINT ( 'NONE',  ( 5.656854249492376141, -5.656854249492374365, 15.08030278392014623 ) ) ;
#22409=CARTESIAN_POINT ( 'NONE',  ( 7.999999999999998224, -0.7555120169168165756, 0.000000000000000000 ) ) ;
#22425=CARTESIAN_POINT ( 'NONE',  ( -5.662595241051935346, 5.662595241051935346, 20.32561528394062833 ) ) ;
#22444=CARTESIAN_POINT ( 'NONE',  ( -7.999999999999989342, -3.313708498984762496, 5.611552783920146226 ) ) ;
#22454=CARTESIAN_POINT ( 'NONE',  ( -6.785933778205718525, -4.286164213032431114, -0.000000000000000000 ) ) ;
#22457=CARTESIAN_POINT ( 'NONE',  ( -2.977408999572647819, 7.188101187499991163, 24.08030278187175455 ) ) ;
#22473=EDGE_CURVE ( 'NONE', #64740, #27089, #16538, .T. ) ;
#22476=CARTESIAN_POINT ( 'NONE',  ( -6.062687379811042554, -5.219768740853823807, 2.519839246067225784E-12 ) ) ;
#22482=CARTESIAN_POINT ( 'NONE',  ( 5.656854249492374365, 5.656854249492375253, 18.26780277982336642 ) ) ;
#22493=ORIENTED_EDGE ( 'NONE', *, *, #21736, .F. ) ;
#22501=CARTESIAN_POINT ( 'NONE',  ( -7.999999999999991118, 3.313708498984756723, 12.92405278392014800 ) ) ;
#22549=SHAPE_DEFINITION_REPRESENTATION ( #56584, #48857 ) ;
#22550=ORIENTED_EDGE ( 'NONE', *, *, #28852, .T. ) ;
#22553=CARTESIAN_POINT ( 'NONE',  ( -4.401442555609577197E-16, 7.188101187499992051, 10.11155278187175455 ) ) ;
#22554=ORIENTED_EDGE ( 'NONE', *, *, #27003, .T. ) ;
#22579=CARTESIAN_POINT ( 'NONE',  ( 1.320432766682872962E-15, -7.188101187499992051, 11.23655278187175455 ) ) ;
#22582=CARTESIAN_POINT ( 'NONE',  ( 3.313708498984756279, 7.999999999999991118, 1.917802784329821320 ) ) ;
#22594=CARTESIAN_POINT ( 'NONE',  ( 7.999999999999991118, 9.797174393178815797E-16, 3.080302779823361981 ) ) ;
#22595=CARTESIAN_POINT ( 'NONE',  ( 0.000000000000000000, 116.0729912458811839, 42.10166426739785095 ) ) ;
#22610=CARTESIAN_POINT ( 'NONE',  ( 7.999999999999991118, 3.313708498984757611, 6.230302784329825982 ) ) ;
#22615=VERTEX_POINT ( 'NONE', #36397 ) ;
#22618=CARTESIAN_POINT ( 'NONE',  ( -4.401442555609577197E-16, 7.188101187499992051, 26.61155278187175455 ) ) ;
#22638=CARTESIAN_POINT ( 'NONE',  ( 2.977408999572650927, -7.188101187499990274, 1.955302781871753881 ) ) ;
#22652=CARTESIAN_POINT ( 'NONE',  ( -7.188101187499990274, -2.977408999572651371, 4.955302781871753659 ) ) ;
#22662=CARTESIAN_POINT ( 'NONE',  ( 5.082755093536318824, 5.082755093536319713, 26.79905278187175455 ) ) ;
#22674=EDGE_CURVE ( 'NONE', #6157, #9404, #58317, .T. ) ;
#22682=CARTESIAN_POINT ( 'NONE',  ( 3.313708498984756279, 7.999999999999991118, 18.36155277982337353 ) ) ;
#22696=CARTESIAN_POINT ( 'NONE',  ( -3.313708498984758943, -7.999999999999989342, 23.66780278432982954 ) ) ;
#22702=VECTOR ( 'NONE', #29391, 1000.000000000000000 ) ;
#22729=CARTESIAN_POINT ( 'NONE',  ( -7.188101187499992051, 0.000000000000000000, 20.98655278187175455 ) ) ;
#22750=CARTESIAN_POINT ( 'NONE',  ( 5.082755093536318824, 5.082755093536319713, 16.29905278187175455 ) ) ;
#22771=CARTESIAN_POINT ( 'NONE',  ( 1.469576158976822172E-15, -7.999999999999991118, 5.705302779823364645 ) ) ;
#22789=EDGE_CURVE ( 'NONE', #46714, #22871, #55125, .T. ) ;
#22800=CARTESIAN_POINT ( 'NONE',  ( -5.662595241051935346, 5.662595241051935346, 15.82561528394063188 ) ) ;
#22814=CYLINDRICAL_SURFACE ( 'NONE', #14894, 7.999999999999991118 ) ;
#22823=CARTESIAN_POINT ( 'NONE',  ( -5.656854249492373476, -5.656854249492376141, 8.705302783920146226 ) ) ;
#22836=( BOUNDED_CURVE ( )  B_SPLINE_CURVE ( 2, ( #68059, #16349, #72601, #39387, #20528, #62386, #43541, #3570, #20908, #43928, #66938 ),
 .UNSPECIFIED., .F., .F. ) 
 B_SPLINE_CURVE_WITH_KNOTS ( ( 3, 2, 2, 2, 2, 3 ),
 ( 0.3706233993366209178, 0.3706234327295814812, 0.3772417083140383043, 0.3838599838984951274, 0.3904782594829518949, 0.3970965164372073364 ),
 .UNSPECIFIED. ) 
 CURVE ( )  GEOMETRIC_REPRESENTATION_ITEM ( )  RATIONAL_B_SPLINE_CURVE ( ( 0.9999992318618620146, 0.9999996159289931130, 1.000000000000000000, 0.9238795325112867385, 1.000000000000000000, 0.9238795325112867385, 1.000000000000000000, 0.9238795325112867385, 1.000000000000000000, 0.9238797467875916603, 0.9999995714485965248 ) ) 
 REPRESENTATION_ITEM ( '' )  );
#22839=CARTESIAN_POINT ( 'NONE',  ( 1.320432766682872962E-15, -7.188101187499992051, 17.23655278187175810 ) ) ;
#22867=CARTESIAN_POINT ( 'NONE',  ( 7.999999999999992895, -3.313708498984756279, 22.48655277982336287 ) ) ;
#22871=VERTEX_POINT ( 'NONE', #37888 ) ;
#22885=CARTESIAN_POINT ( 'NONE',  ( -5.656854249492375253, 5.656854249492375253, 23.14280277982336642 ) ) ;
#22887=CARTESIAN_POINT ( 'NONE',  ( -5.656854249492373476, -5.656854249492376141, 10.20530278392014623 ) ) ;
#22937=ORIENTED_EDGE ( 'NONE', *, *, #38478, .T. ) ;
#22939=CARTESIAN_POINT ( 'NONE',  ( -7.188101187499990274, -2.977408999572651371, 6.080302781871753659 ) ) ;
#22967=CARTESIAN_POINT ( 'NONE',  ( -5.082755093536317936, -5.082755093536320601, 8.049052781871752771 ) ) ;
#22971=CARTESIAN_POINT ( 'NONE',  ( -5.656854249492375253, 5.656854249492375253, 3.699052784329822874 ) ) ;
#22981=CARTESIAN_POINT ( 'NONE',  ( -5.656854249492375253, 5.656854249492375253, 5.142802779823363757 ) ) ;
#22996=CARTESIAN_POINT ( 'NONE',  ( 3.313708498984756279, 7.999999999999991118, 6.417802784329822430 ) ) ;
#22997=CARTESIAN_POINT ( 'NONE',  ( 7.999999999999991118, 9.797174393178815797E-16, 4.580302779823363757 ) ) ;
#23003=CARTESIAN_POINT ( 'NONE',  ( 2.977408999572650927, -7.188101187499990274, 25.95530278187175455 ) ) ;
#23015=CARTESIAN_POINT ( 'NONE',  ( 3.313708498984756279, 7.999999999999991118, 21.54905278392014623 ) ) ;
#23022=DIRECTION ( 'NONE',  ( -0.000000000000000000, -0.000000000000000000, 1.000000000000000000 ) ) ;
#23024=CARTESIAN_POINT ( 'NONE',  ( -4.401442555609577197E-16, 7.188101187499992051, 28.11155278187175455 ) ) ;
#23036=CARTESIAN_POINT ( 'NONE',  ( 5.082755093536320601, -5.082755093536318824, 3.924052781871752327 ) ) ;
#23042=CARTESIAN_POINT ( 'NONE',  ( 3.499857865026532622, -7.193933550196781823, 0.0006324257780546024528 ) ) ;
#23052=CARTESIAN_POINT ( 'NONE',  ( 3.313708498984756279, 7.999999999999991118, 28.86155277982336642 ) ) ;
#23054=ORIENTED_EDGE ( 'NONE', *, *, #27929, .T. ) ;
#23063=CARTESIAN_POINT ( 'NONE',  ( 5.656854249492374365, 5.656854249492375253, 21.26780277982336642 ) ) ;
#23076=CARTESIAN_POINT ( 'NONE',  ( -7.999999999999989342, -3.313708498984762496, 26.48030278432982954 ) ) ;
#23108=CARTESIAN_POINT ( 'NONE',  ( 7.188101187499991163, 2.977408999572648707, 21.83030278187175810 ) ) ;
#23132=CARTESIAN_POINT ( 'NONE',  ( 7.188101187499992051, 2.977408999572647819, 17.70530278187175455 ) ) ;
#23152=CARTESIAN_POINT ( 'NONE',  ( 7.999999999999991118, 9.797174393178815797E-16, 4.580302779823363757 ) ) ;
#23181=CARTESIAN_POINT ( 'NONE',  ( 1.471067592899761672E-15, -8.008118988124991233, 14.88811528394063011 ) ) ;
#23188=CARTESIAN_POINT ( 'NONE',  ( 1.320432766682872962E-15, -7.188101187499992051, 13.86155278187175455 ) ) ;
#23202=CARTESIAN_POINT ( 'NONE',  ( -4.898587196589407898E-16, 7.999999999999991118, 8.142802783920144449 ) ) ;
#23218=CARTESIAN_POINT ( 'NONE',  ( -7.188101187499991163, 2.977408999572646930, 15.26780278187175455 ) ) ;
#23236=CARTESIAN_POINT ( 'NONE',  ( 2.028713400070581319, -7.761291288302830438, -0.000000000000000000 ) ) ;
#23243=CARTESIAN_POINT ( 'NONE',  ( 7.999999999999991118, 9.797174393178815797E-16, 21.08030277982336642 ) ) ;
#23244=CARTESIAN_POINT ( 'NONE',  ( 3.486804365889302648, -7.201712369346796372, 3.176373552203626272E-17 ) ) ;
#23261=CARTESIAN_POINT ( 'NONE',  ( 3.313708498984756279, 7.999999999999991118, 15.54905278392014623 ) ) ;
#23273=ORIENTED_EDGE ( 'NONE', *, *, #53513, .T. ) ;
#23274=CARTESIAN_POINT ( 'NONE',  ( 5.656854249492376141, -5.656854249492374365, 26.89280277982336642 ) ) ;
#23282=( BOUNDED_CURVE ( )  B_SPLINE_CURVE ( 2, ( #66989, #71889, #31916, #20956, #32295, #20582, #33060, #73393, #56058 ),
 .UNSPECIFIED., .F., .F. ) 
 B_SPLINE_CURVE_WITH_KNOTS ( ( 3, 2, 2, 2, 3 ),
 ( 0.2631578947368420907, 0.2697368421052631637, 0.2763157894736841813, 0.2828947368421051989, 0.2894736842105262720 ),
 .UNSPECIFIED. ) 
 CURVE ( )  GEOMETRIC_REPRESENTATION_ITEM ( )  RATIONAL_B_SPLINE_CURVE ( ( 1.000000000000000000, 0.9238795325112867385, 1.000000000000000000, 0.9238795325112867385, 1.000000000000000000, 0.9238795325112867385, 1.000000000000000000, 0.9238795325112874046, 0.9999999999999993339 ) ) 
 REPRESENTATION_ITEM ( '' )  );
#23295=VECTOR ( 'NONE', #11909, 1000.000000000000000 ) ;
#23308=CARTESIAN_POINT ( 'NONE',  ( -7.188101187499992051, 0.000000000000000000, 4.486552781871752771 ) ) ;
#23333=CARTESIAN_POINT ( 'NONE',  ( 7.188101187499992051, 8.802885111219154394E-16, 8.611552781871752771 ) ) ;
#23337=CARTESIAN_POINT ( 'NONE',  ( 7.999999999999992895, -3.313708498984756279, 1.542802784329821097 ) ) ;
#23340=AXIS2_PLACEMENT_3D ( 'NONE', #2829, #71105, #54150 ) ;
#23348=CARTESIAN_POINT ( 'NONE',  ( 7.999999999999991118, 3.313708498984757611, 1.674052779823364423 ) ) ;
#23361=CARTESIAN_POINT ( 'NONE',  ( 7.999999999999991118, 9.797174393178815797E-16, 6.136552784329825094 ) ) ;
#23370=CARTESIAN_POINT ( 'NONE',  ( -2.977408999572647819, -7.188101187499990274, 24.26780278187175810 ) ) ;
#23381=CARTESIAN_POINT ( 'NONE',  ( 3.313708498984756279, 7.999999999999991118, 20.04905278392014978 ) ) ;
#23391=CARTESIAN_POINT ( 'NONE',  ( 7.188101187499992051, 8.802885111219154394E-16, 23.23655278187175455 ) ) ;
#23392=ORIENTED_EDGE ( 'NONE', *, *, #63680, .F. ) ;
#23409=CARTESIAN_POINT ( 'NONE',  ( 5.662595241051936235, -5.662595241051934458, 6.075615283940630995 ) ) ;
#23416=CARTESIAN_POINT ( 'NONE',  ( -7.188101187499992051, 0.000000000000000000, 28.86155278187175810 ) ) ;
#23433=CARTESIAN_POINT ( 'NONE',  ( 5.656854249492374365, 5.656854249492375253, 24.26780277982336642 ) ) ;
#23442=CARTESIAN_POINT ( 'NONE',  ( -7.999999999953861796, 1.809871347124574913E-05, 10.01712378708029938 ) ) ;
#23446=CARTESIAN_POINT ( 'NONE',  ( 7.999999999999991118, 3.313708498984757611, 24.23030278432982598 ) ) ;
#23457=ORIENTED_EDGE ( 'NONE', *, *, #36836, .F. ) ;
#23479=CARTESIAN_POINT ( 'NONE',  ( 2.977408999572650927, -7.188101187499990274, 10.95530278187175455 ) ) ;
#23497=CARTESIAN_POINT ( 'NONE',  ( -7.999999999999991118, 3.313708498984757167, 26.42405278392014978 ) ) ;
#23502=CARTESIAN_POINT ( 'NONE',  ( 5.082755093536318824, 5.082755093536319713, 10.29905278187175455 ) ) ;
#23528=CARTESIAN_POINT ( 'NONE',  ( 3.313708498984756279, 7.999999999999991118, 10.86155277982336820 ) ) ;
#23541=DIRECTION ( 'NONE',  ( 1.000000000000000000, 0.000000000000000000, 0.000000000000000000 ) ) ;
#23551=CARTESIAN_POINT ( 'NONE',  ( -8.008118988124991233, 0.000000000000000000, 16.01311528394063188 ) ) ;
#23558=CARTESIAN_POINT ( 'NONE',  ( -7.188101187499990274, -2.977408999572651815, 7.580302781871751883 ) ) ;
#23572=CARTESIAN_POINT ( 'NONE',  ( -5.656854249492375253, 5.656854249492375253, 6.830302783920143561 ) ) ;
#23586=CARTESIAN_POINT ( 'NONE',  ( 5.082755093536320601, -5.082755093536318824, 18.92405278187175455 ) ) ;
#23590=( BOUNDED_CURVE ( )  B_SPLINE_CURVE ( 2, ( #61498, #14337, #32845, #37369, #8696, #71312, #72054, #65657, #60750 ),
 .UNSPECIFIED., .F., .F. ) 
 B_SPLINE_CURVE_WITH_KNOTS ( ( 3, 2, 2, 2, 3 ),
 ( 0.4473684210526316929, 0.4539473684210527660, 0.4605263157894737835, 0.4671052631578948011, 0.4736842105263158187 ),
 .UNSPECIFIED. ) 
 CURVE ( )  GEOMETRIC_REPRESENTATION_ITEM ( )  RATIONAL_B_SPLINE_CURVE ( ( 0.9999999999999986677, 0.9238795325112880708, 1.000000000000000000, 0.9238795325112867385, 1.000000000000000000, 0.9238795325112867385, 1.000000000000000000, 0.9238795325112860723, 1.000000000000000666 ) ) 
 REPRESENTATION_ITEM ( '' )  );
#23595=CARTESIAN_POINT ( 'NONE',  ( 7.999999999999991118, 9.797174393178815797E-16, 4.580302779823363757 ) ) ;
#23601=CARTESIAN_POINT ( 'NONE',  ( 7.999999999999991118, 9.797174393178815797E-16, 27.08030277982336642 ) ) ;
#23606=CARTESIAN_POINT ( 'NONE',  ( 2.648895341738178200, -7.552205831922027990, -0.000000000000000000 ) ) ;
#23613=CARTESIAN_POINT ( 'NONE',  ( 3.313708498984756279, 7.999999999999991118, 19.86155277982336997 ) ) ;
#23635=CARTESIAN_POINT ( 'NONE',  ( 3.313708498984762496, -7.999999999999989342, 4.486552783920144449 ) ) ;
#23682=CARTESIAN_POINT ( 'NONE',  ( 5.082755093536320601, -5.082755093536318824, 5.049052781871752771 ) ) ;
#23706=CARTESIAN_POINT ( 'NONE',  ( -7.188101187499990274, -2.977408999572651371, 10.95530278187175455 ) ) ;
#23709=CARTESIAN_POINT ( 'NONE',  ( 1.469576158976822172E-15, -7.999999999999991118, -0.2384472156701772649 ) ) ;
#23719=CARTESIAN_POINT ( 'NONE',  ( 5.656854249492376141, -5.656854249492374365, 25.58030278392014978 ) ) ;
#23755=CARTESIAN_POINT ( 'NONE',  ( -4.898587196589407898E-16, 7.999999999999991118, 18.64280278392014623 ) ) ;
#23764=CARTESIAN_POINT ( 'NONE',  ( -7.188101187499992051, 0.000000000000000000, 23.98655278187175455 ) ) ;
#23784=CARTESIAN_POINT ( 'NONE',  ( 8.008118988124993010, -3.317071493978877239, 4.669365283940630107 ) ) ;
#23791=CARTESIAN_POINT ( 'NONE',  ( 1.320432766682872962E-15, -7.188101187499992051, 27.73655278187175455 ) ) ;
#23809=CARTESIAN_POINT ( 'NONE',  ( 5.656854249492374365, 5.656854249492375253, 16.76780277982336287 ) ) ;
#23823=CARTESIAN_POINT ( 'NONE',  ( -7.999999999999991118, 0.000000000000000000, 24.88655278432982598 ) ) ;
#23846=CARTESIAN_POINT ( 'NONE',  ( 3.313708498984756279, 7.999999999999991118, 12.54905278392014800 ) ) ;
#23852=VECTOR ( 'NONE', #27043, 1000.000000000000114 ) ;
#23855=CARTESIAN_POINT ( 'NONE',  ( -4.401442555609577197E-16, 7.188101187499992051, 11.61155278187175632 ) ) ;
#23879=CARTESIAN_POINT ( 'NONE',  ( -4.401442555609577197E-16, 7.188101187499992051, 10.48655278187175455 ) ) ;
#23899=CARTESIAN_POINT ( 'NONE',  ( -7.999999999999015010, 2.678670460604446806E-06, 11.51770387648012317 ) ) ;
#23923=CARTESIAN_POINT ( 'NONE',  ( 3.317071493978883456, -8.008118988124989457, 16.48186528394062833 ) ) ;
#23928=CARTESIAN_POINT ( 'NONE',  ( 7.188101187499992051, 8.802885111219154394E-16, 6.736552781871754547 ) ) ;
#23933=UNCERTAINTY_MEASURE_WITH_UNIT (LENGTH_MEASURE( 1.000000000000000082E-05 ), #53643, 'distance_accuracy_value', 'NONE');
#23943=CARTESIAN_POINT ( 'NONE',  ( -5.656854249492373476, -5.656854249492376141, 4.205302783920145338 ) ) ;
#23958=CARTESIAN_POINT ( 'NONE',  ( 7.188101187499993827, -2.977408999572645598, 20.51780278187175455 ) ) ;
#23965=CARTESIAN_POINT ( 'NONE',  ( -7.188101187499990274, -2.977408999572651815, 25.95530278187175810 ) ) ;
#23970=CYLINDRICAL_SURFACE ( 'NONE', #32205, 7.999999999999991118 ) ;
#23981=CARTESIAN_POINT ( 'NONE',  ( 3.313708498984762496, -7.999999999999989342, 16.29905277982336642 ) ) ;
#23997=CARTESIAN_POINT ( 'NONE',  ( -7.999999999999991118, 0.000000000000000000, 4.017802783920145338 ) ) ;
#24015=CARTESIAN_POINT ( 'NONE',  ( 5.656854249492374365, 5.656854249492375253, 10.95530278392014800 ) ) ;
#24045=CARTESIAN_POINT ( 'NONE',  ( -7.188101187499990274, -2.977408999572651371, 4.580302781871752771 ) ) ;
#24068=CARTESIAN_POINT ( 'NONE',  ( -5.082755093536319713, 5.082755093536319713, 12.17405278187175277 ) ) ;
#24071=CARTESIAN_POINT ( 'NONE',  ( -12.18025451098408318, 1.885907279315492735, -0.7157898419446178107 ) ) ;
#24081=CARTESIAN_POINT ( 'NONE',  ( -5.656854249492375253, 5.656854249492375253, 23.33030278392014978 ) ) ;
#24102=CARTESIAN_POINT ( 'NONE',  ( -7.188101187499992051, 0.000000000000000000, 28.48655278187175810 ) ) ;
#24112=CARTESIAN_POINT ( 'NONE',  ( 3.313708498984762496, -7.999999999999989342, 19.48655278392014978 ) ) ;
#24121=ORIENTED_EDGE ( 'NONE', *, *, #12132, .T. ) ;
#24125=CARTESIAN_POINT ( 'NONE',  ( -5.082755093536317936, -5.082755093536320601, 27.17405278187175455 ) ) ;
#24142=CARTESIAN_POINT ( 'NONE',  ( 8.008118988124993010, -3.317071493978877239, 1.669365283940626998 ) ) ;
#24146=CARTESIAN_POINT ( 'NONE',  ( 4.707324249721353659, -6.606384249263396846, 0.04231178935258603918 ) ) ;
#24158=EDGE_CURVE ( 'NONE', #58023, #72561, #14407, .T. ) ;
#24168=CARTESIAN_POINT ( 'NONE',  ( -4.898587196589407898E-16, 7.999999999999991118, 12.45530277982336642 ) ) ;
#24170=( BOUNDED_CURVE ( )  B_SPLINE_CURVE ( 2, ( #55507, #15488, #66428, #9849, #3819, #50569, #26816, #72084, #32874 ),
 .UNSPECIFIED., .F., .F. ) 
 B_SPLINE_CURVE_WITH_KNOTS ( ( 3, 2, 2, 2, 3 ),
 ( 0.4210526315789475116, 0.4276315789473685847, 0.4342105263157896022, 0.4407894736842106198, 0.4473684210526316929 ),
 .UNSPECIFIED. ) 
 CURVE ( )  GEOMETRIC_REPRESENTATION_ITEM ( )  RATIONAL_B_SPLINE_CURVE ( ( 0.9999999999999981126, 0.9238795325112886259, 1.000000000000000000, 0.9238795325112867385, 1.000000000000000000, 0.9238795325112867385, 1.000000000000000000, 0.9238795325112854062, 1.000000000000001332 ) ) 
 REPRESENTATION_ITEM ( '' )  );
#24184=CARTESIAN_POINT ( 'NONE',  ( -7.999999999999989342, -3.313708498984762496, 15.98030278432982243 ) ) ;
#24214=CARTESIAN_POINT ( 'NONE',  ( 2.977408999572646486, 7.188101187499991163, 10.01780278187175632 ) ) ;
#24239=CARTESIAN_POINT ( 'NONE',  ( -5.082755093536319713, 5.082755093536319713, 13.67405278187175455 ) ) ;
#24288=CARTESIAN_POINT ( 'NONE',  ( 8.008118988124991233, 3.317071493978879015, 12.35686528394062833 ) ) ;
#24295=CARTESIAN_POINT ( 'NONE',  ( 2.977408999572646486, 7.188101187499992051, 10.01780278187175632 ) ) ;
#24309=CARTESIAN_POINT ( 'NONE',  ( 3.313708498984762496, -7.999999999999989342, 4.486552783920144449 ) ) ;
#24324=CARTESIAN_POINT ( 'NONE',  ( -4.401442555609577197E-16, 7.188101187499992051, 16.48655278187175810 ) ) ;
#24326=CARTESIAN_POINT ( 'NONE',  ( 5.656854249492374365, 5.656854249492375253, 3.267802779823362425 ) ) ;
#24334=CARTESIAN_POINT ( 'NONE',  ( 7.188101187499992051, 2.977408999572647819, 26.70530278187175455 ) ) ;
#24351=CARTESIAN_POINT ( 'NONE',  ( -5.656854249492373476, -5.656854249492376141, 13.20530278392014623 ) ) ;
#24352=CARTESIAN_POINT ( 'NONE',  ( 3.313708498984756279, 7.999999999999991118, 13.86155277982336465 ) ) ;
#24370=CARTESIAN_POINT ( 'NONE',  ( 3.313708498984762496, -7.999999999999989342, 5.986552783920146226 ) ) ;
#24409=CARTESIAN_POINT ( 'NONE',  ( -7.999999999999991118, 0.000000000000000000, 5.330302779823363757 ) ) ;
#24416=LINE ( 'NONE', #8174, #56688 ) ;
#24419=CARTESIAN_POINT ( 'NONE',  ( -7.188101187499991163, 2.977408999572646930, 7.392802781871750994 ) ) ;
#24443=CARTESIAN_POINT ( 'NONE',  ( -4.401442555609577197E-16, 7.188101187499992051, 4.486552781871752771 ) ) ;
#24456=CARTESIAN_POINT ( 'NONE',  ( -4.898587196589407898E-16, 7.999999999999991118, 26.14280278392014623 ) ) ;
#24479=CARTESIAN_POINT ( 'NONE',  ( -2.977408999572647819, 7.188101187499992051, 19.20530278187175455 ) ) ;
#24490=CARTESIAN_POINT ( 'NONE',  ( -4.898587196589407898E-16, 7.999999999999991118, 20.14280278392014623 ) ) ;
#24500=CARTESIAN_POINT ( 'NONE',  ( -7.188101187499992051, 0.000000000000000000, 26.98655278187175455 ) ) ;
#24513=CARTESIAN_POINT ( 'NONE',  ( 7.999999999999991118, 3.313708498984758055, 15.17405277982336642 ) ) ;
#24516=CARTESIAN_POINT ( 'NONE',  ( -4.903558642999205574E-16, 8.008118988124991233, 3.638115283940628775 ) ) ;
#24523=CARTESIAN_POINT ( 'NONE',  ( 7.188101187499993827, -2.977408999572645598, 23.51780278187175455 ) ) ;
#24539=CARTESIAN_POINT ( 'NONE',  ( 3.313708498984762496, -7.999999999999989342, 16.29905277982336642 ) ) ;
#24554=CARTESIAN_POINT ( 'NONE',  ( -7.999999999999991118, 0.000000000000000000, 18.88655278432982243 ) ) ;
#24563=B_SPLINE_CURVE_WITH_KNOTS ( 'NONE', 3,
 ( #10020, #37948, #20574, #55303 ),
 .UNSPECIFIED., .F., .F.,
 ( 4, 4 ),
 ( 0.000000000000000000, 1.000000000000000000 ),
 .UNSPECIFIED. ) ;
#24586=CARTESIAN_POINT ( 'NONE',  ( 2.977408999572646486, 7.188101187499991163, 11.51780278187175810 ) ) ;
#24606=CARTESIAN_POINT ( 'NONE',  ( 2.977408999572650927, -7.188101187499990274, 9.830302781871754547 ) ) ;
#24611=CARTESIAN_POINT ( 'NONE',  ( 3.313708498984756279, 7.999999999999991118, 3.549052783920144893 ) ) ;
#24651=CARTESIAN_POINT ( 'NONE',  ( -5.662595241051933570, -5.662595241051936235, 7.200615283940628331 ) ) ;
#24656=CARTESIAN_POINT ( 'NONE',  ( 5.082755093536320601, -5.082755093536318824, 8.049052781871752771 ) ) ;
#24670=CARTESIAN_POINT ( 'NONE',  ( 7.999999999999992895, -3.313708498984756279, 3.174052783920144893 ) ) ;
#24682=ORIENTED_EDGE ( 'NONE', *, *, #12132, .F. ) ;
#24684=CARTESIAN_POINT ( 'NONE',  ( 7.188101187499992051, 8.802885111219154394E-16, 14.61155278187175455 ) ) ;
#24705=DIRECTION ( 'NONE',  ( -1.000000000000000000, 0.000000000000000000, 0.000000000000000000 ) ) ;
#24712=CARTESIAN_POINT ( 'NONE',  ( 1.469576158976822172E-15, -7.999999999999991118, 17.70530277982336642 ) ) ;
#24758=ORIENTED_EDGE ( 'NONE', *, *, #18681, .F. ) ;
#24763=FACE_OUTER_BOUND ( 'NONE', #73478, .T. ) ;
#24775=CARTESIAN_POINT ( 'NONE',  ( 2.977408999572646486, 7.188101187499991163, 1.017802781871753215 ) ) ;
#24800=CARTESIAN_POINT ( 'NONE',  ( 7.188101187499993827, -2.977408999572645598, 2.517802781871750550 ) ) ;
#24813=CYLINDRICAL_SURFACE ( 'NONE', #46833, 7.999999999999991118 ) ;
#24816=CARTESIAN_POINT ( 'NONE',  ( 7.999999999999991118, 3.313708498984757611, 24.36155278392014623 ) ) ;
#24833=CARTESIAN_POINT ( 'NONE',  ( 5.656854249492376141, -5.656854249492374365, 12.08030278392014445 ) ) ;
#24836=CARTESIAN_POINT ( 'NONE',  ( 7.188101187499992051, 8.802885111219154394E-16, 20.23655278187175099 ) ) ;
#24844=CARTESIAN_POINT ( 'NONE',  ( 5.656854249492374365, 5.656854249492375253, 15.45530278392014623 ) ) ;
#24853=ADVANCED_FACE ( 'NONE', ( #44133 ), #67143, .F. ) ;
#24856=CARTESIAN_POINT ( 'NONE',  ( -5.082755093536317936, -5.082755093536320601, 22.67405278187175455 ) ) ;
#24862=CARTESIAN_POINT ( 'NONE',  ( 7.999999999667481099, -7.293937043860970585E-05, 4.767800658666735636 ) ) ;
#24867=CARTESIAN_POINT ( 'NONE',  ( -2.977408999572647819, 7.188101187499991163, 1.580302781871753437 ) ) ;
#24872=CARTESIAN_POINT ( 'NONE',  ( -8.008118988124991233, 0.000000000000000000, 5.513115283940630107 ) ) ;
#24879=CARTESIAN_POINT ( 'NONE',  ( 1.320432766682872962E-15, -7.188101187499992051, 24.73655278187175810 ) ) ;
#24885=LINE ( 'NONE', #13562, #23852 ) ;
#24898=CARTESIAN_POINT ( 'NONE',  ( -3.313708498984758943, -7.999999999999989342, 17.61155277982336997 ) ) ;
#24913=CARTESIAN_POINT ( 'NONE',  ( -7.999999999999991118, 3.313708498984756723, 17.29280278432982598 ) ) ;
#24946=CARTESIAN_POINT ( 'NONE',  ( -7.188101187499991163, 2.977408999572646930, 11.89280278187175277 ) ) ;
#24970=CARTESIAN_POINT ( 'NONE',  ( 5.082755093536318824, 5.082755093536319713, 11.79905278187175632 ) ) ;
#24975=CARTESIAN_POINT ( 'NONE',  ( -5.656854249492375253, 5.656854249492375253, 3.830302783920144893 ) ) ;
#25003=CARTESIAN_POINT ( 'NONE',  ( -7.999999999994639843, -6.164467849698474977E-06, 23.51803407853789807 ) ) ;
#25013=CARTESIAN_POINT ( 'NONE',  ( -4.903558642999205574E-16, 8.008118988124991233, 6.638115283940628331 ) ) ;
#25018=CARTESIAN_POINT ( 'NONE',  ( 1.320432766682872962E-15, -7.188101187499992051, 6.361552781871754547 ) ) ;
#25032=CARTESIAN_POINT ( 'NONE',  ( -7.999999999999991118, 0.000000000000000000, 4.017802783920145338 ) ) ;
#25054=CYLINDRICAL_SURFACE ( 'NONE', #4436, 7.999999999999991118 ) ;
#25056=CARTESIAN_POINT ( 'NONE',  ( 7.188101187499992051, 8.802885111219154394E-16, 28.11155278187175455 ) ) ;
#25077=CARTESIAN_POINT ( 'NONE',  ( -7.999999999999989342, -3.313708498984762496, 12.92405277982336287 ) ) ;
#25079=CARTESIAN_POINT ( 'NONE',  ( 1.469576158976822172E-15, -7.999999999999991118, 17.89280278392014623 ) ) ;
#25096=CARTESIAN_POINT ( 'NONE',  ( 7.999999999732929190, -6.536825277765295045E-05, 6.267800880277100362 ) ) ;
#25141=EDGE_CURVE ( 'NONE', #26953, #59338, #33493, .T. ) ;
#25144=CARTESIAN_POINT ( 'NONE',  ( 5.082755093536320601, -5.082755093536318824, 3.549052781871751883 ) ) ;
#25152=PRODUCT_DEFINITION ( 'UNKNOWN', '', #64713, #34261 ) ;
#25169=CARTESIAN_POINT ( 'NONE',  ( 7.188101187499992051, 8.802885111219154394E-16, 4.111552781871752771 ) ) ;
#25184=CARTESIAN_POINT ( 'NONE',  ( 0.000000000000000000, 0.000000000000000000, 30.00000000000000000 ) ) ;
#25187=CARTESIAN_POINT ( 'NONE',  ( -7.999999999999991118, 3.313708498984756723, 23.42405278392015333 ) ) ;
#25207=CARTESIAN_POINT ( 'NONE',  ( 7.188101187499992051, 2.977408999572647819, 20.33030278187175810 ) ) ;
#25217=CARTESIAN_POINT ( 'NONE',  ( 5.656854249492376141, -5.656854249492374365, 16.58030278392014978 ) ) ;
#25227=DIRECTION ( 'NONE',  ( -1.000000000000000000, 0.000000000000000000, 0.000000000000000000 ) ) ;
#25228=CARTESIAN_POINT ( 'NONE',  ( 5.082755093536320601, -5.082755093536318824, 18.54905278187175455 ) ) ;
#25240=CARTESIAN_POINT ( 'NONE',  ( -3.313708498984757611, 7.999999999999991118, 15.54905277982336642 ) ) ;
#25245=CARTESIAN_POINT ( 'NONE',  ( -7.999999999999991118, 0.000000000000000000, 26.51780278392014623 ) ) ;
#25252=CARTESIAN_POINT ( 'NONE',  ( -7.188101187499991163, 2.977408999572646930, 19.76780278187175455 ) ) ;
#25269=CARTESIAN_POINT ( 'NONE',  ( 3.313708498984756279, 7.999999999999991118, 12.36155277982336820 ) ) ;
#25284=CARTESIAN_POINT ( 'NONE',  ( 7.999999999999992895, -3.313708498984756279, 15.04280278432982421 ) ) ;
#25316=CARTESIAN_POINT ( 'NONE',  ( 2.977408999572650927, -7.188101187499990274, 4.955302781871753659 ) ) ;
#25317=EDGE_LOOP ( 'NONE', ( #27306, #59364, #5276, #9269 ) ) ;
#25327=VECTOR ( 'NONE', #14788, 1000.000000000000000 ) ;
#25339=( BOUNDED_CURVE ( )  B_SPLINE_CURVE ( 2, ( #69256, #51907, #51524, #16807, #33831, #56828, #28888, #5149, #45127 ),
 .UNSPECIFIED., .F., .F. ) 
 B_SPLINE_CURVE_WITH_KNOTS ( ( 3, 2, 2, 2, 3 ),
 ( 0.000000000000000000, 0.006618275584456850824, 0.01323655116891370165, 0.01985482675337055247, 0.02647310233782740330 ),
 .UNSPECIFIED. ) 
 CURVE ( )  GEOMETRIC_REPRESENTATION_ITEM ( )  RATIONAL_B_SPLINE_CURVE ( ( 1.000000000000000000, 0.9238795325112867385, 1.000000000000000000, 0.9238795325112867385, 1.000000000000000000, 0.9238795325112867385, 1.000000000000000000, 0.9238795325112849621, 1.000000000000001776 ) ) 
 REPRESENTATION_ITEM ( '' )  );
#25341=CARTESIAN_POINT ( 'NONE',  ( 7.188101187499992051, 8.802885111219154394E-16, 7.111552781871754547 ) ) ;
#25348=ORIENTED_EDGE ( 'NONE', *, *, #38985, .T. ) ;
#25364=CARTESIAN_POINT ( 'NONE',  ( 5.656854249492376141, -5.656854249492374365, 1.392802779823364201 ) ) ;
#25371=CARTESIAN_POINT ( 'NONE',  ( 7.999999999999991118, 9.797174393178815797E-16, 9.080302779823364645 ) ) ;
#25387=CARTESIAN_POINT ( 'NONE',  ( -5.662595241051935346, 5.662595241051935346, 6.825615283940628331 ) ) ;
#25388=UNCERTAINTY_MEASURE_WITH_UNIT (LENGTH_MEASURE( 1.000000000000000082E-05 ), #34272, 'distance_accuracy_value', 'NONE');
#25396=CARTESIAN_POINT ( 'NONE',  ( 7.188101187499993827, -2.977408999572645598, 0.6428027818717527708 ) ) ;
#25409=CARTESIAN_POINT ( 'NONE',  ( 5.082755093536318824, 5.082755093536319713, 27.92405278187175455 ) ) ;
#25425=CARTESIAN_POINT ( 'NONE',  ( 7.999999999999991118, 9.797174393178815797E-16, 1.767802783920142895 ) ) ;
#25431=CARTESIAN_POINT ( 'NONE',  ( -5.082755093536317936, -5.082755093536320601, 27.54905278187175455 ) ) ;
#25450=CARTESIAN_POINT ( 'NONE',  ( -7.999999999999991118, 3.313708498984756723, 15.73655277982336642 ) ) ;
#25464=CARTESIAN_POINT ( 'NONE',  ( -5.656854249492375253, 5.656854249492375253, 27.64280277982336642 ) ) ;
#25470=( BOUNDED_CURVE ( )  B_SPLINE_CURVE ( 2, ( #17813, #47216, #41929, #57829, #860, #23846, #6869, #29141, #18923 ),
 .UNSPECIFIED., .F., .F. ) 
 B_SPLINE_CURVE_WITH_KNOTS ( ( 3, 2, 2, 2, 3 ),
 ( 0.5294620445568896105, 0.5360803223410017804, 0.5426985979254586034, 0.5493168735099153155, 0.5559351258181921551 ),
 .UNSPECIFIED. ) 
 CURVE ( )  GEOMETRIC_REPRESENTATION_ITEM ( )  RATIONAL_B_SPLINE_CURVE ( ( 1.000000000000000000, 0.9238795325112867385, 1.000000000000000000, 0.9238795325112867385, 1.000000000000000000, 0.9238795325112867385, 1.000000000000000000, 0.9238798002235764084, 0.9999994645773038204 ) ) 
 REPRESENTATION_ITEM ( '' )  );
#25479=CARTESIAN_POINT ( 'NONE',  ( 8.008118988124991233, 3.317071493978879015, 24.35686528394063188 ) ) ;
#25505=CARTESIAN_POINT ( 'NONE',  ( 5.656854249492376141, -5.656854249492374365, 9.080302783920146226 ) ) ;
#25511=CARTESIAN_POINT ( 'NONE',  ( -6.062599403785866592, -5.219663636056774081, 0.8834915628530353171 ) ) ;
#25512=ORIENTED_EDGE ( 'NONE', *, *, #17047, .T. ) ;
#25515=CARTESIAN_POINT ( 'NONE',  ( 2.977408999572646486, 7.188101187499991163, 2.517802781871750550 ) ) ;
#25539=CARTESIAN_POINT ( 'NONE',  ( 2.977408999572646486, 7.188101187499991163, 1.392802781871753437 ) ) ;
#25555=CARTESIAN_POINT ( 'NONE',  ( -7.999999999999991118, 3.313708498984756723, 21.92405278392015333 ) ) ;
#25577=CARTESIAN_POINT ( 'NONE',  ( 5.082755093536320601, -5.082755093536318824, 18.54905278187175455 ) ) ;
#25589=CARTESIAN_POINT ( 'NONE',  ( 5.656854249492376141, -5.656854249492374365, 12.08030278392014445 ) ) ;
#25590=CARTESIAN_POINT ( 'NONE',  ( -7.999999999999991118, -3.618600720434140080E-05, 19.01780380767893064 ) ) ;
#25599=CARTESIAN_POINT ( 'NONE',  ( -2.977408999572647819, 7.188101187499991163, 16.20530278187175455 ) ) ;
#25617=CARTESIAN_POINT ( 'NONE',  ( 3.313708498984762496, -7.999999999999989342, 25.48655278392014623 ) ) ;
#25624=CARTESIAN_POINT ( 'NONE',  ( -7.188101187499990274, -2.977408999572651371, 19.95530278187175810 ) ) ;
#25640=CARTESIAN_POINT ( 'NONE',  ( -4.898587196589407898E-16, 7.999999999999991118, 7.955302779823362869 ) ) ;
#25656=CARTESIAN_POINT ( 'NONE',  ( -5.656854249492373476, -5.656854249492376141, 20.57405278432982243 ) ) ;
#25685=CARTESIAN_POINT ( 'NONE',  ( -2.977408999572648707, -7.188101187499990274, 7.767802781871751883 ) ) ;
#25708=CARTESIAN_POINT ( 'NONE',  ( -2.977408999572647819, -7.188101187499990274, 3.642802781871751883 ) ) ;
#25733=ORIENTED_EDGE ( 'NONE', *, *, #1238, .T. ) ;
#25736=CARTESIAN_POINT ( 'NONE',  ( -7.999999999999991118, 9.797174393178815797E-16, 30.00000000000000000 ) ) ;
#25737=CARTESIAN_POINT ( 'NONE',  ( -5.656854249492373476, -5.656854249492376141, 8.705302783920146226 ) ) ;
#25740=DIRECTION ( 'NONE',  ( 0.000000000000000000, -0.2588190451025146332, 0.9659258262890699775 ) ) ;
#25755=CARTESIAN_POINT ( 'NONE',  ( 8.008118988124991233, 3.317071493978879015, 10.85686528394063188 ) ) ;
#25761=CARTESIAN_POINT ( 'NONE',  ( 5.082755093536318824, 5.082755093536319713, 2.424052781871750994 ) ) ;
#25773=CARTESIAN_POINT ( 'NONE',  ( 2.977408999572646486, 7.188101187499991163, 23.51780278187175455 ) ) ;
#25793=CARTESIAN_POINT ( 'NONE',  ( 5.656854249492374365, 5.656854249492375253, 24.45530278392014978 ) ) ;
#25800=CARTESIAN_POINT ( 'NONE',  ( 2.977408999572646486, 7.188101187499992051, 22.39280278187175810 ) ) ;
#25802=CARTESIAN_POINT ( 'NONE',  ( 7.999999999999991118, 2.512580743551133942E-05, 22.76780349476856458 ) ) ;
#25818=CARTESIAN_POINT ( 'NONE',  ( 5.656854249492376141, -5.656854249492374365, 13.58030278392014623 ) ) ;
#25819=CARTESIAN_POINT ( 'NONE',  ( 7.999999999999991118, 9.797174393178815797E-16, 9.080302779823364645 ) ) ;
#25846=CARTESIAN_POINT ( 'NONE',  ( 3.317071493978883456, -8.008118988124989457, 25.48186528394063188 ) ) ;
#25864=CONICAL_SURFACE ( 'NONE', #72851, 12.50000000000000178, 0.06208826691561822320 ) ;
#25879=CARTESIAN_POINT ( 'NONE',  ( -7.188101187499990274, -2.977408999572651371, 3.080302781871750994 ) ) ;
#25907=CARTESIAN_POINT ( 'NONE',  ( 7.999999999999991118, 9.797174393178815797E-16, 25.58030277982336997 ) ) ;
#25908=DIRECTION ( 'NONE',  ( 1.000000000000000000, 0.000000000000000000, 0.000000000000000000 ) ) ;
#25925=CARTESIAN_POINT ( 'NONE',  ( 7.999999999999991118, 3.313708498984757611, 18.36155278392014623 ) ) ;
#25943=CARTESIAN_POINT ( 'NONE',  ( -7.999999999999989342, -3.313708498984762496, 11.61155278392014445 ) ) ;
#25946=CARTESIAN_POINT ( 'NONE',  ( -5.082755093536319713, 5.082755093536319713, 22.29905278187175455 ) ) ;
#25947=CARTESIAN_POINT ( 'NONE',  ( -3.313708498984759387, -7.999999999999989342, 16.29905278392014623 ) ) ;
#25953=CARTESIAN_POINT ( 'NONE',  ( 7.999999999999991118, 3.313708498984757611, 13.86155278392014623 ) ) ;
#25964=CARTESIAN_POINT ( 'NONE',  ( 2.977408999572646486, 7.188101187499991163, 20.51780278187175455 ) ) ;
#25965=VERTEX_POINT ( 'NONE', #25003 ) ;
#25980=CARTESIAN_POINT ( 'NONE',  ( 7.999999999999992895, -3.313708498984756279, 25.67405278392015333 ) ) ;
#25987=CARTESIAN_POINT ( 'NONE',  ( 2.977408999572650927, -7.188101187499990274, 24.83030278187175455 ) ) ;
#26004=CARTESIAN_POINT ( 'NONE',  ( 7.999999999999992895, -3.313708498984756279, 11.98655277982336997 ) ) ;
#26005=FACE_OUTER_BOUND ( 'NONE', #13047, .T. ) ;
#26022=CARTESIAN_POINT ( 'NONE',  ( 1.469576158976822172E-15, -7.999999999999991118, 10.26155278432982598 ) ) ;
#26054=CARTESIAN_POINT ( 'NONE',  ( 2.977408999572646486, 7.188101187499991163, 4.017802781871751883 ) ) ;
#26056=ADVANCED_FACE ( 'NONE', ( #70673 ), #19351, .F. ) ;
#26068=CARTESIAN_POINT ( 'NONE',  ( 1.320432766682872962E-15, -7.188101187499992051, 9.736552781871754547 ) ) ;
#26080=CARTESIAN_POINT ( 'NONE',  ( -2.977408999572647819, 7.188101187499992051, 7.580302781871751883 ) ) ;
#26097=CARTESIAN_POINT ( 'NONE',  ( -3.313708498984758943, -7.999999999999989342, 26.61155277982337708 ) ) ;
#26110=CARTESIAN_POINT ( 'NONE',  ( -3.313708498984757167, 7.999999999999991118, 0.7365527839201455595 ) ) ;
#26127=CARTESIAN_POINT ( 'NONE',  ( 1.471067592899761672E-15, -8.008118988124991233, 10.38811528394063188 ) ) ;
#26135=CARTESIAN_POINT ( 'NONE',  ( 7.188101187499993827, -2.977408999572645598, 5.142802781871753659 ) ) ;
#26149=CARTESIAN_POINT ( 'NONE',  ( -2.977408999572648707, -7.188101187499990274, 22.76780278187175455 ) ) ;
#26173=CARTESIAN_POINT ( 'NONE',  ( -7.188101187499990274, -2.977408999572651815, 22.95530278187175455 ) ) ;
#26193=CARTESIAN_POINT ( 'NONE',  ( 5.656854249492374365, 5.656854249492375253, 9.267802779823364645 ) ) ;
#26195=FACE_OUTER_BOUND ( 'NONE', #13395, .T. ) ;
#26236=VERTEX_POINT ( 'NONE', #58093 ) ;
#26242=CARTESIAN_POINT ( 'NONE',  ( -7.999999999999948486, 3.313708498984799355, 14.23655277982336287 ) ) ;
#26256=CARTESIAN_POINT ( 'NONE',  ( 2.977408999572646486, 7.188101187499991163, 28.39280278187175810 ) ) ;
#26280=CARTESIAN_POINT ( 'NONE',  ( 7.999999999999992895, -3.313708498984756279, 28.48655277982336642 ) ) ;
#26298=CARTESIAN_POINT ( 'NONE',  ( -3.313708498984757167, 7.999999999999991118, 20.23655278392014978 ) ) ;
#26301=CARTESIAN_POINT ( 'NONE',  ( 4.172829859562196653, -6.868037143713721981, 0.000000000000000000 ) ) ;
#26321=CARTESIAN_POINT ( 'NONE',  ( 5.082755093536320601, -5.082755093536318824, 12.54905278187175277 ) ) ;
#26322=CARTESIAN_POINT ( 'NONE',  ( -7.999999999999989342, -3.313708498984762496, 16.11155278392014623 ) ) ;
#26331=CARTESIAN_POINT ( 'NONE',  ( -5.656854249492375253, 5.656854249492375253, 11.33030278392014445 ) ) ;
#26343=CARTESIAN_POINT ( 'NONE',  ( -2.977408999572647819, 7.188101187499991163, 17.70530278187175455 ) ) ;
#26348=CARTESIAN_POINT ( 'NONE',  ( 5.656854249492376141, -5.656854249492374365, 24.08030278392014978 ) ) ;
#26350=DIRECTION ( 'NONE',  ( 1.000000000000000000, 0.000000000000000000, 0.000000000000000000 ) ) ;
#26359=CARTESIAN_POINT ( 'NONE',  ( -3.313708498984757167, 7.999999999999991118, 27.73655278392014978 ) ) ;
#26366=CARTESIAN_POINT ( 'NONE',  ( 7.188101187499991163, 2.977408999572648707, 16.20530278187175455 ) ) ;
#26380=CARTESIAN_POINT ( 'NONE',  ( -5.656854249492373476, -5.656854249492376141, 7.017802779823365533 ) ) ;
#26393=CARTESIAN_POINT ( 'NONE',  ( 3.313708498984762496, -7.999999999999989342, 2.986552783920144893 ) ) ;
#26396=CARTESIAN_POINT ( 'NONE',  ( -3.313708498984757167, 7.999999999999991118, 14.10530278432982421 ) ) ;
#26401=VERTEX_POINT ( 'NONE', #35081 ) ;
#26417=EDGE_CURVE ( 'NONE', #33251, #52951, #70146, .T. ) ;
#26430=CARTESIAN_POINT ( 'NONE',  ( 5.082755093536318824, 5.082755093536319713, 8.424052781871752771 ) ) ;
#26444=CARTESIAN_POINT ( 'NONE',  ( 2.977408999572650927, -7.188101187499990274, 12.83030278187175277 ) ) ;
#26454=CARTESIAN_POINT ( 'NONE',  ( -5.447321926944742820, -4.689934168550192517, 0.4069290644665413681 ) ) ;
#26458=CARTESIAN_POINT ( 'NONE',  ( -5.082755093536319713, 5.082755093536319713, 4.674052781871752771 ) ) ;
#26475=CARTESIAN_POINT ( 'NONE',  ( -5.656854249492375253, 5.656854249492375253, 24.64280277982336642 ) ) ;
#26486=CARTESIAN_POINT ( 'NONE',  ( 5.656854249492374365, 5.656854249492375253, 0.4553027839201452265 ) ) ;
#26509=CARTESIAN_POINT ( 'NONE',  ( 1.320432766682872962E-15, -7.188101187499992051, 4.861552781871752771 ) ) ;
#26521=EDGE_CURVE ( 'NONE', #59338, #8699, #10395, .T. ) ;
#26524=CARTESIAN_POINT ( 'NONE',  ( -4.401442555609577197E-16, 7.188101187499992051, 22.11155278187175455 ) ) ;
#26537=VECTOR ( 'NONE', #48524, 1000.000000000000000 ) ;
#26549=CARTESIAN_POINT ( 'NONE',  ( -7.188101187499990274, -2.977408999572651815, 19.95530278187175455 ) ) ;
#26570=CARTESIAN_POINT ( 'NONE',  ( -5.656854249492373476, -5.656854249492376141, 8.517802779823362869 ) ) ;
#26603=CARTESIAN_POINT ( 'NONE',  ( 3.317071493978877683, 8.008118988124991233, 24.54436528394063188 ) ) ;
#26621=CARTESIAN_POINT ( 'NONE',  ( 3.313708498984756279, 7.999999999999991118, 13.86155277982336465 ) ) ;
#26636=CARTESIAN_POINT ( 'NONE',  ( -7.188101187499992051, 0.000000000000000000, 22.86155278187175455 ) ) ;
#26664=CARTESIAN_POINT ( 'NONE',  ( 7.999999999999992895, -3.313708498984756279, 25.48655277982336642 ) ) ;
#26682=CARTESIAN_POINT ( 'NONE',  ( 5.656854249492374365, 5.656854249492375253, 18.45530278392014623 ) ) ;
#26707=CARTESIAN_POINT ( 'NONE',  ( -7.188101187499992051, 2.977408999572646930, 14.89280278187175455 ) ) ;
#26717=CARTESIAN_POINT ( 'NONE',  ( -7.999999999999991118, 0.000000000000000000, 10.01780278392014623 ) ) ;
#26728=CARTESIAN_POINT ( 'NONE',  ( -5.082755093536317936, -5.082755093536320601, 10.67405278187175455 ) ) ;
#26733=CARTESIAN_POINT ( 'NONE',  ( -7.999999999999991118, 0.000000000000000000, 17.33030277982336287 ) ) ;
#26755=CARTESIAN_POINT ( 'NONE',  ( 5.082755093536320601, -5.082755093536318824, 14.42405278187175455 ) ) ;
#26772=CARTESIAN_POINT ( 'NONE',  ( 3.313708498984756279, 7.999999999999991118, 6.361552779823365533 ) ) ;
#26785=CARTESIAN_POINT ( 'NONE',  ( 5.656854249492376141, -5.656854249492374365, 3.080302783920144005 ) ) ;
#26787=CARTESIAN_POINT ( 'NONE',  ( 7.999999999999991118, 9.797174393178815797E-16, 10.63655278432982598 ) ) ;
#26788=VECTOR ( 'NONE', #66199, 1000.000000000000000 ) ;
#26808=CARTESIAN_POINT ( 'NONE',  ( 7.999999999999991118, 9.797174393178815797E-16, 19.58030277982336642 ) ) ;
#26816=CARTESIAN_POINT ( 'NONE',  ( 5.656854249492374365, 5.656854249492375253, 16.76780277982336287 ) ) ;
#26820=CARTESIAN_POINT ( 'NONE',  ( -2.977408999572648707, -7.188101187499990274, 9.267802781871756324 ) ) ;
#26832=CARTESIAN_POINT ( 'NONE',  ( -7.188101187499991163, 2.977408999572646930, 12.26780278187175455 ) ) ;
#26845=CARTESIAN_POINT ( 'NONE',  ( 7.188101187499993827, -2.977408999572645598, 2.517802781871750994 ) ) ;
#26862=CARTESIAN_POINT ( 'NONE',  ( 3.313708498984756279, 7.999999999999991118, 25.86155277982337353 ) ) ;
#26874=CARTESIAN_POINT ( 'NONE',  ( 5.656854249492376141, -5.656854249492374365, 3.080302783920144005 ) ) ;
#26894=CARTESIAN_POINT ( 'NONE',  ( 5.082755093536318824, 5.082755093536319713, 5.424052781871753659 ) ) ;
#26908=CARTESIAN_POINT ( 'NONE',  ( 2.977408999572646486, 7.188101187499991163, 26.51780278187175455 ) ) ;
#26912=ORIENTED_EDGE ( 'NONE', *, *, #9317, .F. ) ;
#26914=CARTESIAN_POINT ( 'NONE',  ( -6.985140028429535519, 4.041179811479543638, 0.000000000000000000 ) ) ;
#26926=CARTESIAN_POINT ( 'NONE',  ( -7.999999999999991118, 0.000000000000000000, 21.83030277982336997 ) ) ;
#26929=DIRECTION ( 'NONE',  ( -1.000000000000000000, 0.000000000000000000, 0.000000000000000000 ) ) ;
#26930=CARTESIAN_POINT ( 'NONE',  ( -5.082755093536319713, 5.082755093536319713, 24.17405278187175455 ) ) ;
#26949=CARTESIAN_POINT ( 'NONE',  ( -3.313708498984757167, 7.999999999999991118, 8.049052779823362869 ) ) ;
#26953=VERTEX_POINT ( 'NONE', #28013 ) ;
#26960=CARTESIAN_POINT ( 'NONE',  ( -3.313708498984759387, -7.999999999999989342, 10.29905278392014445 ) ) ;
#26980=CARTESIAN_POINT ( 'NONE',  ( -8.008118988124989457, -3.317071493978883900, 19.10686528394063188 ) ) ;
#27003=EDGE_CURVE ( 'NONE', #6793, #46714, #59651, .T. ) ;
#27004=B_SPLINE_CURVE_WITH_KNOTS ( 'NONE', 3,
 ( #27585, #26454, #15514, #3846 ),
 .UNSPECIFIED., .F., .F.,
 ( 4, 4 ),
 ( 0.000000000000000000, 1.000000000000000000 ),
 .UNSPECIFIED. ) ;
#27016=CARTESIAN_POINT ( 'NONE',  ( 2.977408999572646486, 7.188101187499991163, 23.89280278187176165 ) ) ;
#27020=CYLINDRICAL_SURFACE ( 'NONE', #27923, 7.999999999999991118 ) ;
#27042=CARTESIAN_POINT ( 'NONE',  ( 7.999999999999992895, -3.313708498984756279, 26.98655277982336997 ) ) ;
#27043=DIRECTION ( 'NONE',  ( 7.598735409842530687E-18, -0.9801239283673559566, -0.1983862017423140278 ) ) ;
#27053=ORIENTED_EDGE ( 'NONE', *, *, #32012, .F. ) ;
#27061=CARTESIAN_POINT ( 'NONE',  ( -3.313708498984757167, 7.999999999999991118, 18.73655278392014623 ) ) ;
#27072=CARTESIAN_POINT ( 'NONE',  ( 3.313708498984762496, -7.999999999999989342, 28.29905277982337353 ) ) ;
#27082=CARTESIAN_POINT ( 'NONE',  ( -5.082755093536317936, -5.082755093536320601, 13.67405278187175455 ) ) ;
#27089=VERTEX_POINT ( 'NONE', #41558 ) ;
#27092=CARTESIAN_POINT ( 'NONE',  ( 7.999999999999991118, 9.797174393178815797E-16, 7.767802783920144449 ) ) ;
#27097=CARTESIAN_POINT ( 'NONE',  ( 7.999999999999991118, 9.797174393178815797E-16, 12.08030277982336642 ) ) ;
#27103=CARTESIAN_POINT ( 'NONE',  ( -4.401442555609577197E-16, 7.188101187499992051, 14.61155278187175455 ) ) ;
#27128=CARTESIAN_POINT ( 'NONE',  ( 5.082755093536318824, 5.082755093536319713, 14.79905278187175455 ) ) ;
#27143=CARTESIAN_POINT ( 'NONE',  ( 7.999999999999992895, -3.313708498984756279, 10.48655277982336642 ) ) ;
#27157=CARTESIAN_POINT ( 'NONE',  ( -7.999999999999991118, 3.313708498984756723, 11.29280278432982421 ) ) ;
#27187=CARTESIAN_POINT ( 'NONE',  ( -7.188101187499992051, 0.000000000000000000, 1.486552781871753437 ) ) ;
#27199=CARTESIAN_POINT ( 'NONE',  ( -7.188101187499990274, -2.977408999572651371, 10.95530278187175455 ) ) ;
#27212=CARTESIAN_POINT ( 'NONE',  ( 0.000000000000000000, 0.000000000000000000, 29.33030277982336642 ) ) ;
#27228=CARTESIAN_POINT ( 'NONE',  ( 3.313708498984756279, 7.999999999999991118, 28.86155277982336642 ) ) ;
#27236=ORIENTED_EDGE ( 'NONE', *, *, #45453, .T. ) ;
#27240=CARTESIAN_POINT ( 'NONE',  ( 3.313708498984756279, 7.999999999999991118, 0.5490527839201453375 ) ) ;
#27244=ORIENTED_EDGE ( 'NONE', *, *, #43886, .F. ) ;
#27246=CIRCLE ( 'NONE', #4372, 12.50000000000000711 ) ;
#27276=CARTESIAN_POINT ( 'NONE',  ( -7.188101187499990274, -2.977408999572651371, 16.58030278187175455 ) ) ;
#27279=ORIENTED_EDGE ( 'NONE', *, *, #35751, .F. ) ;
#27289=VERTEX_POINT ( 'NONE', #53170 ) ;
#27300=CARTESIAN_POINT ( 'NONE',  ( 5.082755093536318824, 5.082755093536319713, 20.79905278187175455 ) ) ;
#27306=ORIENTED_EDGE ( 'NONE', *, *, #48601, .F. ) ;
#27317=CARTESIAN_POINT ( 'NONE',  ( -5.656854249492375253, 5.656854249492375253, 6.642802779823365533 ) ) ;
#27328=CARTESIAN_POINT ( 'NONE',  ( 7.999999999999706901, -2.135495361439877059E-06, 10.76780272350167245 ) ) ;
#27346=CARTESIAN_POINT ( 'NONE',  ( 3.317071493978883456, -8.008118988124989457, 19.48186528394063544 ) ) ;
#27358=( BOUNDED_CURVE ( )  B_SPLINE_CURVE ( 2, ( #35971, #20075, #25364, #60076, #8395, #48381, #64637, #7296, #59354 ),
 .UNSPECIFIED., .F., .F. ) 
 B_SPLINE_CURVE_WITH_KNOTS ( ( 3, 2, 2, 2, 3 ),
 ( 0.9736842105263158187, 0.9802631578947368363, 0.9868421052631578538, 0.9934210526315789824, 0.9940576599040155115 ),
 .UNSPECIFIED. ) 
 CURVE ( )  GEOMETRIC_REPRESENTATION_ITEM ( )  RATIONAL_B_SPLINE_CURVE ( ( 1.000000000000000000, 0.9238795325112867385, 1.000000000000000000, 0.9238795325112867385, 1.000000000000000000, 0.9238795325112867385, 1.000000000000000000, 0.9926342558359432244, 0.9866939939076171395 ) ) 
 REPRESENTATION_ITEM ( '' )  );
#27381=CARTESIAN_POINT ( 'NONE',  ( 2.977408999572650927, -7.188101187499990274, 24.83030278187175455 ) ) ;
#27396=ORIENTED_EDGE ( 'NONE', *, *, #34648, .F. ) ;
#27407=CARTESIAN_POINT ( 'NONE',  ( 5.656854249492374365, 5.656854249492375253, 24.26780277982336642 ) ) ;
#27422=CARTESIAN_POINT ( 'NONE',  ( -7.999999999999991118, 9.797174393178815797E-16, 30.00000000000000000 ) ) ;
#27425=CARTESIAN_POINT ( 'NONE',  ( 1.469576158976822172E-15, -7.999999999999991118, 10.39280278392014800 ) ) ;
#27444=CARTESIAN_POINT ( 'NONE',  ( 7.188101187499993827, -2.977408999572645598, 17.14280278187175455 ) ) ;
#27470=CARTESIAN_POINT ( 'NONE',  ( -5.082755093536319713, 5.082755093536319713, 13.29905278187175277 ) ) ;
#27473=VERTEX_POINT ( 'NONE', #33645 ) ;
#27496=CARTESIAN_POINT ( 'NONE',  ( -7.188101187499992051, 0.000000000000000000, 16.86155278187175810 ) ) ;
#27514=CARTESIAN_POINT ( 'NONE',  ( -3.313708498984757167, 7.999999999999991118, 2.049052779823364645 ) ) ;
#27530=CARTESIAN_POINT ( 'NONE',  ( 1.469576158976822172E-15, -7.999999999999991118, 13.26155278432982421 ) ) ;
#27540=FACE_OUTER_BOUND ( 'NONE', #10572, .T. ) ;
#27562=CARTESIAN_POINT ( 'NONE',  ( 7.188101187499993827, -2.977408999572645598, 2.142802781871750550 ) ) ;
#27576=CARTESIAN_POINT ( 'NONE',  ( 2.977408999572650927, -7.188101187499990274, 8.330302781871752771 ) ) ;
#27585=CARTESIAN_POINT ( 'NONE',  ( -5.447323953993864265, -4.689931814214729044, 0.5319290643893268555 ) ) ;
#27603=CARTESIAN_POINT ( 'NONE',  ( 7.999999999999991118, 3.313708498984757611, 27.17405277982336997 ) ) ;
#27617=CARTESIAN_POINT ( 'NONE',  ( -5.656854249492375253, 5.656854249492375253, 2.330302783920143561 ) ) ;
#27623=ADVANCED_FACE ( 'NONE', ( #28702 ), #51370, .F. ) ;
#27644=CARTESIAN_POINT ( 'NONE',  ( 7.999999999836578723, -5.113295603412193572E-05, 3.267801294049292871 ) ) ;
#27652=CARTESIAN_POINT ( 'NONE',  ( 2.977408999572650927, -7.188101187499990274, 19.95530278187175810 ) ) ;
#27672=CARTESIAN_POINT ( 'NONE',  ( 3.313708498984762496, -7.999999999999989342, 22.29905277982336287 ) ) ;
#27677=CARTESIAN_POINT ( 'NONE',  ( 1.320432766682872962E-15, -7.188101187499992051, 14.23655278187175455 ) ) ;
#27694=CARTESIAN_POINT ( 'NONE',  ( 3.313708498984762496, -7.999999999999989342, 5.799052779823364645 ) ) ;
#27704=CARTESIAN_POINT ( 'NONE',  ( 3.313708498984762496, -7.999999999999989342, 10.48655278392014800 ) ) ;
#27723=CARTESIAN_POINT ( 'NONE',  ( -5.662595241051933570, -5.662595241051936235, 20.70061528394062833 ) ) ;
#27737=ORIENTED_EDGE ( 'NONE', *, *, #7928, .T. ) ;
#27742=CARTESIAN_POINT ( 'NONE',  ( 7.999999999999991118, 9.797174393178815797E-16, 13.58030277982336465 ) ) ;
#27756=CARTESIAN_POINT ( 'NONE',  ( -7.188101187499991163, 2.977408999572646930, 24.26780278187175455 ) ) ;
#27782=CARTESIAN_POINT ( 'NONE',  ( -3.313708498984757167, 7.999999999999991118, 18.54905277982336287 ) ) ;
#27802=CARTESIAN_POINT ( 'NONE',  ( -4.898587196589407898E-16, 7.999999999999991118, 14.14280278392014623 ) ) ;
#27835=ADVANCED_FACE ( 'NONE', ( #26005 ), #55839, .F. ) ;
#27842=CARTESIAN_POINT ( 'NONE',  ( 0.000000000000000000, 0.000000000000000000, 11.00000000000000000 ) ) ;
#27852=CARTESIAN_POINT ( 'NONE',  ( -7.188101187499992051, 0.000000000000000000, 11.98655278187175277 ) ) ;
#27875=CARTESIAN_POINT ( 'NONE',  ( -2.977408999572648707, -7.188101187499990274, 14.14280278187175455 ) ) ;
#27890=CARTESIAN_POINT ( 'NONE',  ( -5.656854249492375253, 5.656854249492375253, 3.642802779823362869 ) ) ;
#27891=CARTESIAN_POINT ( 'NONE',  ( 7.999999999988127719, 1.377684776014802281E-05, 21.26780317368888618 ) ) ;
#27909=CARTESIAN_POINT ( 'NONE',  ( 7.999999999999991118, 9.797174393178815797E-16, 7.636552784329823318 ) ) ;
#27910=CARTESIAN_POINT ( 'NONE',  ( 5.656854249492374365, 5.656854249492375253, 4.767802779823363757 ) ) ;
#27923=AXIS2_PLACEMENT_3D ( 'NONE', #44378, #72293, #54962 ) ;
#27929=EDGE_CURVE ( 'NONE', #19453, #16032, #45638, .T. ) ;
#27952=EDGE_CURVE ( 'NONE', #59170, #71548, #17209, .T. ) ;
#27956=CARTESIAN_POINT ( 'NONE',  ( 7.188101187499992051, 8.802885111219154394E-16, 8.611552781871752771 ) ) ;
#27986=CARTESIAN_POINT ( 'NONE',  ( 7.999999999999992895, -3.313708498984756279, 23.98655277982336642 ) ) ;
#27998=CARTESIAN_POINT ( 'NONE',  ( 1.469576158976822172E-15, -7.999999999999991118, 23.76155278432982598 ) ) ;
#28008=ORIENTED_EDGE ( 'NONE', *, *, #67405, .F. ) ;
#28013=CARTESIAN_POINT ( 'NONE',  ( 7.999999999999991118, 9.797174393178815797E-16, 12.08030277982336642 ) ) ;
#28018=( BOUNDED_CURVE ( )  B_SPLINE_CURVE ( 2, ( #67331, #74100, #22398, #34132, #57132, #33759, #68073, #50710, #62036, #9989, #33021 ),
 .UNSPECIFIED., .F., .F. ) 
 B_SPLINE_CURVE_WITH_KNOTS ( ( 3, 2, 2, 2, 2, 3 ),
 ( 0.4500427433262104704, 0.4566610153275200701, 0.4632792909119768376, 0.4698975664964336607, 0.4765158420808904283, 0.4765158731794318925 ),
 .UNSPECIFIED. ) 
 CURVE ( )  GEOMETRIC_REPRESENTATION_ITEM ( )  RATIONAL_B_SPLINE_CURVE ( ( 1.000000000000000000, 0.9238795325112867385, 1.000000000000000000, 0.9238795325112867385, 1.000000000000000000, 0.9238795325112867385, 1.000000000000000000, 0.9238795325112867385, 1.000000000000000000, 0.9999996423183825645, 0.9999992846401264401 ) ) 
 REPRESENTATION_ITEM ( '' )  );
#28030=CARTESIAN_POINT ( 'NONE',  ( -4.401442555609577197E-16, 7.188101187499992051, 20.61155278187175455 ) ) ;
#28052=CARTESIAN_POINT ( 'NONE',  ( 7.188101187499993827, -2.977408999572645598, 14.51780278187175455 ) ) ;
#28096=CARTESIAN_POINT ( 'NONE',  ( -4.903558642999205574E-16, 8.008118988124991233, 20.13811528394062833 ) ) ;
#28114=EDGE_CURVE ( 'NONE', #51815, #60780, #57806, .T. ) ;
#28127=CARTESIAN_POINT ( 'NONE',  ( -7.118986530994914297, -3.658836280118772599, 0.000000000000000000 ) ) ;
#28131=CARTESIAN_POINT ( 'NONE',  ( -7.188101187499990274, -2.977408999572651371, 21.45530278187175810 ) ) ;
#28153=( BOUNDED_CURVE ( )  B_SPLINE_CURVE ( 2, ( #2388, #42004, #7318, #59740, #8048, #31053, #53711, #30324, #53342 ),
 .UNSPECIFIED., .F., .F. ) 
 B_SPLINE_CURVE_WITH_KNOTS ( ( 3, 2, 2, 2, 3 ),
 ( 0.5526315789473684736, 0.5592105263157894912, 0.5657894736842106198, 0.5723684210526316374, 0.5789473684210527660 ),
 .UNSPECIFIED. ) 
 CURVE ( )  GEOMETRIC_REPRESENTATION_ITEM ( )  RATIONAL_B_SPLINE_CURVE ( ( 1.000000000000000000, 0.9238795325112867385, 1.000000000000000000, 0.9238795325112867385, 1.000000000000000000, 0.9238795325112867385, 1.000000000000000000, 0.9238795325112854062, 1.000000000000001332 ) ) 
 REPRESENTATION_ITEM ( '' )  );
#28158=CARTESIAN_POINT ( 'NONE',  ( -5.656854249492375253, 5.656854249492375253, 20.14280277982336642 ) ) ;
#28176=CARTESIAN_POINT ( 'NONE',  ( 1.469576158976822172E-15, -7.999999999999991118, 11.89280278392014445 ) ) ;
#28200=EDGE_CURVE ( 'NONE', #21048, #31338, #39963, .T. ) ;
#28213=DIRECTION ( 'NONE',  ( -1.000000000000000000, -0.000000000000000000, -0.000000000000000000 ) ) ;
#28215=ADVANCED_FACE ( 'NONE', ( #14233 ), #8593, .F. ) ;
#28226=CARTESIAN_POINT ( 'NONE',  ( 7.188101187499992051, 8.802885111219154394E-16, 12.73655278187175277 ) ) ;
#28252=CARTESIAN_POINT ( 'NONE',  ( -2.977408999572647819, 7.188101187499991163, 12.08030278187175099 ) ) ;
#28254=CARTESIAN_POINT ( 'NONE',  ( 7.999999999752645863, -6.290875383172500320E-05, 1.767801038436179750 ) ) ;
#28256=CARTESIAN_POINT ( 'NONE',  ( -9.121419926064122663, -1.666886344965055722, -0.5794300317457429239 ) ) ;
#28267=CARTESIAN_POINT ( 'NONE',  ( 3.313708498984756279, 7.999999999999991118, 4.861552779823364645 ) ) ;
#28285=CARTESIAN_POINT ( 'NONE',  ( -7.999999999999991118, 3.313708498984756723, 6.792802784329821542 ) ) ;
#28312=CARTESIAN_POINT ( 'NONE',  ( -2.977408999572647819, 7.188101187499991163, 2.705302781871750994 ) ) ;
#28325=CARTESIAN_POINT ( 'NONE',  ( 5.082755093536318824, 5.082755093536319713, 7.299052781871751883 ) ) ;
#28326=EDGE_CURVE ( 'NONE', #51761, #65370, #71210, .T. ) ;
#28342=CARTESIAN_POINT ( 'NONE',  ( -4.898587196589407898E-16, 7.999999999999991118, 28.95530277982336642 ) ) ;
#28352=CARTESIAN_POINT ( 'NONE',  ( 5.656854249492376141, -5.656854249492374365, 20.89280277982336642 ) ) ;
#28366=CARTESIAN_POINT ( 'NONE',  ( -5.656854249492373476, -5.656854249492376141, 26.57405278432982243 ) ) ;
#28377=ORIENTED_EDGE ( 'NONE', *, *, #53528, .T. ) ;
#28397=CARTESIAN_POINT ( 'NONE',  ( -2.045563441603947318E-15, 16.70329308849007077, 0.000000000000000000 ) ) ;
#28398=ADVANCED_FACE ( 'NONE', ( #38021 ), #32744, .F. ) ;
#28401=CARTESIAN_POINT ( 'NONE',  ( -5.082755093536319713, 5.082755093536319713, 20.79905278187175455 ) ) ;
#28413=ORIENTED_EDGE ( 'NONE', *, *, #55686, .F. ) ;
#28424=CARTESIAN_POINT ( 'NONE',  ( 2.977408999572646486, 7.188101187499992051, 16.39280278187175455 ) ) ;
#28459=CARTESIAN_POINT ( 'NONE',  ( 7.152797884309432419, -3.603458643537627459, -0.000000000000000000 ) ) ;
#28472=CARTESIAN_POINT ( 'NONE',  ( 7.999999999999920064, -1.061780717098090627E-06, 7.767802753882760314 ) ) ;
#28473=CARTESIAN_POINT ( 'NONE',  ( 5.662595241051934458, 5.662595241051935346, 21.45061528394063188 ) ) ;
#28492=CARTESIAN_POINT ( 'NONE',  ( 7.999999999999991118, 3.313708498984757611, 10.86155278392014800 ) ) ;
#28505=CARTESIAN_POINT ( 'NONE',  ( -5.082755093536317936, -5.082755093536320601, 18.54905278187175455 ) ) ;
#28530=CARTESIAN_POINT ( 'NONE',  ( -3.313708498984758943, -7.999999999999989342, 23.61155277982336997 ) ) ;
#28537=CARTESIAN_POINT ( 'NONE',  ( 7.999999999999950262, -3.313708498984798467, 8.986552779823366421 ) ) ;
#28548=CARTESIAN_POINT ( 'NONE',  ( -7.999999999999991118, 0.000000000000000000, 11.51780278392014445 ) ) ;
#28581=( BOUNDED_CURVE ( )  B_SPLINE_CURVE ( 2, ( #62870, #21761, #22885, #56489, #4806, #46268, #45157, #63243, #62498 ),
 .UNSPECIFIED., .F., .F. ) 
 B_SPLINE_CURVE_WITH_KNOTS ( ( 3, 2, 2, 2, 3 ),
 ( 0.2105263157894737558, 0.2171052631578948011, 0.2236842105263158187, 0.2302631578947368085, 0.2368421052631578261 ),
 .UNSPECIFIED. ) 
 CURVE ( )  GEOMETRIC_REPRESENTATION_ITEM ( )  RATIONAL_B_SPLINE_CURVE ( ( 0.9999999999999990008, 0.9238795325112877377, 1.000000000000000000, 0.9238795325112867385, 1.000000000000000000, 0.9238795325112867385, 1.000000000000000000, 0.9238795325112874046, 0.9999999999999993339 ) ) 
 REPRESENTATION_ITEM ( '' )  );
#28593=CARTESIAN_POINT ( 'NONE',  ( 7.999999999732929190, -6.536825277765295045E-05, 6.267800880277100362 ) ) ;
#28598=CARTESIAN_POINT ( 'NONE',  ( 2.977408999572646486, 7.188101187499991163, 8.517802781871754547 ) ) ;
#28614=EDGE_CURVE ( 'NONE', #65370, #2593, #15671, .T. ) ;
#28623=CARTESIAN_POINT ( 'NONE',  ( 1.320432766682872962E-15, -7.188101187499992051, 8.236552781871752771 ) ) ;
#28636=CARTESIAN_POINT ( 'NONE',  ( 1.469576158976822172E-15, -7.999999999999991118, 2.705302779823365533 ) ) ;
#28651=CARTESIAN_POINT ( 'NONE',  ( -7.999999999999991118, 0.000000000000000000, 3.886552784329822874 ) ) ;
#28655=ORIENTED_EDGE ( 'NONE', *, *, #25141, .F. ) ;
#28657=CARTESIAN_POINT ( 'NONE',  ( -5.082755093536319713, 5.082755093536319713, 28.29905278187175810 ) ) ;
#28669=CARTESIAN_POINT ( 'NONE',  ( -5.656854249492375253, 5.656854249492375253, 21.83030278392014623 ) ) ;
#28672=CARTESIAN_POINT ( 'NONE',  ( -5.656854249492375253, 5.656854249492375253, 9.830302783920146226 ) ) ;
#28679=CARTESIAN_POINT ( 'NONE',  ( 1.320432766682872962E-15, -7.188101187499992051, 0.3615527818717524378 ) ) ;
#28693=CARTESIAN_POINT ( 'NONE',  ( -2.977408999572648707, -7.188101187499990274, 8.142802781871750994 ) ) ;
#28702=FACE_OUTER_BOUND ( 'NONE', #7619, .T. ) ;
#28716=CARTESIAN_POINT ( 'NONE',  ( 7.999999999999991118, 9.797174393178815797E-16, 18.08030277982336642 ) ) ;
#28721=CARTESIAN_POINT ( 'NONE',  ( -3.313708498984757167, 7.999999999999991118, 21.54905277982336287 ) ) ;
#28733=CARTESIAN_POINT ( 'NONE',  ( 7.999999999999991118, 3.313708498984757611, 21.23030278432982954 ) ) ;
#28768=CARTESIAN_POINT ( 'NONE',  ( -7.188101187499992051, 0.000000000000000000, 16.48655278187175810 ) ) ;
#28781=ORIENTED_EDGE ( 'NONE', *, *, #28614, .T. ) ;
#28784=AXIS2_PLACEMENT_3D ( 'NONE', #37697, #36207, #30542 ) ;
#28793=CARTESIAN_POINT ( 'NONE',  ( -2.977408999572647819, 7.188101187499992051, 18.08030278187175455 ) ) ;
#28812=CARTESIAN_POINT ( 'NONE',  ( -3.313708498984758943, -7.999999999999989342, 5.611552779823364645 ) ) ;
#28839=CARTESIAN_POINT ( 'NONE',  ( -4.898587196589407898E-16, 7.999999999999991118, 8.142802783920144449 ) ) ;
#28840=CARTESIAN_POINT ( 'NONE',  ( -8.008118988124989457, -3.317071493978883900, 14.60686528394063011 ) ) ;
#28846=CARTESIAN_POINT ( 'NONE',  ( 7.188101187499992051, 2.977408999572647819, 14.33030278187175277 ) ) ;
#28852=EDGE_CURVE ( 'NONE', #3504, #4422, #7515, .T. ) ;
#28861=CARTESIAN_POINT ( 'NONE',  ( -5.656854249492375253, 5.656854249492375253, 9.830302783920146226 ) ) ;
#28876=CARTESIAN_POINT ( 'NONE',  ( 7.188101187499991163, 2.977408999572648707, 19.20530278187175810 ) ) ;
#28885=CARTESIAN_POINT ( 'NONE',  ( 7.999999999999992895, -3.313708498984756279, 4.486552779823363757 ) ) ;
#28888=CARTESIAN_POINT ( 'NONE',  ( 5.656854249492374365, 5.656854249492375253, 27.45530278392014978 ) ) ;
#28904=CARTESIAN_POINT ( 'NONE',  ( -7.999999999999991118, 3.313708498984756723, 18.73655277982336642 ) ) ;
#28905=CARTESIAN_POINT ( 'NONE',  ( 3.459103461385761413, -7.213501455148458419, -0.0001169852011744028255 ) ) ;
#28925=CARTESIAN_POINT ( 'NONE',  ( 5.656854249492374365, 5.656854249492375253, 13.95530278392014623 ) ) ;
#28941=CARTESIAN_POINT ( 'NONE',  ( -5.656854249492375253, 5.656854249492375253, 11.33030278392014445 ) ) ;
#28971=CARTESIAN_POINT ( 'NONE',  ( 5.082755093536320601, -5.082755093536318824, 6.549052781871754547 ) ) ;
#28973=VERTEX_POINT ( 'NONE', #67716 ) ;
#28997=CARTESIAN_POINT ( 'NONE',  ( -7.188101187499990274, -2.977408999572651371, 7.955302781871752771 ) ) ;
#29000=CARTESIAN_POINT ( 'NONE',  ( -4.898587196589407898E-16, 7.999999999999991118, 0.5115527843298234290 ) ) ;
#29010=CARTESIAN_POINT ( 'NONE',  ( 7.999999999999991118, 3.313708498984757611, 6.174052779823364645 ) ) ;
#29026=CARTESIAN_POINT ( 'NONE',  ( 3.313708498984756279, 7.999999999999991118, 7.917802784329823318 ) ) ;
#29034=CARTESIAN_POINT ( 'NONE',  ( 2.977408999572650927, -7.188101187499990274, 24.45530278187175810 ) ) ;
#29046=CARTESIAN_POINT ( 'NONE',  ( 7.999999999999991118, 3.313708498984757611, 18.36155278392014623 ) ) ;
#29054=VERTEX_POINT ( 'NONE', #50349 ) ;
#29058=CARTESIAN_POINT ( 'NONE',  ( 7.188101187499991163, 2.977408999572648707, 21.83030278187175810 ) ) ;
#29073=CARTESIAN_POINT ( 'NONE',  ( -2.977408999572648707, -7.188101187499990274, 0.6428027818717528818 ) ) ;
#29077=CARTESIAN_POINT ( 'NONE',  ( -4.903558642999205574E-16, 8.008118988124991233, 5.138115283940630107 ) ) ;
#29084=CARTESIAN_POINT ( 'NONE',  ( 2.977408999572646486, 7.188101187499991163, 25.39280278187176165 ) ) ;
#29103=CARTESIAN_POINT ( 'NONE',  ( -7.999999999999991118, 3.313708498984756723, 21.73655277982336287 ) ) ;
#29116=CARTESIAN_POINT ( 'NONE',  ( -7.999999999999989342, -3.313708498984762496, 24.98030278432982598 ) ) ;
#29130=VERTEX_POINT ( 'NONE', #55663 ) ;
#29141=CARTESIAN_POINT ( 'NONE',  ( 7.999991080290834056, 3.313717418693915562, 12.36155314080052214 ) ) ;
#29142=ORIENTED_EDGE ( 'NONE', *, *, #18006, .T. ) ;
#29150=CARTESIAN_POINT ( 'NONE',  ( -5.082755093536317936, -5.082755093536320601, 15.17405278187175455 ) ) ;
#29176=CARTESIAN_POINT ( 'NONE',  ( -2.977408999572647819, -7.188101187499990274, 14.14280278187175455 ) ) ;
#29197=CARTESIAN_POINT ( 'NONE',  ( 7.999999999999991118, 3.313708498984757611, 1.674052779823364423 ) ) ;
#29222=CARTESIAN_POINT ( 'NONE',  ( -8.008118988124989457, -3.317071493978883900, 11.60686528394062833 ) ) ;
#29229=CARTESIAN_POINT ( 'NONE',  ( 7.188101187499992051, 2.977408999572647819, 11.33030278187175455 ) ) ;
#29236=ORIENTED_EDGE ( 'NONE', *, *, #37866, .F. ) ;
#29244=CARTESIAN_POINT ( 'NONE',  ( -5.656854249492375253, 5.656854249492375253, 8.330302783920144449 ) ) ;
#29255=ORIENTED_EDGE ( 'NONE', *, *, #43779, .T. ) ;
#29256=EDGE_CURVE ( 'NONE', #65370, #9404, #25339, .T. ) ;
#29259=CARTESIAN_POINT ( 'NONE',  ( -7.188101187499990274, -2.977408999572651371, 15.45530278187175455 ) ) ;
#29278=CARTESIAN_POINT ( 'NONE',  ( 0.000000000000000000, 0.000000000000000000, 0.000000000000000000 ) ) ;
#29279=DIRECTION ( 'NONE',  ( -0.000000000000000000, -0.000000000000000000, 1.000000000000000000 ) ) ;
#29286=CARTESIAN_POINT ( 'NONE',  ( 7.999999999999991118, 9.797174393178815797E-16, 22.58030277982336997 ) ) ;
#29304=CARTESIAN_POINT ( 'NONE',  ( -3.313708498984757167, 7.999999999999991118, 8.236552783920144449 ) ) ;
#29319=CARTESIAN_POINT ( 'NONE',  ( -1.512640440460914449E-15, 7.999999999999991118, 29.33030277982336642 ) ) ;
#29355=CARTESIAN_POINT ( 'NONE',  ( 2.977408999572650927, -7.188101187499990274, 6.455302781871754547 ) ) ;
#29367=CARTESIAN_POINT ( 'NONE',  ( 0.000000000000000000, 0.000000000000000000, 30.00000000000000000 ) ) ;
#29380=CARTESIAN_POINT ( 'NONE',  ( 7.188101187499992051, 8.802885111219154394E-16, 7.111552781871754547 ) ) ;
#29385=CARTESIAN_POINT ( 'NONE',  ( 5.656854249492376141, -5.656854249492374365, 7.580302783920144449 ) ) ;
#29391=DIRECTION ( 'NONE',  ( -0.000000000000000000, -0.000000000000000000, 1.000000000000000000 ) ) ;
#29394=CARTESIAN_POINT ( 'NONE',  ( -3.313708498984758943, -7.999999999999989342, 23.79905278392014978 ) ) ;
#29402=ORIENTED_EDGE ( 'NONE', *, *, #47295, .F. ) ;
#29423=CARTESIAN_POINT ( 'NONE',  ( -7.999999999999989342, -3.313708498984762496, 22.11155278392014623 ) ) ;
#29432=CARTESIAN_POINT ( 'NONE',  ( 2.977408999572650927, -7.188101187499990274, 24.45530278187175455 ) ) ;
#29445=CARTESIAN_POINT ( 'NONE',  ( 5.082755093536318824, 5.082755093536319713, 1.299052781871753215 ) ) ;
#29450=AXIS2_PLACEMENT_3D ( 'NONE', #7154, #35827, #64121 ) ;
#29451=CARTESIAN_POINT ( 'NONE',  ( -4.903558642999205574E-16, 8.008118988124991233, 2.138115283940627442 ) ) ;
#29458=CARTESIAN_POINT ( 'NONE',  ( 2.977408999572650927, -7.188101187499990274, 27.83030278187176165 ) ) ;
#29475=CARTESIAN_POINT ( 'NONE',  ( 1.469576158976822172E-15, -7.999999999999991118, 22.20530277982336997 ) ) ;
#29489=CARTESIAN_POINT ( 'NONE',  ( 3.313708498984762496, -7.999999999999989342, 25.35530278432982598 ) ) ;
#29494=ORIENTED_EDGE ( 'NONE', *, *, #13304, .T. ) ;
#29504=ORIENTED_EDGE ( 'NONE', *, *, #25141, .T. ) ;
#29521=CARTESIAN_POINT ( 'NONE',  ( -2.977408999572647819, 7.188101187499991163, 10.20530278187175455 ) ) ;
#29538=CARTESIAN_POINT ( 'NONE',  ( 5.656854249492374365, 5.656854249492375253, 25.95530278392014623 ) ) ;
#29543=CARTESIAN_POINT ( 'NONE',  ( 7.188101187499993827, -2.977408999572645598, 11.51780278187175632 ) ) ;
#29568=( BOUNDED_CURVE ( )  B_SPLINE_CURVE ( 2, ( #8552, #60226, #49661, #31566, #21721, #72292, #20981, #54961, #71914 ),
 .UNSPECIFIED., .F., .F. ) 
 B_SPLINE_CURVE_WITH_KNOTS ( ( 3, 2, 2, 2, 3 ),
 ( 0.4235696451107979765, 0.4301879129896927778, 0.4368061885741496009, 0.4434244641586063684, 0.4500427433262104704 ),
 .UNSPECIFIED. ) 
 CURVE ( )  GEOMETRIC_REPRESENTATION_ITEM ( )  RATIONAL_B_SPLINE_CURVE ( ( 1.000000000000000000, 0.9238795325112867385, 1.000000000000000000, 0.9238795325112867385, 1.000000000000000000, 0.9238795325112867385, 1.000000000000000000, 0.9238795325112867385, 1.000000000000000000 ) ) 
 REPRESENTATION_ITEM ( '' )  );
#29590=CARTESIAN_POINT ( 'NONE',  ( -4.903558642999205574E-16, 8.008118988124991233, 17.13811528394063544 ) ) ;
#29597=CARTESIAN_POINT ( 'NONE',  ( -4.401442555609577197E-16, 7.188101187499992051, 7.111552781871751883 ) ) ;
#29611=CARTESIAN_POINT ( 'NONE',  ( 3.313708498984756279, 7.999999999999991118, 3.549052783920144893 ) ) ;
#29626=CARTESIAN_POINT ( 'NONE',  ( -5.082755093536319713, 5.082755093536319713, 19.67405278187175455 ) ) ;
#29630=CARTESIAN_POINT ( 'NONE',  ( 7.999999999999991118, -2.975320552349488356E-08, 19.76780278304987348 ) ) ;
#29634=CARTESIAN_POINT ( 'NONE',  ( 1.469576158976822172E-15, -7.999999999999991118, 4.205302779823362869 ) ) ;
#29649=CARTESIAN_POINT ( 'NONE',  ( 7.999999999999991118, 9.797174393178815797E-16, 18.08030277982336642 ) ) ;
#29667=CARTESIAN_POINT ( 'NONE',  ( -7.999999999999989342, -3.313708498984762496, 8.611552783920146226 ) ) ;
#29691=( BOUNDED_CURVE ( )  B_SPLINE_CURVE ( 2, ( #3181, #49187, #72197, #27672, #32229, #15228, #60513, #14849, #26926 ),
 .UNSPECIFIED., .F., .F. ) 
 B_SPLINE_CURVE_WITH_KNOTS ( ( 3, 2, 2, 2, 3 ),
 ( 0.2368421052631578261, 0.2434210526315789269, 0.2499999999999999722, 0.2565789473684210731, 0.2631578947368420907 ),
 .UNSPECIFIED. ) 
 CURVE ( )  GEOMETRIC_REPRESENTATION_ITEM ( )  RATIONAL_B_SPLINE_CURVE ( ( 1.000000000000000666, 0.9238795325112860723, 1.000000000000000000, 0.9238795325112867385, 1.000000000000000000, 0.9238795325112867385, 1.000000000000000000, 0.9238795325112867385, 1.000000000000000000 ) ) 
 REPRESENTATION_ITEM ( '' )  );
#29719=CARTESIAN_POINT ( 'NONE',  ( 2.977408999572646486, 7.188101187499991163, 7.017802781871751883 ) ) ;
#29728=ORIENTED_EDGE ( 'NONE', *, *, #10946, .T. ) ;
#29740=CARTESIAN_POINT ( 'NONE',  ( -5.082755093536317936, -5.082755093536320601, 11.04905278187175455 ) ) ;
#29743=CARTESIAN_POINT ( 'NONE',  ( 7.999999999999992895, -3.313708498984756279, 3.042802784329822430 ) ) ;
#29745=CARTESIAN_POINT ( 'NONE',  ( -7.999999999999991118, 0.000000000000000000, 7.017802783920144449 ) ) ;
#29753=CARTESIAN_POINT ( 'NONE',  ( -4.898587196589407898E-16, 7.999999999999991118, 23.14280278392014978 ) ) ;
#29765=CARTESIAN_POINT ( 'NONE',  ( -6.062591786044946751, -5.219672483564715471, -0.3118205092643556720 ) ) ;
#29776=CARTESIAN_POINT ( 'NONE',  ( -2.977408999572647819, 7.188101187499992051, 26.70530278187175455 ) ) ;
#29790=CARTESIAN_POINT ( 'NONE',  ( -5.656854249492373476, -5.656854249492376141, 19.20530278392014978 ) ) ;
#29799=CARTESIAN_POINT ( 'NONE',  ( 7.188101187499993827, -2.977408999572645598, 27.64280278187175810 ) ) ;
#29814=CARTESIAN_POINT ( 'NONE',  ( -5.272366635369878374, -4.893143551702760163, 0.5406094755204297053 ) ) ;
#29818=CARTESIAN_POINT ( 'NONE',  ( 8.008118988124991233, 3.317071493978879015, 3.356865283940628331 ) ) ;
#29843=CARTESIAN_POINT ( 'NONE',  ( -5.656854249492373476, -5.656854249492376141, 17.51780277982336287 ) ) ;
#29859=CARTESIAN_POINT ( 'NONE',  ( 5.656854249492374365, 5.656854249492375253, 18.32405278432982243 ) ) ;
#29876=VECTOR ( 'NONE', #56869, 1000.000000000000000 ) ;
#29890=CARTESIAN_POINT ( 'NONE',  ( 7.188101187499991163, 2.977408999572648707, 12.83030278187175277 ) ) ;
#29912=CARTESIAN_POINT ( 'NONE',  ( 5.082755093536318824, 5.082755093536319713, 8.799052781871752771 ) ) ;
#29946=LINE ( 'NONE', #6201, #73559 ) ;
#29960=CARTESIAN_POINT ( 'NONE',  ( -5.662595241051933570, -5.662595241051936235, 13.20061528394063011 ) ) ;
#29965=CARTESIAN_POINT ( 'NONE',  ( 7.188101187499993827, -2.977408999572645598, 8.142802781871752771 ) ) ;
#29977=CARTESIAN_POINT ( 'NONE',  ( 5.656854249492374365, 5.656854249492375253, 3.455302783920144449 ) ) ;
#29995=CARTESIAN_POINT ( 'NONE',  ( -7.188101187499990274, -2.977408999572651371, 16.95530278187175455 ) ) ;
#30003=CARTESIAN_POINT ( 'NONE',  ( 5.656854249492376141, -5.656854249492374365, 5.892802779823364645 ) ) ;
#30005=CARTESIAN_POINT ( 'NONE',  ( -2.977408999572647819, 7.188101187499992051, 27.08030278187175810 ) ) ;
#30016=CARTESIAN_POINT ( 'NONE',  ( -3.295887129531270165, -7.292874925529289065, -0.000000000000000000 ) ) ;
#30017=DIRECTION ( 'NONE',  ( 1.000000000000000000, 0.000000000000000000, 0.000000000000000000 ) ) ;
#30022=CARTESIAN_POINT ( 'NONE',  ( 7.999999999999992895, -3.313708498984756279, 17.98655277982336642 ) ) ;
#30038=ADVANCED_FACE ( 'NONE', ( #17204 ), #64352, .F. ) ;
#30039=CARTESIAN_POINT ( 'NONE',  ( 3.313708498984756279, 7.999999999999991118, 8.049052783920146226 ) ) ;
#30085=CARTESIAN_POINT ( 'NONE',  ( -5.082755093536319713, 5.082755093536319713, 4.299052781871752771 ) ) ;
#30112=CARTESIAN_POINT ( 'NONE',  ( -7.188101187499991163, 2.977408999572646930, 3.267802781871751439 ) ) ;
#30125=EDGE_CURVE ( 'NONE', #71597, #70510, #6650, .T. ) ;
#30126=CARTESIAN_POINT ( 'NONE',  ( 1.469576158976822172E-15, -7.999999999999991118, 23.89280278392014978 ) ) ;
#30143=CARTESIAN_POINT ( 'NONE',  ( -3.313708498984759387, -7.999999999999989342, 11.79905278392014623 ) ) ;
#30148=CARTESIAN_POINT ( 'NONE',  ( 5.082755093536320601, -5.082755093536318824, 24.54905278187175810 ) ) ;
#30149=VECTOR ( 'NONE', #72875, 1000.000000000000000 ) ;
#30155=CARTESIAN_POINT ( 'NONE',  ( 5.656854249492374365, 5.656854249492375253, 18.45530278392014623 ) ) ;
#30167=CARTESIAN_POINT ( 'NONE',  ( -5.082755093536319713, 5.082755093536319713, 26.79905278187175455 ) ) ;
#30180=CARTESIAN_POINT ( 'NONE',  ( -7.999999999999991118, 0.000000000000000000, 15.83030277982336642 ) ) ;
#30185=CARTESIAN_POINT ( 'NONE',  ( 1.471067592899761672E-15, -8.008118988124991233, 1.388115283940630107 ) ) ;
#30192=CARTESIAN_POINT ( 'NONE',  ( -5.082755093536319713, 5.082755093536319713, 22.67405278187175455 ) ) ;
#30208=CARTESIAN_POINT ( 'NONE',  ( -5.656854249492375253, 5.656854249492375253, 14.14280277982336465 ) ) ;
#30224=CARTESIAN_POINT ( 'NONE',  ( 3.313708498984756279, 7.999999999999991118, 16.91780278432982243 ) ) ;
#30259=CARTESIAN_POINT ( 'NONE',  ( 7.188101187499993827, -2.977408999572645598, 12.64280278187175277 ) ) ;
#30281=CARTESIAN_POINT ( 'NONE',  ( 7.188101187499993827, -2.977408999572645598, 10.01780278187175632 ) ) ;
#30286=CARTESIAN_POINT ( 'NONE',  ( -7.999999999999989342, -1.759397900368767025E-05, 4.017803281681348260 ) ) ;
#30305=VERTEX_POINT ( 'NONE', #68067 ) ;
#30316=CIRCLE ( 'NONE', #47153, 7.999999999999991118 ) ;
#30324=CARTESIAN_POINT ( 'NONE',  ( -8.000000000000033751, -3.313708498984719864, 12.92405277982336465 ) ) ;
#30326=CARTESIAN_POINT ( 'NONE',  ( -3.317071493978880348, -8.008118988124989457, 13.29436528394063011 ) ) ;
#30332=CARTESIAN_POINT ( 'NONE',  ( 7.188101187499992051, 8.802885111219154394E-16, 11.23655278187175455 ) ) ;
#30346=CARTESIAN_POINT ( 'NONE',  ( 5.656854249492374365, 5.656854249492375253, 0.4553027839201452265 ) ) ;
#30362=CARTESIAN_POINT ( 'NONE',  ( -2.977408999572648707, -7.188101187499990274, 14.14280278187175455 ) ) ;
#30365=CARTESIAN_POINT ( 'NONE',  ( -3.313708498984757611, 7.999999999999991118, 3.549052779823362425 ) ) ;
#30384=FACE_OUTER_BOUND ( 'NONE', #62257, .T. ) ;
#30389=CARTESIAN_POINT ( 'NONE',  ( 3.313708498984762496, -7.999999999999989342, 13.48655278392014623 ) ) ;
#30390=CARTESIAN_POINT ( 'NONE',  ( -7.999999999999991118, 0.000000000000000000, 12.83030277982336465 ) ) ;
#30457=CARTESIAN_POINT ( 'NONE',  ( 2.977408999572650927, -7.188101187499990274, 3.455302781871751439 ) ) ;
#30480=CARTESIAN_POINT ( 'NONE',  ( -5.082755093536317936, -5.082755093536320601, 6.549052781871754547 ) ) ;
#30494=CARTESIAN_POINT ( 'NONE',  ( 7.999999999999992895, -3.313708498984756279, 22.67405278392015333 ) ) ;
#30514=CARTESIAN_POINT ( 'NONE',  ( -7.188101187499990274, -2.977408999572651815, 21.08030278187175810 ) ) ;
#30525=CARTESIAN_POINT ( 'NONE',  ( -5.656854249492375253, 5.656854249492375253, 15.83030278392014800 ) ) ;
#30535=ORIENTED_EDGE ( 'NONE', *, *, #11317, .F. ) ;
#30538=CARTESIAN_POINT ( 'NONE',  ( -7.188101187499991163, 2.977408999572646930, 25.39280278187176165 ) ) ;
#30542=DIRECTION ( 'NONE',  ( 1.000000000000000000, 0.000000000000000000, 0.000000000000000000 ) ) ;
#30556=CARTESIAN_POINT ( 'NONE',  ( -8.008118988124989457, -3.317071493978883900, 4.106865283940629219 ) ) ;
#30562=CARTESIAN_POINT ( 'NONE',  ( 7.188101187499992051, 8.802885111219154394E-16, 20.61155278187175455 ) ) ;
#30577=CARTESIAN_POINT ( 'NONE',  ( 5.656854249492376141, -5.656854249492374365, 13.39280277982336465 ) ) ;
#30592=CARTESIAN_POINT ( 'NONE',  ( 1.469576158976822172E-15, -7.999999999999991118, 17.76155278432982243 ) ) ;
#30624=CARTESIAN_POINT ( 'NONE',  ( 7.188101187499992051, 8.802885111219154394E-16, 14.23655278187175455 ) ) ;
#30625=ORIENTED_EDGE ( 'NONE', *, *, #65422, .T. ) ;
#30648=CARTESIAN_POINT ( 'NONE',  ( 7.188101187499992051, 2.977408999572647819, 13.20530278187175277 ) ) ;
#30650=DIRECTION ( 'NONE',  ( -0.000000000000000000, -0.000000000000000000, 1.000000000000000000 ) ) ;
#30652=DIRECTION ( 'NONE',  ( -0.000000000000000000, -0.000000000000000000, 1.000000000000000000 ) ) ;
#30684=CARTESIAN_POINT ( 'NONE',  ( 0.000000000000000000, 0.000000000000000000, 30.00000000000000000 ) ) ;
#30695=CARTESIAN_POINT ( 'NONE',  ( 5.662595241051936235, -5.662595241051934458, 10.57561528394063188 ) ) ;
#30700=CARTESIAN_POINT ( 'NONE',  ( 2.977408999572650927, -7.188101187499990274, 6.455302781871754547 ) ) ;
#30709=EDGE_CURVE ( 'NONE', #35470, #46714, #61506, .T. ) ;
#30713=CARTESIAN_POINT ( 'NONE',  ( 7.999999999999991118, 9.797174393178815797E-16, 1.767802783920142895 ) ) ;
#30738=CARTESIAN_POINT ( 'NONE',  ( -7.188101187499992051, 2.977408999572646930, 28.76780278187175810 ) ) ;
#30755=CARTESIAN_POINT ( 'NONE',  ( 1.469576158976822172E-15, -7.999999999999991118, 14.70530277982336642 ) ) ;
#30782=EDGE_CURVE ( 'NONE', #27089, #55503, #49882, .T. ) ;
#30786=CARTESIAN_POINT ( 'NONE',  ( -5.662595241051935346, 5.662595241051935346, 24.82561528394063544 ) ) ;
#30804=DIRECTION ( 'NONE',  ( 0.000000000000000000, 0.2588190451025145777, -0.9659258262890699775 ) ) ;
#30817=CARTESIAN_POINT ( 'NONE',  ( -2.977408999572648707, -7.188101187499990274, 0.2678027818717523822 ) ) ;
#30842=CARTESIAN_POINT ( 'NONE',  ( -7.188101187499991163, 2.977408999572646930, 1.767802781871753881 ) ) ;
#30859=CARTESIAN_POINT ( 'NONE',  ( -5.656854249492375253, 5.656854249492375253, 24.83030278392014978 ) ) ;
#30881=CARTESIAN_POINT ( 'NONE',  ( -7.188101187499992051, 2.977408999572646930, 19.39280278187176165 ) ) ;
#30883=CARTESIAN_POINT ( 'NONE',  ( 7.999999999842164478, 5.025161467855852442E-05, 22.76780420562571905 ) ) ;
#30890=CARTESIAN_POINT ( 'NONE',  ( -7.999999999999989342, -3.313708498984762496, 11.61155278392014445 ) ) ;
#30893=VERTEX_POINT ( 'NONE', #4613 ) ;
#30901=CARTESIAN_POINT ( 'NONE',  ( -2.977408999572648707, -7.188101187499990274, 21.26780278187175810 ) ) ;
#30913=CARTESIAN_POINT ( 'NONE',  ( -7.999999999999968914, 3.313708498984778039, 15.73655277982336287 ) ) ;
#30917=CARTESIAN_POINT ( 'NONE',  ( 7.999999999999991118, 9.797174393178815797E-16, 25.76780278392014978 ) ) ;
#30923=CARTESIAN_POINT ( 'NONE',  ( 2.977408999572650927, -7.188101187499990274, 20.33030278187175455 ) ) ;
#30932=CARTESIAN_POINT ( 'NONE',  ( 3.313708498984756279, 7.999999999999991118, 18.36155277982337353 ) ) ;
#30942=CARTESIAN_POINT ( 'NONE',  ( 7.999999999999992895, -3.313708498984756279, 17.98655277982336642 ) ) ;
#30957=CARTESIAN_POINT ( 'NONE',  ( 5.656854249492374365, 5.656854249492375253, 15.32405278432982421 ) ) ;
#30989=CARTESIAN_POINT ( 'NONE',  ( 5.082755093536318824, 5.082755093536319713, 6.924052781871750994 ) ) ;
#31011=CARTESIAN_POINT ( 'NONE',  ( 5.082755093536318824, 5.082755093536319713, 13.29905278187175277 ) ) ;
#31035=CARTESIAN_POINT ( 'NONE',  ( 7.999999999999983125, -3.313708498984766493, 23.98655277982336287 ) ) ;
#31053=CARTESIAN_POINT ( 'NONE',  ( -3.313708498984759387, -7.999999999999989342, 13.11155277982336465 ) ) ;
#31055=CARTESIAN_POINT ( 'NONE',  ( -3.317071493978878571, 8.008118988124991233, 9.731865283940631883 ) ) ;
#31060=CARTESIAN_POINT ( 'NONE',  ( -2.977408999572647819, -7.188101187499990274, 1.767802781871753437 ) ) ;
#31073=CARTESIAN_POINT ( 'NONE',  ( -5.656854249492373476, -5.656854249492376141, 2.705302783920143561 ) ) ;
#31087=VERTEX_POINT ( 'NONE', #66281 ) ;
#31092=CARTESIAN_POINT ( 'NONE',  ( -7.999999999999991118, 3.313708498984757167, 2.424052783920144005 ) ) ;
#31096=CARTESIAN_POINT ( 'NONE',  ( -5.656854249492373476, -5.656854249492376141, 5.517802779823364645 ) ) ;
#31100=CARTESIAN_POINT ( 'NONE',  ( 0.000000000000000000, 0.000000000000000000, 30.00000000000000000 ) ) ;
#31120=CARTESIAN_POINT ( 'NONE',  ( -3.313708498984757167, 7.999999999999991118, 12.54905277982336287 ) ) ;
#31130=LINE ( 'NONE', #42447, #56181 ) ;
#31150=CARTESIAN_POINT ( 'NONE',  ( -5.662595241051933570, -5.662595241051936235, 26.70061528394063188 ) ) ;
#31188=CARTESIAN_POINT ( 'NONE',  ( -7.188101187499991163, 2.977408999572646930, 1.392802781871753437 ) ) ;
#31214=CARTESIAN_POINT ( 'NONE',  ( -5.082755093536317936, -5.082755093536320601, 5.049052781871752771 ) ) ;
#31231=CARTESIAN_POINT ( 'NONE',  ( 3.313708498984756279, 7.999999999999991118, 20.04905278392014978 ) ) ;
#31248=CARTESIAN_POINT ( 'NONE',  ( -7.999999999999015010, 2.678670460604446806E-06, 11.51770387648012317 ) ) ;
#31251=CARTESIAN_POINT ( 'NONE',  ( 2.977408999572650927, -7.188101187499990274, 18.45530278187175455 ) ) ;
#31259=CARTESIAN_POINT ( 'NONE',  ( -7.999999999999991118, 0.000000000000000000, 14.51780278392014800 ) ) ;
#31271=CARTESIAN_POINT ( 'NONE',  ( 7.188101187499991163, 2.977408999572648707, 17.33030278187175455 ) ) ;
#31274=ORIENTED_EDGE ( 'NONE', *, *, #28326, .F. ) ;
#31277=CARTESIAN_POINT ( 'NONE',  ( 1.469576158976822172E-15, -7.999999999999991118, 5.892802783920146226 ) ) ;
#31288=CARTESIAN_POINT ( 'NONE',  ( 5.656854249492376141, -5.656854249492374365, 24.08030278392014978 ) ) ;
#31294=CARTESIAN_POINT ( 'NONE',  ( 2.977408999572646486, 7.188101187499991163, 23.89280278187176165 ) ) ;
#31312=CARTESIAN_POINT ( 'NONE',  ( -5.656854249492373476, -5.656854249492376141, 16.01780277982336642 ) ) ;
#31327=CARTESIAN_POINT ( 'NONE',  ( -7.999999999999991118, 0.000000000000000000, 20.38655278432982243 ) ) ;
#31338=VERTEX_POINT ( 'NONE', #20653 ) ;
#31346=EDGE_CURVE ( 'NONE', #3963, #60631, #42522, .T. ) ;
#31355=CARTESIAN_POINT ( 'NONE',  ( 0.000000000000000000, 0.000000000000000000, 30.00000000000000000 ) ) ;
#31362=CARTESIAN_POINT ( 'NONE',  ( -5.082755093536317936, -5.082755093536320601, 6.174052781871754547 ) ) ;
#31367=CIRCLE ( 'NONE', #17057, 7.999999999999991118 ) ;
#31387=CARTESIAN_POINT ( 'NONE',  ( 5.082755093536320601, -5.082755093536318824, 5.424052781871753659 ) ) ;
#31410=ORIENTED_EDGE ( 'NONE', *, *, #19987, .F. ) ;
#31415=CARTESIAN_POINT ( 'NONE',  ( 5.656854249492374365, 5.656854249492375253, 7.955302783920145338 ) ) ;
#31434=CARTESIAN_POINT ( 'NONE',  ( 3.317071493978883456, -8.008118988124989457, 7.481865283940628331 ) ) ;
#31442=CARTESIAN_POINT ( 'NONE',  ( 5.082755093536320601, -5.082755093536318824, 5.049052781871752771 ) ) ;
#31450=ADVANCED_FACE ( 'NONE', ( #1656 ), #40897, .F. ) ;
#31457=CARTESIAN_POINT ( 'NONE',  ( 7.188101187499991163, 2.977408999572648707, 24.83030278187175455 ) ) ;
#31460=ORIENTED_EDGE ( 'NONE', *, *, #32578, .T. ) ;
#31476=CARTESIAN_POINT ( 'NONE',  ( 7.999999999999992895, -2.501763238865420012E-05, 24.26780207613217399 ) ) ;
#31482=CARTESIAN_POINT ( 'NONE',  ( -7.188101187499992051, 2.977408999572646930, 22.76780278187175455 ) ) ;
#31501=CARTESIAN_POINT ( 'NONE',  ( -3.313708498984758943, -7.999999999999989342, 11.61155277982336820 ) ) ;
#31503=CARTESIAN_POINT ( 'NONE',  ( -7.999999999970034636, -1.442163225726577833E-05, 17.51834960462420909 ) ) ;
#31544=ORIENTED_EDGE ( 'NONE', *, *, #54813, .F. ) ;
#31550=VERTEX_POINT ( 'NONE', #34888 ) ;
#31558=EDGE_CURVE ( 'NONE', #1239, #22615, #29946, .T. ) ;
#31564=CARTESIAN_POINT ( 'NONE',  ( -4.401442555609577197E-16, 7.188101187499992051, 28.48655278187175810 ) ) ;
#31566=CARTESIAN_POINT ( 'NONE',  ( -3.313708498984757611, 7.999999999999991118, 15.73655278392014623 ) ) ;
#31591=CARTESIAN_POINT ( 'NONE',  ( -7.188101187499991163, 2.977408999572646930, 4.767802781871753659 ) ) ;
#31592=CYLINDRICAL_SURFACE ( 'NONE', #58030, 7.999999999999991118 ) ;
#31606=CARTESIAN_POINT ( 'NONE',  ( -7.999999999999989342, -3.313708498984762496, 17.61155278392014623 ) ) ;
#31607=CARTESIAN_POINT ( 'NONE',  ( 0.000000000000000000, 0.000000000000000000, 30.00000000000000000 ) ) ;
#31611=DIRECTION ( 'NONE',  ( 0.000000000000000000, 0.000000000000000000, -1.000000000000000000 ) ) ;
#31617=CARTESIAN_POINT ( 'NONE',  ( 7.999999999999992895, -7.224685084787812073E-14, 27.26780278391845513 ) ) ;
#31629=CARTESIAN_POINT ( 'NONE',  ( -2.977408999572647819, 7.188101187499992051, 23.70530278187175455 ) ) ;
#31639=CARTESIAN_POINT ( 'NONE',  ( 5.656854249492376141, -5.656854249492374365, 15.08030278392014623 ) ) ;
#31645=CARTESIAN_POINT ( 'NONE',  ( -5.656854249492375253, 5.656854249492375253, 12.64280277982336287 ) ) ;
#31648=( BOUNDED_CURVE ( )  B_SPLINE_CURVE ( 2, ( #10136, #44469, #44843, #21076, #56172, #4485, #61446, #55051, #26733 ),
 .UNSPECIFIED., .F., .F. ) 
 B_SPLINE_CURVE_WITH_KNOTS ( ( 3, 2, 2, 2, 3 ),
 ( 0.3947368421052632192, 0.4013157894736842923, 0.4078947368421053654, 0.4144736842105264385, 0.4210526315789475116 ),
 .UNSPECIFIED. ) 
 CURVE ( )  GEOMETRIC_REPRESENTATION_ITEM ( )  RATIONAL_B_SPLINE_CURVE ( ( 0.9999999999999993339, 0.9238795325112874046, 1.000000000000000000, 0.9238795325112867385, 1.000000000000000000, 0.9238795325112867385, 1.000000000000000000, 0.9238795325112848511, 1.000000000000001998 ) ) 
 REPRESENTATION_ITEM ( '' )  );
#31652=CARTESIAN_POINT ( 'NONE',  ( -7.188101187499991163, 2.977408999572646930, 19.39280278187176165 ) ) ;
#31671=CARTESIAN_POINT ( 'NONE',  ( 3.317071493978883456, -8.008118988124989457, -0.01813471605937123921 ) ) ;
#31678=CARTESIAN_POINT ( 'NONE',  ( 5.082755093536320601, -5.082755093536318824, 21.92405278187175455 ) ) ;
#31693=CARTESIAN_POINT ( 'NONE',  ( -7.999999999999991118, 0.000000000000000000, 9.830302779823364645 ) ) ;
#31709=CARTESIAN_POINT ( 'NONE',  ( 5.656854249492376141, -5.656854249492374365, 11.94905278432982243 ) ) ;
#31740=CARTESIAN_POINT ( 'NONE',  ( -7.188101187499992051, 0.000000000000000000, 7.486552781871751883 ) ) ;
#31753=CARTESIAN_POINT ( 'NONE',  ( 1.320432766682872962E-15, -7.188101187499992051, 14.23655278187175455 ) ) ;
#31765=CARTESIAN_POINT ( 'NONE',  ( -7.188101187499990274, -2.977408999572651815, 6.455302781871754547 ) ) ;
#31781=CARTESIAN_POINT ( 'NONE',  ( -4.898587196589407898E-16, 7.999999999999991118, 25.95530277982336997 ) ) ;
#31795=CARTESIAN_POINT ( 'NONE',  ( -7.999999999999991118, 0.000000000000000000, 5.517802783920146226 ) ) ;
#31803=ADVANCED_FACE ( 'NONE', ( #72534 ), #43859, .F. ) ;
#31813=CARTESIAN_POINT ( 'NONE',  ( 3.317071493978877683, 8.008118988124991233, 8.044365283940630107 ) ) ;
#31819=CARTESIAN_POINT ( 'NONE',  ( -7.188101187499990274, -2.977408999572651815, 6.080302781871753659 ) ) ;
#31831=CARTESIAN_POINT ( 'NONE',  ( 2.977408999572646486, 7.188101187499991163, 22.01780278187175455 ) ) ;
#31832=ORIENTED_EDGE ( 'NONE', *, *, #47295, .T. ) ;
#31854=CARTESIAN_POINT ( 'NONE',  ( -4.401442555609577197E-16, 7.188101187499992051, 20.98655278187175455 ) ) ;
#31873=CARTESIAN_POINT ( 'NONE',  ( -5.656854249492373476, -5.656854249492376141, 11.51780277982336642 ) ) ;
#31882=CARTESIAN_POINT ( 'NONE',  ( 7.999999999999991118, 3.313708498984758055, 4.861552783920145338 ) ) ;
#31916=CARTESIAN_POINT ( 'NONE',  ( -5.656854249492375253, 5.656854249492375253, 21.64280277982336997 ) ) ;
#31936=CARTESIAN_POINT ( 'NONE',  ( 5.082755093536320601, -5.082755093536318824, 2.049052781871754103 ) ) ;
#31949=DIRECTION ( 'NONE',  ( -0.000000000000000000, -0.000000000000000000, 1.000000000000000000 ) ) ;
#31951=EDGE_CURVE ( 'NONE', #73165, #18628, #58739, .T. ) ;
#31962=CARTESIAN_POINT ( 'NONE',  ( -5.082755093536317936, -5.082755093536320601, 0.5490527818717526598 ) ) ;
#31969=CARTESIAN_POINT ( 'NONE',  ( 5.656854249492376141, -5.656854249492374365, 14.89280277982336642 ) ) ;
#31981=CARTESIAN_POINT ( 'NONE',  ( -5.656854249492375253, 5.656854249492375253, 20.33030278392014623 ) ) ;
#32006=CARTESIAN_POINT ( 'NONE',  ( -5.082755093536319713, 5.082755093536319713, 23.79905278187175455 ) ) ;
#32012=EDGE_CURVE ( 'NONE', #34174, #6758, #39841, .T. ) ;
#32015=CARTESIAN_POINT ( 'NONE',  ( 3.313708498984762496, -7.999999999999989342, 13.48655278392014445 ) ) ;
#32024=ORIENTED_EDGE ( 'NONE', *, *, #31558, .F. ) ;
#32026=CARTESIAN_POINT ( 'NONE',  ( 7.188101187499992051, 8.802885111219154394E-16, 18.73655278187175455 ) ) ;
#32031=CARTESIAN_POINT ( 'NONE',  ( -7.999985423429806453, -3.313723075554945385, 5.611553367133312875 ) ) ;
#32043=CARTESIAN_POINT ( 'NONE',  ( -4.898587196589407898E-16, 7.999999999999991118, 27.64280278392014978 ) ) ;
#32050=CARTESIAN_POINT ( 'NONE',  ( -7.188101187499991163, 2.977408999572646930, 15.26780278187175455 ) ) ;
#32053=EDGE_CURVE ( 'NONE', #8699, #31338, #489, .T. ) ;
#32059=CARTESIAN_POINT ( 'NONE',  ( -4.898587196589407898E-16, 7.999999999999991118, 18.45530277982336642 ) ) ;
#32067=CARTESIAN_POINT ( 'NONE',  ( -3.313708498984757167, 7.999999999999991118, 9.549052779823362869 ) ) ;
#32084=CARTESIAN_POINT ( 'NONE',  ( -7.999999999999989342, -3.313708498984762496, 11.48030278432982243 ) ) ;
#32111=ORIENTED_EDGE ( 'NONE', *, *, #39480, .F. ) ;
#32112=DIRECTION ( 'NONE',  ( -0.000000000000000000, -0.000000000000000000, 1.000000000000000000 ) ) ;
#32117=CARTESIAN_POINT ( 'NONE',  ( 5.082755093536320601, -5.082755093536318824, 5.049052781871752771 ) ) ;
#32131=CARTESIAN_POINT ( 'NONE',  ( -7.188101187499990274, -2.977408999572651371, 9.455302781871754547 ) ) ;
#32143=CARTESIAN_POINT ( 'NONE',  ( 7.188101187499992051, 2.977408999572647819, 5.705302781871753659 ) ) ;
#32159=CARTESIAN_POINT ( 'NONE',  ( -5.656854249492373476, -5.656854249492376141, 25.01780277982336642 ) ) ;
#32172=CARTESIAN_POINT ( 'NONE',  ( 1.469576158976822172E-15, -7.999999999999991118, 2.892802783920144005 ) ) ;
#32195=CARTESIAN_POINT ( 'NONE',  ( -5.082755093536317936, -5.082755093536320601, 1.674052781871753659 ) ) ;
#32197=( BOUNDED_CURVE ( )  B_SPLINE_CURVE ( 2, ( #39040, #4339, #9998, #56030, #54533, #15263, #38675, #66959, #38296, #54907, #9629 ),
 .UNSPECIFIED., .F., .F. ) 
 B_SPLINE_CURVE_WITH_KNOTS ( ( 3, 2, 2, 2, 2, 3 ),
 ( 0.2647310102845484292, 0.2647310233782620981, 0.2713492989627193097, 0.2779675745471765214, 0.2845858501316336775, 0.2912041257482609335 ),
 .UNSPECIFIED. ) 
 CURVE ( )  GEOMETRIC_REPRESENTATION_ITEM ( )  RATIONAL_B_SPLINE_CURVE ( ( 0.9999996988044332902, 0.9999998494019186612, 1.000000000000000000, 0.9238795325112867385, 1.000000000000000000, 0.9238795325112867385, 1.000000000000000000, 0.9238795325112867385, 1.000000000000000000, 0.9238795325112867385, 1.000000000000000000 ) ) 
 REPRESENTATION_ITEM ( '' )  );
#32205=AXIS2_PLACEMENT_3D ( 'NONE', #7736, #69632, #46977 ) ;
#32209=CARTESIAN_POINT ( 'NONE',  ( -5.082755093536319713, 5.082755093536319713, 26.79905278187175455 ) ) ;
#32229=CARTESIAN_POINT ( 'NONE',  ( 1.469576158976822172E-15, -7.999999999999991118, 22.20530277982336997 ) ) ;
#32235=CARTESIAN_POINT ( 'NONE',  ( -2.977408999572647819, -7.188101187499990274, 20.14280278187176165 ) ) ;
#32255=CARTESIAN_POINT ( 'NONE',  ( -7.999999999999989342, -3.313708498984762496, 9.924052779823364645 ) ) ;
#32258=ORIENTED_EDGE ( 'NONE', *, *, #36836, .T. ) ;
#32285=CARTESIAN_POINT ( 'NONE',  ( 8.008118988124991233, 9.807117285998411148E-16, 24.26311528394063188 ) ) ;
#32295=CARTESIAN_POINT ( 'NONE',  ( -4.898587196589407898E-16, 7.999999999999991118, 21.45530277982336642 ) ) ;
#32321=CARTESIAN_POINT ( 'NONE',  ( 7.188101187499992051, 8.802885111219154394E-16, 26.61155278187175810 ) ) ;
#32346=CARTESIAN_POINT ( 'NONE',  ( -2.977408999572648707, -7.188101187499990274, 0.6428027818717528818 ) ) ;
#32363=CARTESIAN_POINT ( 'NONE',  ( -7.999999999999991118, 0.000000000000000000, 19.01780278392014623 ) ) ;
#32378=VECTOR ( 'NONE', #55806, 1000.000000000000000 ) ;
#32384=CARTESIAN_POINT ( 'NONE',  ( 2.977408999572650927, -7.188101187499990274, 15.45530278187175632 ) ) ;
#32385=CARTESIAN_POINT ( 'NONE',  ( 1.469576158976822172E-15, -7.999999999999991118, 16.39280278392014978 ) ) ;
#32394=CARTESIAN_POINT ( 'NONE',  ( 7.999999999999991118, 3.313708498984757611, 7.861552783920145338 ) ) ;
#32395=CARTESIAN_POINT ( 'NONE',  ( -3.313708498984757611, 7.999999999999991118, 18.73655278392014623 ) ) ;
#32407=CARTESIAN_POINT ( 'NONE',  ( 2.977408999572650927, -7.188101187499990274, 21.45530278187175810 ) ) ;
#32426=CARTESIAN_POINT ( 'NONE',  ( 5.656854249492374365, 5.656854249492375253, 24.45530278392014978 ) ) ;
#32433=CARTESIAN_POINT ( 'NONE',  ( 5.082755093536318824, 5.082755093536319713, 13.29905278187175277 ) ) ;
#32450=CARTESIAN_POINT ( 'NONE',  ( -7.999999999999991118, 0.000000000000000000, 6.830302779823365533 ) ) ;
#32451=CARTESIAN_POINT ( 'NONE',  ( 3.313708498984756279, 7.999999999999991118, 21.54905278392014623 ) ) ;
#32467=CARTESIAN_POINT ( 'NONE',  ( -3.313708498984758943, -7.999999999999989342, 13.16780278432982421 ) ) ;
#32499=CARTESIAN_POINT ( 'NONE',  ( 2.977408999572650927, -7.188101187499990274, 9.455302781871754547 ) ) ;
#32511=CARTESIAN_POINT ( 'NONE',  ( -7.188101187499990274, -2.977408999572651371, 13.95530278187175277 ) ) ;
#32523=CARTESIAN_POINT ( 'NONE',  ( 7.999999999999991118, 0.000000000000000000, 30.00000000000000000 ) ) ;
#32526=ADVANCED_FACE ( 'NONE', ( #54415 ), #71737, .F. ) ;
#32527=CARTESIAN_POINT ( 'NONE',  ( -7.188101187499992051, 2.977408999572646930, 6.267802781871754547 ) ) ;
#32533=ORIENTED_EDGE ( 'NONE', *, *, #41485, .F. ) ;
#32543=CARTESIAN_POINT ( 'NONE',  ( -7.999999999999991118, 0.000000000000000000, 26.33030277982336997 ) ) ;
#32555=CARTESIAN_POINT ( 'NONE',  ( 7.999999999999991118, 3.313708498984757611, 27.23030278432983309 ) ) ;
#32561=( BOUNDED_CURVE ( )  B_SPLINE_CURVE ( 2, ( #11077, #23497, #17089, #58233, #34105, #6532, #29538, #57100, #52549 ),
 .UNSPECIFIED., .F., .F. ) 
 B_SPLINE_CURVE_WITH_KNOTS ( ( 3, 2, 2, 2, 3 ),
 ( 0.05294620388485415940, 0.05956448026011130353, 0.06618275584456811966, 0.07280103142902494273, 0.07941930701348173804 ),
 .UNSPECIFIED. ) 
 CURVE ( )  GEOMETRIC_REPRESENTATION_ITEM ( )  RATIONAL_B_SPLINE_CURVE ( ( 1.000000000000000000, 0.9238795325112867385, 1.000000000000000000, 0.9238795325112867385, 1.000000000000000000, 0.9238795325112867385, 1.000000000000000000, 0.9238795325112867385, 1.000000000000000000 ) ) 
 REPRESENTATION_ITEM ( '' )  );
#32577=CARTESIAN_POINT ( 'NONE',  ( -4.401442555609577197E-16, 7.188101187499992051, 2.611552781871750994 ) ) ;
#32578=EDGE_CURVE ( 'NONE', #33233, #51609, #54038, .T. ) ;
#32593=CARTESIAN_POINT ( 'NONE',  ( 2.977408999572646486, 7.188101187499991163, 25.01780278187175455 ) ) ;
#32617=CARTESIAN_POINT ( 'NONE',  ( 7.188101187499992051, 8.802885111219154394E-16, 23.61155278187175455 ) ) ;
#32636=CARTESIAN_POINT ( 'NONE',  ( -5.656854249492373476, -5.656854249492376141, 10.01780277982336465 ) ) ;
#32638=CARTESIAN_POINT ( 'NONE',  ( 7.999999999999992895, 6.888416461457931717E-06, 21.26780297880423021 ) ) ;
#32639=ORIENTED_EDGE ( 'NONE', *, *, #73288, .T. ) ;
#32643=CARTESIAN_POINT ( 'NONE',  ( 5.656854249492374365, 5.656854249492375253, 13.95530278392014623 ) ) ;
#32666=CARTESIAN_POINT ( 'NONE',  ( 8.008118988124991233, 9.807117285998411148E-16, 22.76311528394063188 ) ) ;
#32700=CARTESIAN_POINT ( 'NONE',  ( 2.977408999572650927, -7.188101187499990274, 21.83030278187175810 ) ) ;
#32725=CARTESIAN_POINT ( 'NONE',  ( 5.656854249492374365, 5.656854249492375253, 25.76780277982336997 ) ) ;
#32726=CARTESIAN_POINT ( 'NONE',  ( -5.447323953993864265, -4.689931814214729044, 0.5319290643893268555 ) ) ;
#32739=CARTESIAN_POINT ( 'NONE',  ( -5.656854249492373476, -5.656854249492376141, 11.51780277982336642 ) ) ;
#32742=CARTESIAN_POINT ( 'NONE',  ( 7.999999999999992895, -3.313708498984756279, 21.17405278392015333 ) ) ;
#32744=CYLINDRICAL_SURFACE ( 'NONE', #66160, 7.999999999999991118 ) ;
#32757=LINE ( 'NONE', #66692, #37502 ) ;
#32764=CARTESIAN_POINT ( 'NONE',  ( -5.082755093536317936, -5.082755093536320601, 12.17405278187175277 ) ) ;
#32775=CARTESIAN_POINT ( 'NONE',  ( 1.469576158976822172E-15, -7.999999999999991118, 10.39280278392014800 ) ) ;
#32787=CARTESIAN_POINT ( 'NONE',  ( -7.188101187499992051, 0.000000000000000000, 10.48655278187175455 ) ) ;
#32794=CARTESIAN_POINT ( 'NONE',  ( 7.999999999971009856, 2.153409470846384379E-05, 12.26780339315719814 ) ) ;
#32812=CARTESIAN_POINT ( 'NONE',  ( 7.188101187499992051, 8.802885111219154394E-16, 13.11155278187175277 ) ) ;
#32828=CARTESIAN_POINT ( 'NONE',  ( 7.999999999999992895, -3.313708498984756279, 7.486552779823366421 ) ) ;
#32843=CARTESIAN_POINT ( 'NONE',  ( -5.656854249492375253, 5.656854249492375253, 12.69905278432982421 ) ) ;
#32845=CARTESIAN_POINT ( 'NONE',  ( 5.656854249492376141, -5.656854249492374365, 16.39280277982336287 ) ) ;
#32872=CARTESIAN_POINT ( 'NONE',  ( -7.999999999999991118, 0.000000000000000000, 28.01780278392014978 ) ) ;
#32874=CARTESIAN_POINT ( 'NONE',  ( 7.999999999999991118, 9.797174393178815797E-16, 16.58030277982336287 ) ) ;
#32879=CARTESIAN_POINT ( 'NONE',  ( 2.977408999572646486, 7.188101187499991163, 1.017802781871753215 ) ) ;
#32894=CARTESIAN_POINT ( 'NONE',  ( 7.188101187499992051, 8.802885111219154394E-16, 11.61155278187175632 ) ) ;
#32895=EDGE_LOOP ( 'NONE', ( #4871, #61701, #70340 ) ) ;
#32909=DIRECTION ( 'NONE',  ( 0.000000000000000000, 0.000000000000000000, 1.000000000000000000 ) ) ;
#32924=CARTESIAN_POINT ( 'NONE',  ( -7.999999999999991118, 3.313708498984756723, 24.73655277982336997 ) ) ;
#32935=CARTESIAN_POINT ( 'NONE',  ( -5.867873826482948196, -5.445834672501801421, -0.3031401758652553791 ) ) ;
#32937=EDGE_CURVE ( 'NONE', #51172, #60780, #10606, .T. ) ;
#32973=CARTESIAN_POINT ( 'NONE',  ( -2.977408999572648707, -7.188101187499990274, 27.26780278187175099 ) ) ;
#32976=ORIENTED_EDGE ( 'NONE', *, *, #69212, .F. ) ;
#32996=CARTESIAN_POINT ( 'NONE',  ( -4.401442555609577197E-16, 7.188101187499992051, 25.48655278187175810 ) ) ;
#33006=LINE ( 'NONE', #4320, #40825 ) ;
#33015=CARTESIAN_POINT ( 'NONE',  ( 5.656854249492374365, 5.656854249492375253, 7.767802779823362869 ) ) ;
#33021=CARTESIAN_POINT ( 'NONE',  ( -7.999999999974042098, 1.357258486152048259E-05, 14.51729352187485311 ) ) ;
#33022=CARTESIAN_POINT ( 'NONE',  ( -3.313708498984757611, 7.999999999999991118, 2.049052779823364645 ) ) ;
#33046=CARTESIAN_POINT ( 'NONE',  ( 8.008118988124991233, 3.317071493978879015, 19.85686528394063188 ) ) ;
#33060=CARTESIAN_POINT ( 'NONE',  ( 5.656854249492374365, 5.656854249492375253, 21.26780277982336642 ) ) ;
#33063=VECTOR ( 'NONE', #15019, 1000.000000000000000 ) ;
#33068=ORIENTED_EDGE ( 'NONE', *, *, #34800, .T. ) ;
#33081=CARTESIAN_POINT ( 'NONE',  ( 2.977408999572646486, 7.188101187499991163, 20.89280278187176521 ) ) ;
#33106=CARTESIAN_POINT ( 'NONE',  ( -3.313708498984757167, 7.999999999999991118, 24.54905277982336287 ) ) ;
#33127=CARTESIAN_POINT ( 'NONE',  ( 7.999999999999991118, 3.313708498984757611, 10.86155278392014800 ) ) ;
#33137=( BOUNDED_CURVE ( )  B_SPLINE_CURVE ( 2, ( #73694, #15970, #16704, #22005, #45388, #45032, #68040, #39369, #63114 ),
 .UNSPECIFIED., .F., .F. ) 
 B_SPLINE_CURVE_WITH_KNOTS ( ( 3, 2, 2, 2, 3 ),
 ( 0.7368421052631579649, 0.7434210526315789824, 0.7500000000000000000, 0.7565789473684210176, 0.7631578947368420351 ),
 .UNSPECIFIED. ) 
 CURVE ( )  GEOMETRIC_REPRESENTATION_ITEM ( )  RATIONAL_B_SPLINE_CURVE ( ( 0.9999999999999986677, 0.9238795325112880708, 1.000000000000000000, 0.9238795325112867385, 1.000000000000000000, 0.9238795325112867385, 1.000000000000000000, 0.9238795325112880708, 0.9999999999999986677 ) ) 
 REPRESENTATION_ITEM ( '' )  );
#33149=CARTESIAN_POINT ( 'NONE',  ( 5.082755093536318824, 5.082755093536319713, 17.42405278187175810 ) ) ;
#33169=CARTESIAN_POINT ( 'NONE',  ( -7.188101187499991163, 2.977408999572646930, 10.39280278187175810 ) ) ;
#33174=CARTESIAN_POINT ( 'NONE',  ( 7.999999999843520726, -5.003525229023116430E-05, 24.26780136833107093 ) ) ;
#33194=CARTESIAN_POINT ( 'NONE',  ( -4.401442555609577197E-16, 7.188101187499992051, 14.98655278187175455 ) ) ;
#33210=CARTESIAN_POINT ( 'NONE',  ( -3.313708498984758943, -7.999999999999989342, 7.111552779823365533 ) ) ;
#33223=CARTESIAN_POINT ( 'NONE',  ( -7.999999999999991118, 0.000000000000000000, 9.886552784329824206 ) ) ;
#33228=( BOUNDED_CURVE ( )  B_SPLINE_CURVE ( 2, ( #20518, #25802, #48822, #71829, #3189, #66178, #37521, #43532, #66547, #9216, #50685 ),
 .UNSPECIFIED., .F., .F. ) 
 B_SPLINE_CURVE_WITH_KNOTS ( ( 3, 2, 2, 2, 2, 3 ),
 ( 0.1853116620478932886, 0.1853117163647907406, 0.1919299919492475637, 0.1985482675337043590, 0.2051665431181611821, 0.2117847674899544508 ),
 .UNSPECIFIED. ) 
 CURVE ( )  GEOMETRIC_REPRESENTATION_ITEM ( )  RATIONAL_B_SPLINE_CURVE ( ( 0.9999987505525751441, 0.9999993752711603401, 1.000000000000000000, 0.9238795325112867385, 1.000000000000000000, 0.9238795325112867385, 1.000000000000000000, 0.9238795325112867385, 1.000000000000000000, 0.9238801215366059250, 0.9999988219584774463 ) ) 
 REPRESENTATION_ITEM ( '' )  );
#33233=VERTEX_POINT ( 'NONE', #28716 ) ;
#33250=CARTESIAN_POINT ( 'NONE',  ( -5.082755093536319713, 5.082755093536319713, 2.799052781871750994 ) ) ;
#33251=VERTEX_POINT ( 'NONE', #34038 ) ;
#33263=CARTESIAN_POINT ( 'NONE',  ( -5.082755093536319713, 5.082755093536319713, 7.674052781871751883 ) ) ;
#33293=CARTESIAN_POINT ( 'NONE',  ( 7.999999999999992895, -3.313708498984756279, 28.48655277982336642 ) ) ;
#33305=CARTESIAN_POINT ( 'NONE',  ( -4.898587196589407898E-16, 7.999999999999991118, 3.642802783920144449 ) ) ;
#33309=ORIENTED_EDGE ( 'NONE', *, *, #32012, .T. ) ;
#33310=CIRCLE ( 'NONE', #779, 12.50000000000000711 ) ;
#33313=CARTESIAN_POINT ( 'NONE',  ( -7.999999999999991118, 0.000000000000000000, 24.83030277982336642 ) ) ;
#33332=ORIENTED_EDGE ( 'NONE', *, *, #40133, .T. ) ;
#33337=CARTESIAN_POINT ( 'NONE',  ( 2.977408999572646486, 7.188101187499991163, 19.01780278187175810 ) ) ;
#33361=CARTESIAN_POINT ( 'NONE',  ( 7.188101187499992051, 8.802885111219154394E-16, 14.61155278187175455 ) ) ;
#33379=CARTESIAN_POINT ( 'NONE',  ( 7.999999999999991118, 3.313708498984757611, 3.174052779823361981 ) ) ;
#33390=CARTESIAN_POINT ( 'NONE',  ( 7.999999999999992895, -3.313708498984756279, 10.67405278392014623 ) ) ;
#33409=CARTESIAN_POINT ( 'NONE',  ( -8.008118988124991233, 0.000000000000000000, 17.51311528394063188 ) ) ;
#33418=VECTOR ( 'NONE', #20972, 1000.000000000000114 ) ;
#33442=( BOUNDED_CURVE ( )  B_SPLINE_CURVE ( 2, ( #12186, #58599, #52557, #46892, #6905, #47618, #18595, #46521, #69540 ),
 .UNSPECIFIED., .F., .F. ) 
 B_SPLINE_CURVE_WITH_KNOTS ( ( 3, 2, 2, 2, 3 ),
 ( 0.2894736842105262720, 0.2960526315789473450, 0.3026315789473684181, 0.3092105263157894912, 0.3157894736842105643 ),
 .UNSPECIFIED. ) 
 CURVE ( )  GEOMETRIC_REPRESENTATION_ITEM ( )  RATIONAL_B_SPLINE_CURVE ( ( 1.000000000000000666, 0.9238795325112860723, 1.000000000000000000, 0.9238795325112867385, 1.000000000000000000, 0.9238795325112867385, 1.000000000000000000, 0.9238795325112860723, 1.000000000000000666 ) ) 
 REPRESENTATION_ITEM ( '' )  );
#33446=CARTESIAN_POINT ( 'NONE',  ( -2.977408999572647819, 7.188101187499991163, 25.58030278187175810 ) ) ;
#33471=CARTESIAN_POINT ( 'NONE',  ( -5.656854249492373476, -5.656854249492376141, 26.51780277982336997 ) ) ;
#33489=CARTESIAN_POINT ( 'NONE',  ( 5.656854249492376141, -5.656854249492374365, 10.58030278392014800 ) ) ;
#33493=LINE ( 'NONE', #45904, #29876 ) ;
#33512=CARTESIAN_POINT ( 'NONE',  ( -7.188101187499992051, 0.000000000000000000, 17.98655278187175455 ) ) ;
#33537=CARTESIAN_POINT ( 'NONE',  ( 7.188101187499992051, 8.802885111219154394E-16, 14.23655278187175455 ) ) ;
#33561=CARTESIAN_POINT ( 'NONE',  ( -2.977408999572647819, 7.188101187499991163, 18.08030278187175455 ) ) ;
#33577=CARTESIAN_POINT ( 'NONE',  ( 7.999999999999991118, 9.797174393178815797E-16, 4.580302779823363757 ) ) ;
#33593=CARTESIAN_POINT ( 'NONE',  ( 1.469576158976822172E-15, -7.999999999999991118, 8.761552784329824206 ) ) ;
#33601=CARTESIAN_POINT ( 'NONE',  ( 0.000000000000000000, 0.000000000000000000, 30.00000000000000000 ) ) ;
#33622=CARTESIAN_POINT ( 'NONE',  ( -2.977408999572648707, -7.188101187499990274, 3.267802781871751439 ) ) ;
#33624=ORIENTED_EDGE ( 'NONE', *, *, #53368, .T. ) ;
#33635=CARTESIAN_POINT ( 'NONE',  ( -2.977408999572647819, 7.188101187499991163, 7.580302781871751883 ) ) ;
#33644=CARTESIAN_POINT ( 'NONE',  ( 0.000000000000000000, 0.000000000000000000, 30.00000000000000000 ) ) ;
#33645=CARTESIAN_POINT ( 'NONE',  ( -7.999999999999991118, 0.000000000000000000, 18.83030277982336642 ) ) ;
#33663=CARTESIAN_POINT ( 'NONE',  ( 7.999999999999991118, 9.797174393178815797E-16, 19.58030277982336642 ) ) ;
#33672=ORIENTED_EDGE ( 'NONE', *, *, #16309, .F. ) ;
#33678=CARTESIAN_POINT ( 'NONE',  ( -7.999999999999991118, -4.672035931492118266, 28.01873199342790244 ) ) ;
#33698=DIRECTION ( 'NONE',  ( -1.000000000000000000, -0.000000000000000000, -0.000000000000000000 ) ) ;
#33713=CARTESIAN_POINT ( 'NONE',  ( -2.977408999572647819, 7.188101187499991163, 16.20530278187175455 ) ) ;
#33735=CARTESIAN_POINT ( 'NONE',  ( 2.977408999572646486, 7.188101187499992051, 17.89280278187175455 ) ) ;
#33744=CARTESIAN_POINT ( 'NONE',  ( -5.867873826487101319, -5.445834672497646523, -0.3031401758654214129 ) ) ;
#33759=CARTESIAN_POINT ( 'NONE',  ( -3.313708498984759387, -7.999999999999989342, 14.79905278392014978 ) ) ;
#33764=EDGE_CURVE ( 'NONE', #5549, #60564, #5236, .T. ) ;
#33785=CARTESIAN_POINT ( 'NONE',  ( -3.317071493978880348, -8.008118988124989457, 19.29436528394063544 ) ) ;
#33820=CARTESIAN_POINT ( 'NONE',  ( 1.320432766682872962E-15, -7.188101187499992051, 21.73655278187175455 ) ) ;
#33831=CARTESIAN_POINT ( 'NONE',  ( -4.898587196589407898E-16, 7.999999999999991118, 27.64280278392014978 ) ) ;
#33835=VERTEX_POINT ( 'NONE', #60659 ) ;
#33845=CARTESIAN_POINT ( 'NONE',  ( -3.313708498984757167, 7.999999999999991118, 21.54905277982336287 ) ) ;
#33864=CARTESIAN_POINT ( 'NONE',  ( -7.999999999999989342, -3.313708498984762496, 13.11155278392014623 ) ) ;
#33913=CARTESIAN_POINT ( 'NONE',  ( -7.188101187499992051, 0.000000000000000000, 13.48655278187175455 ) ) ;
#33937=CARTESIAN_POINT ( 'NONE',  ( -2.977408999572648707, -7.188101187499990274, 8.142802781871750994 ) ) ;
#33940=CARTESIAN_POINT ( 'NONE',  ( -3.313708498984757167, 7.999999999999991118, 3.605302784329822874 ) ) ;
#33952=CARTESIAN_POINT ( 'NONE',  ( -7.999999999999991118, -4.672035931492118266, 28.14998199301822623 ) ) ;
#33972=CARTESIAN_POINT ( 'NONE',  ( 1.469576158976822172E-15, -7.999999999999991118, 5.761552784329825094 ) ) ;
#34002=CARTESIAN_POINT ( 'NONE',  ( 5.082755093536318824, 5.082755093536319713, 0.9240527818717529929 ) ) ;
#34015=CARTESIAN_POINT ( 'NONE',  ( -2.977408999572647819, 7.188101187499991163, 4.580302781871752771 ) ) ;
#34027=CARTESIAN_POINT ( 'NONE',  ( 2.977408999572646486, 7.188101187499992051, 1.392802781871753437 ) ) ;
#34034=CIRCLE ( 'NONE', #50849, 20.00000000000000355 ) ;
#34038=CARTESIAN_POINT ( 'NONE',  ( 7.999999999999991118, 9.797174393178815797E-16, 1.580302779823364201 ) ) ;
#34043=CARTESIAN_POINT ( 'NONE',  ( -3.313708498984757167, 7.999999999999991118, 20.04905277982336642 ) ) ;
#34051=CARTESIAN_POINT ( 'NONE',  ( 7.999999999999992895, -3.313708498984756279, 0.1740527839201450044 ) ) ;
#34058=CARTESIAN_POINT ( 'NONE',  ( 5.656854249492376141, -5.656854249492374365, 20.94905278432982243 ) ) ;
#34087=CARTESIAN_POINT ( 'NONE',  ( 5.082755093536318824, 5.082755093536319713, 20.42405278187175455 ) ) ;
#34105=CARTESIAN_POINT ( 'NONE',  ( -4.898587196589407898E-16, 7.999999999999991118, 26.14280278392014623 ) ) ;
#34108=CARTESIAN_POINT ( 'NONE',  ( 5.082755093536318824, 5.082755093536319713, 17.79905278187175810 ) ) ;
#34127=CARTESIAN_POINT ( 'NONE',  ( -6.062601303906716588, -5.219661428662635494, 1.000679062340938064 ) ) ;
#34132=CARTESIAN_POINT ( 'NONE',  ( 3.313708498984762496, -7.999999999999989342, 14.98655278392014623 ) ) ;
#34155=CARTESIAN_POINT ( 'NONE',  ( 8.008118988124993010, -3.317071493978877239, 18.16936528394062833 ) ) ;
#34173=CARTESIAN_POINT ( 'NONE',  ( 7.999999999999991118, 3.313708498984757611, 9.361552783920146226 ) ) ;
#34174=VERTEX_POINT ( 'NONE', #29319 ) ;
#34186=CARTESIAN_POINT ( 'NONE',  ( -7.188101187499992051, 0.000000000000000000, 19.86155278187175455 ) ) ;
#34206=CARTESIAN_POINT ( 'NONE',  ( -3.689217076869665934, -7.102672987750866085, -0.000000000000000000 ) ) ;
#34213=CARTESIAN_POINT ( 'NONE',  ( 7.999999999999991118, 3.313708498984757611, 19.67405277982336642 ) ) ;
#34233=CARTESIAN_POINT ( 'NONE',  ( 3.313708498984762496, -7.999999999999989342, 14.98655278392014623 ) ) ;
#34261=PRODUCT_DEFINITION_CONTEXT ( 'detailed design', #65515, 'design' ) ;
#34272=( LENGTH_UNIT ( ) NAMED_UNIT ( * ) SI_UNIT ( .MILLI., .METRE. ) );
#34282=CARTESIAN_POINT ( 'NONE',  ( 7.188101187499992051, 8.802885111219154394E-16, 9.736552781871754547 ) ) ;
#34308=CARTESIAN_POINT ( 'NONE',  ( -7.188101187499991163, 2.977408999572646930, 12.26780278187175455 ) ) ;
#34310=CARTESIAN_POINT ( 'NONE',  ( 7.999999999999991118, 9.797174393178815797E-16, 3.136552784329822430 ) ) ;
#34322=CARTESIAN_POINT ( 'NONE',  ( 5.656854249492376141, -5.656854249492374365, 1.392802779823364201 ) ) ;
#34329=AXIS2_PLACEMENT_3D ( 'NONE', #21726, #38351, #16430 ) ;
#34341=CARTESIAN_POINT ( 'NONE',  ( 1.469576158976822172E-15, -7.999999999999991118, 4.261552784329823318 ) ) ;
#34342=AXIS2_PLACEMENT_3D ( 'NONE', #12155, #63093, #5763 ) ;
#34348=ADVANCED_FACE ( 'NONE', ( #8890 ), #65456, .F. ) ;
#34349=CARTESIAN_POINT ( 'NONE',  ( 7.188101187499993827, -2.977408999572645598, 26.14280278187175455 ) ) ;
#34360=CARTESIAN_POINT ( 'NONE',  ( 7.999999999999991118, 9.797174393178815797E-16, 22.76780278392014623 ) ) ;
#34363=CARTESIAN_POINT ( 'NONE',  ( 3.313708498984756279, 7.999999999999991118, 9.549052783920144449 ) ) ;
#34369=CIRCLE ( 'NONE', #50012, 7.999999999999991118 ) ;
#34370=CARTESIAN_POINT ( 'NONE',  ( -5.082755093536319713, 5.082755093536319713, 28.29905278187175810 ) ) ;
#34384=CARTESIAN_POINT ( 'NONE',  ( 2.977408999572646486, 7.188101187499991163, 5.892802781871754547 ) ) ;
#34392=CARTESIAN_POINT ( 'NONE',  ( -7.999999999999991118, 0.000000000000000000, 6.830302779823365533 ) ) ;
#34397=CARTESIAN_POINT ( 'NONE',  ( -5.447323953993864265, -4.689931814214729044, 0.5319290643893268555 ) ) ;
#34412=CARTESIAN_POINT ( 'NONE',  ( -5.656854249492375253, 5.656854249492375253, 20.14280277982336642 ) ) ;
#34422=ADVANCED_FACE ( 'NONE', ( #68302 ), #42304, .F. ) ;
#34427=CARTESIAN_POINT ( 'NONE',  ( -5.656854249492373476, -5.656854249492376141, 22.07405278432982243 ) ) ;
#34459=DIRECTION ( 'NONE',  ( 1.000000000000000000, 0.000000000000000000, 0.000000000000000000 ) ) ;
#34462=CARTESIAN_POINT ( 'NONE',  ( 7.188101187499993827, -2.977408999572645598, 17.14280278187175455 ) ) ;
#34485=CARTESIAN_POINT ( 'NONE',  ( 7.188101187499993827, -2.977408999572645598, 16.01780278187175099 ) ) ;
#34506=CARTESIAN_POINT ( 'NONE',  ( -3.313708498984757167, 7.999999999999991118, 3.549052779823362425 ) ) ;
#34520=CARTESIAN_POINT ( 'NONE',  ( 5.886648204683470276, -5.430392733765462054, 0.000000000000000000 ) ) ;
#34532=CARTESIAN_POINT ( 'NONE',  ( -3.317071493978878571, 8.008118988124991233, 12.73186528394062833 ) ) ;
#34551=CARTESIAN_POINT ( 'NONE',  ( -7.999999999999991118, 3.313708498984756723, 9.924052783920146226 ) ) ;
#34564=CARTESIAN_POINT ( 'NONE',  ( 5.082755093536320601, -5.082755093536318824, 15.92405278187175632 ) ) ;
#34588=CARTESIAN_POINT ( 'NONE',  ( -3.313708498984758943, -7.999999999999989342, 20.61155277982337353 ) ) ;
#34591=ORIENTED_EDGE ( 'NONE', *, *, #1238, .F. ) ;
#34597=VERTEX_POINT ( 'NONE', #2246 ) ;
#34605=CARTESIAN_POINT ( 'NONE',  ( 3.313708498984762496, -7.999999999999989342, 10.48655278392014800 ) ) ;
#34646=( NAMED_UNIT ( * ) SI_UNIT ( $, .STERADIAN. ) SOLID_ANGLE_UNIT ( ) );
#34648=EDGE_CURVE ( 'NONE', #47940, #71597, #38451, .T. ) ;
#34658=CARTESIAN_POINT ( 'NONE',  ( 5.082755093536320601, -5.082755093536318824, 8.049052781871752771 ) ) ;
#34681=CARTESIAN_POINT ( 'NONE',  ( 7.188101187499993827, -2.977408999572645598, 11.51780278187175810 ) ) ;
#34684=CARTESIAN_POINT ( 'NONE',  ( -5.656854249492375253, 5.656854249492375253, 2.199052784329821542 ) ) ;
#34693=CARTESIAN_POINT ( 'NONE',  ( -5.656854249492373476, -5.656854249492376141, 5.517802779823364645 ) ) ;
#34695=CARTESIAN_POINT ( 'NONE',  ( 7.999999999999991118, 0.000000000000000000, 30.00000000000000000 ) ) ;
#34707=CARTESIAN_POINT ( 'NONE',  ( -3.313708498984757167, 7.999999999999991118, 8.105302784329824206 ) ) ;
#34717=CARTESIAN_POINT ( 'NONE',  ( 7.188101187499992051, 2.977408999572647819, 27.83030278187176165 ) ) ;
#34731=CARTESIAN_POINT ( 'NONE',  ( -7.999999999999989342, -3.313708498984762496, 19.11155278392014623 ) ) ;
#34743=CARTESIAN_POINT ( 'NONE',  ( -4.401442555609577197E-16, 7.188101187499992051, 23.61155278187175455 ) ) ;
#34756=CARTESIAN_POINT ( 'NONE',  ( 2.977408999572650927, -7.188101187499990274, 6.830302781871755435 ) ) ;
#34759=FACE_OUTER_BOUND ( 'NONE', #61061, .T. ) ;
#34762=CARTESIAN_POINT ( 'NONE',  ( -8.008118988124991233, 0.000000000000000000, 2.513115283940627886 ) ) ;
#34769=CARTESIAN_POINT ( 'NONE',  ( -5.082755093536319713, 5.082755093536319713, 28.67405278187175810 ) ) ;
#34786=CARTESIAN_POINT ( 'NONE',  ( 3.313708498984762496, -7.999999999999989342, 19.29905277982336642 ) ) ;
#34799=CARTESIAN_POINT ( 'NONE',  ( -3.313708498984757167, 7.999999999999991118, 24.60530278432982598 ) ) ;
#34800=EDGE_CURVE ( 'NONE', #27473, #29054, #61452, .T. ) ;
#34832=CARTESIAN_POINT ( 'NONE',  ( 1.320432766682872962E-15, -7.188101187499992051, 16.86155278187175810 ) ) ;
#34855=CARTESIAN_POINT ( 'NONE',  ( 7.188101187499993827, -2.977408999572645598, 19.01780278187175099 ) ) ;
#34875=CARTESIAN_POINT ( 'NONE',  ( 7.999999999999992895, -3.313708498984756279, 5.986552779823365533 ) ) ;
#34888=CARTESIAN_POINT ( 'NONE',  ( -7.999999999995399236, -5.826008446853342637E-06, 20.51801720710344767 ) ) ;
#34903=CARTESIAN_POINT ( 'NONE',  ( -8.008118988124991233, 3.317071493978878127, 12.91936528394062833 ) ) ;
#34909=CARTESIAN_POINT ( 'NONE',  ( -2.977408999572647819, 7.188101187499992051, 10.20530278187175455 ) ) ;
#34922=CARTESIAN_POINT ( 'NONE',  ( -7.999999999999991118, 0.000000000000000000, 5.517802783920146226 ) ) ;
#34936=CARTESIAN_POINT ( 'NONE',  ( 2.977408999572646486, 7.188101187499991163, 19.39280278187176165 ) ) ;
#34939=CYLINDRICAL_SURFACE ( 'NONE', #64060, 7.999999999999991118 ) ;
#34958=DIRECTION ( 'NONE',  ( -0.000000000000000000, -0.000000000000000000, 1.000000000000000000 ) ) ;
#34959=CARTESIAN_POINT ( 'NONE',  ( 5.656854249492376141, -5.656854249492374365, 23.89280277982336642 ) ) ;
#34969=ORIENTED_EDGE ( 'NONE', *, *, #15733, .F. ) ;
#34978=CARTESIAN_POINT ( 'NONE',  ( 5.656854249492374365, 5.656854249492375253, 9.455302783920146226 ) ) ;
#35003=( BOUNDED_CURVE ( )  B_SPLINE_CURVE ( 2, ( #37746, #10190, #26785, #26393, #38118, #73190, #16192, #3409, #3784 ),
 .UNSPECIFIED., .F., .F. ) 
 B_SPLINE_CURVE_WITH_KNOTS ( ( 3, 2, 2, 2, 3 ),
 ( 0.8736124324192364732, 0.8802306527327560248, 0.8868489283172127369, 0.8934672039016696710, 0.9000854414465758735 ),
 .UNSPECIFIED. ) 
 CURVE ( )  GEOMETRIC_REPRESENTATION_ITEM ( )  RATIONAL_B_SPLINE_CURVE ( ( 0.9999987286070540771, 0.9238801682130686199, 1.000000000000000000, 0.9238795325112867385, 1.000000000000000000, 0.9238795325112867385, 1.000000000000000000, 0.9238799700253094160, 0.9999991249769839552 ) ) 
 REPRESENTATION_ITEM ( '' )  );
#35027=CARTESIAN_POINT ( 'NONE',  ( -7.188101187499990274, -2.977408999572651371, 7.580302781871751883 ) ) ;
#35036=EDGE_LOOP ( 'NONE', ( #38132, #21617, #27053, #58902 ) ) ;
#35051=CARTESIAN_POINT ( 'NONE',  ( -7.188101187499991163, 2.977408999572646930, 7.767802781871751883 ) ) ;
#35064=CARTESIAN_POINT ( 'NONE',  ( -7.999999999999989342, -3.313708498984762496, 25.11155278392014623 ) ) ;
#35081=CARTESIAN_POINT ( 'NONE',  ( -7.999999999999991118, 0.000000000000000000, 27.83030277982336642 ) ) ;
#35085=CARTESIAN_POINT ( 'NONE',  ( 7.188101187499993827, -2.977408999572645598, 24.64280278187176165 ) ) ;
#35096=CARTESIAN_POINT ( 'NONE',  ( -5.656854249492375253, 5.656854249492375253, 17.33030278392014623 ) ) ;
#35108=CARTESIAN_POINT ( 'NONE',  ( -2.977408999572647819, 7.188101187499991163, 25.20530278187175810 ) ) ;
#35121=CARTESIAN_POINT ( 'NONE',  ( 7.188101187499993827, -2.977408999572645598, 1.017802781871753215 ) ) ;
#35126=CARTESIAN_POINT ( 'NONE',  ( 5.662595241051934458, 5.662595241051935346, 0.4506152839406291633 ) ) ;
#35151=CARTESIAN_POINT ( 'NONE',  ( -5.656854249492373476, -5.656854249492376141, 23.51780277982336642 ) ) ;
#35164=CARTESIAN_POINT ( 'NONE',  ( 7.999999999999991118, 9.797174393178815797E-16, 24.13655278432982598 ) ) ;
#35196=CARTESIAN_POINT ( 'NONE',  ( -5.082755093536317936, -5.082755093536320601, 13.67405278187175455 ) ) ;
#35197=ORIENTED_EDGE ( 'NONE', *, *, #56468, .F. ) ;
#35219=CARTESIAN_POINT ( 'NONE',  ( -5.082755093536317936, -5.082755093536320601, 12.54905278187175277 ) ) ;
#35225=ORIENTED_EDGE ( 'NONE', *, *, #39480, .T. ) ;
#35267=CARTESIAN_POINT ( 'NONE',  ( -5.662595241051933570, -5.662595241051936235, 16.20061528394063188 ) ) ;
#35274=CARTESIAN_POINT ( 'NONE',  ( -2.977408999572647819, 7.188101187499992051, 11.70530278187175277 ) ) ;
#35288=CARTESIAN_POINT ( 'NONE',  ( 7.999999999999991118, 3.313708498984757611, 0.3615527839201451710 ) ) ;
#35301=CARTESIAN_POINT ( 'NONE',  ( -2.977408999572647819, 7.188101187499991163, 15.08030278187175455 ) ) ;
#35312=CARTESIAN_POINT ( 'NONE',  ( -7.188101187499990274, -2.977408999572651815, 27.45530278187175455 ) ) ;
#35330=CARTESIAN_POINT ( 'NONE',  ( -3.313708498984757167, 7.999999999999991118, 20.04905277982336642 ) ) ;
#35347=CARTESIAN_POINT ( 'NONE',  ( -3.313708498984758943, -7.999999999999989342, 4.299052783920145338 ) ) ;
#35361=CARTESIAN_POINT ( 'NONE',  ( -7.999999999999991118, 0.000000000000000000, 26.33030277982336997 ) ) ;
#35394=CARTESIAN_POINT ( 'NONE',  ( -5.082755093536319713, 5.082755093536319713, 7.299052781871751883 ) ) ;
#35418=CARTESIAN_POINT ( 'NONE',  ( 7.188101187499993827, -2.977408999572645598, 13.01780278187175277 ) ) ;
#35422=CARTESIAN_POINT ( 'NONE',  ( 3.313708498984762496, -7.999999999999989342, -0.1446972156701771817 ) ) ;
#35431=CARTESIAN_POINT ( 'NONE',  ( -7.999999999999991118, 0.000000000000000000, 22.01780278392014623 ) ) ;
#35450=CARTESIAN_POINT ( 'NONE',  ( -4.401442555609577197E-16, 7.188101187499992051, 28.11155278187175455 ) ) ;
#35459=CARTESIAN_POINT ( 'NONE',  ( 1.469576158976822172E-15, -7.999999999999991118, 22.39280278392014623 ) ) ;
#35469=CARTESIAN_POINT ( 'NONE',  ( 2.977408999572650927, -7.188101187499990274, 22.95530278187175455 ) ) ;
#35470=VERTEX_POINT ( 'NONE', #67403 ) ;
#35487=CARTESIAN_POINT ( 'NONE',  ( 8.008118988124991233, 3.317071493978879015, 0.3568652839406291077 ) ) ;
#35491=CARTESIAN_POINT ( 'NONE',  ( 8.000000000000037303, -3.313708498984713202, 7.486552779823369086 ) ) ;
#35511=CARTESIAN_POINT ( 'NONE',  ( -7.999999999999989342, -3.313708498984762496, 15.92405277982336465 ) ) ;
#35526=CARTESIAN_POINT ( 'NONE',  ( 3.313708498984756279, 7.999999999999991118, 25.91780278432982598 ) ) ;
#35536=( BOUNDED_CURVE ( )  B_SPLINE_CURVE ( 2, ( #72984, #32638, #5077, #56757, #15998, #16358, #10356, #21660, #39396, #55647, #21290 ),
 .UNSPECIFIED., .F., .F. ) 
 B_SPLINE_CURVE_WITH_KNOTS ( ( 3, 2, 2, 2, 2, 3 ),
 ( 0.2382579061490637251, 0.2382579210404291437, 0.2448761966248874100, 0.2514944722093456209, 0.2581127477938038872, 0.2647310102845484292 ),
 .UNSPECIFIED. ) 
 CURVE ( )  GEOMETRIC_REPRESENTATION_ITEM ( )  RATIONAL_B_SPLINE_CURVE ( ( 0.9999996574530229942, 0.9999998287261261387, 1.000000000000000000, 0.9238795325112867385, 1.000000000000000000, 0.9238795325112867385, 1.000000000000000000, 0.9238795325112867385, 1.000000000000000000, 0.9238796831093680773, 0.9999996988044332902 ) ) 
 REPRESENTATION_ITEM ( '' )  );
#35559=CARTESIAN_POINT ( 'NONE',  ( -2.977408999572648707, -7.188101187499990274, 12.26780278187175455 ) ) ;
#35581=CARTESIAN_POINT ( 'NONE',  ( -2.977408999572647819, -7.188101187499990274, 9.642802781871756324 ) ) ;
#35626=CARTESIAN_POINT ( 'NONE',  ( 3.317071493978877683, 8.008118988124991233, 14.04436528394063011 ) ) ;
#35632=CARTESIAN_POINT ( 'NONE',  ( 7.188101187499992051, 8.802885111219154394E-16, 8.236552781871752771 ) ) ;
#35647=CARTESIAN_POINT ( 'NONE',  ( 1.469576158976822172E-15, -7.999999999999991118, 4.392802783920145338 ) ) ;
#35662=CARTESIAN_POINT ( 'NONE',  ( -2.977408999572648707, -7.188101187499990274, 15.64280278187175632 ) ) ;
#35681=CARTESIAN_POINT ( 'NONE',  ( -3.093166311732832963, -7.380995655184879212, 0.000000000000000000 ) ) ;
#35682=CARTESIAN_POINT ( 'NONE',  ( 0.000000000000000000, 0.000000000000000000, 30.00000000000000000 ) ) ;
#35687=CARTESIAN_POINT ( 'NONE',  ( 3.313708498984756279, 7.999999999999991118, 15.36155277982336642 ) ) ;
#35705=CARTESIAN_POINT ( 'NONE',  ( 5.656854249492376141, -5.656854249492374365, 9.080302783920146226 ) ) ;
#35723=CARTESIAN_POINT ( 'NONE',  ( -7.999999999999991118, 3.313708498984757167, 11.42405278392014623 ) ) ;
#35751=EDGE_CURVE ( 'NONE', #30305, #31550, #31130, .T. ) ;
#35753=CARTESIAN_POINT ( 'NONE',  ( -5.082755093536317936, -5.082755093536320601, 6.174052781871754547 ) ) ;
#35779=CARTESIAN_POINT ( 'NONE',  ( -2.977408999572648707, -7.188101187499990274, 5.142802781871752771 ) ) ;
#35793=CARTESIAN_POINT ( 'NONE',  ( -5.656854249492373476, -5.656854249492376141, 26.70530278392014623 ) ) ;
#35815=CARTESIAN_POINT ( 'NONE',  ( -5.082755093536319713, 5.082755093536319713, 25.29905278187175810 ) ) ;
#35824=CARTESIAN_POINT ( 'NONE',  ( -3.313708498984757167, 7.999999999999991118, 20.23655278392014978 ) ) ;
#35827=DIRECTION ( 'NONE',  ( -0.000000000000000000, -0.000000000000000000, 1.000000000000000000 ) ) ;
#35835=CARTESIAN_POINT ( 'NONE',  ( 2.977408999572646486, 7.188101187499991163, 25.01780278187175455 ) ) ;
#35848=CARTESIAN_POINT ( 'NONE',  ( -5.447323953993864265, -4.689931814214729933, 0.5319290643893268555 ) ) ;
#35853=CARTESIAN_POINT ( 'NONE',  ( -5.662595241051933570, -5.662595241051936235, 5.700615283940630995 ) ) ;
#35860=CARTESIAN_POINT ( 'NONE',  ( 7.188101187499991163, 2.977408999572648707, 20.70530278187175455 ) ) ;
#35878=CARTESIAN_POINT ( 'NONE',  ( 5.656854249492376141, -5.656854249492374365, 14.89280277982336642 ) ) ;
#35894=CARTESIAN_POINT ( 'NONE',  ( -7.999999999999991118, 0.000000000000000000, 17.38655278432982243 ) ) ;
#35926=CARTESIAN_POINT ( 'NONE',  ( 1.320432766682872962E-15, -7.188101187499992051, 15.36155278187175277 ) ) ;
#35948=CARTESIAN_POINT ( 'NONE',  ( 1.320432766682872962E-15, -7.188101187499992051, 12.73655278187175277 ) ) ;
#35971=CARTESIAN_POINT ( 'NONE',  ( 7.999999999999991118, 9.797174393178815797E-16, 1.580302779823364201 ) ) ;
#35997=CARTESIAN_POINT ( 'NONE',  ( -8.008118988124991233, 0.000000000000000000, 14.51311528394063188 ) ) ;
#36002=CARTESIAN_POINT ( 'NONE',  ( -5.082755093536319713, 5.082755093536319713, 10.29905278187175455 ) ) ;
#36007=ORIENTED_EDGE ( 'NONE', *, *, #62110, .T. ) ;
#36015=CARTESIAN_POINT ( 'NONE',  ( -7.999999999999991118, 0.000000000000000000, 2.517802783920143561 ) ) ;
#36018=ORIENTED_EDGE ( 'NONE', *, *, #31558, .T. ) ;
#36030=EDGE_CURVE ( 'NONE', #31550, #63012, #32197, .T. ) ;
#36031=CARTESIAN_POINT ( 'NONE',  ( -4.401442555609577197E-16, 7.188101187499992051, 11.98655278187175632 ) ) ;
#36040=CARTESIAN_POINT ( 'NONE',  ( -5.082755093536319713, 5.082755093536319713, 28.67405278187175810 ) ) ;
#36042=DIRECTION ( 'NONE',  ( 1.000000000000000000, 0.000000000000000000, 0.000000000000000000 ) ) ;
#36057=CARTESIAN_POINT ( 'NONE',  ( 7.999999999999992895, -3.313708498984756279, 13.48655277982336465 ) ) ;
#36059=CARTESIAN_POINT ( 'NONE',  ( -5.656854249492373476, -5.656854249492376141, 17.70530278392014623 ) ) ;
#36108=ORIENTED_EDGE ( 'NONE', *, *, #19750, .T. ) ;
#36120=CARTESIAN_POINT ( 'NONE',  ( 1.320432766682872962E-15, -7.188101187499992051, 7.861552781871751883 ) ) ;
#36145=CARTESIAN_POINT ( 'NONE',  ( 7.188101187499993827, -2.977408999572645598, 7.017802781871755435 ) ) ;
#36147=DIRECTION ( 'NONE',  ( -1.000000000000000000, -1.224646799147353207E-16, 0.000000000000000000 ) ) ;
#36159=CARTESIAN_POINT ( 'NONE',  ( -7.999999999999989342, -3.313708498984762496, 23.61155278392014978 ) ) ;
#36181=CARTESIAN_POINT ( 'NONE',  ( -7.188101187499992051, 2.977408999572646930, 23.89280278187175810 ) ) ;
#36184=AXIS2_PLACEMENT_3D ( 'NONE', #29278, #65445, #24705 ) ;
#36193=CARTESIAN_POINT ( 'NONE',  ( 3.313708498984762496, -7.999999999999989342, 16.48655278392014623 ) ) ;
#36196=CARTESIAN_POINT ( 'NONE',  ( 7.999999999999991118, 0.000000000000000000, 30.00000000000000000 ) ) ;
#36203=CARTESIAN_POINT ( 'NONE',  ( -7.188101187499991163, 2.977408999572646930, 22.39280278187175810 ) ) ;
#36204=ORIENTED_EDGE ( 'NONE', *, *, #13968, .T. ) ;
#36207=DIRECTION ( 'NONE',  ( -0.000000000000000000, -0.000000000000000000, 1.000000000000000000 ) ) ;
#36221=CARTESIAN_POINT ( 'NONE',  ( 5.662595241051934458, 5.662595241051935346, 4.950615283940630107 ) ) ;
#36222=CARTESIAN_POINT ( 'NONE',  ( 7.999999999999991118, 0.000000000000000000, 30.00000000000000000 ) ) ;
#36227=CARTESIAN_POINT ( 'NONE',  ( 5.082755093536318824, 5.082755093536319713, 22.29905278187175455 ) ) ;
#36236=CARTESIAN_POINT ( 'NONE',  ( 7.999999999999991118, 9.797174393178815797E-16, 15.08030277982336642 ) ) ;
#36246=CARTESIAN_POINT ( 'NONE',  ( 3.313708498984756279, 7.999999999999991118, 13.86155277982336465 ) ) ;
#36255=ORIENTED_EDGE ( 'NONE', *, *, #285, .T. ) ;
#36261=CARTESIAN_POINT ( 'NONE',  ( 7.999999999999992895, -3.313708498984756279, 16.54280278432982598 ) ) ;
#36273=ORIENTED_EDGE ( 'NONE', *, *, #74560, .F. ) ;
#36293=CARTESIAN_POINT ( 'NONE',  ( -7.188101187499991163, 2.977408999572646930, 13.39280278187175455 ) ) ;
#36305=EDGE_CURVE ( 'NONE', #8103, #14923, #52165, .T. ) ;
#36317=CARTESIAN_POINT ( 'NONE',  ( 7.188101187499993827, -2.977408999572645598, 13.01780278187175277 ) ) ;
#36323=CARTESIAN_POINT ( 'NONE',  ( 7.999999999999991118, 3.313708498984758055, 3.361552783920144893 ) ) ;
#36339=CARTESIAN_POINT ( 'NONE',  ( -5.656854249492373476, -5.656854249492376141, 23.51780277982336642 ) ) ;
#36350=DIRECTION ( 'NONE',  ( -0.000000000000000000, -0.000000000000000000, 1.000000000000000000 ) ) ;
#36361=CARTESIAN_POINT ( 'NONE',  ( -8.008118988124991233, 3.317071493978878127, 6.919365283940628331 ) ) ;
#36366=CARTESIAN_POINT ( 'NONE',  ( 5.082755093536318824, 5.082755093536319713, 9.924052781871754547 ) ) ;
#36378=CYLINDRICAL_SURFACE ( 'NONE', #47634, 7.999999999999991118 ) ;
#36379=CARTESIAN_POINT ( 'NONE',  ( -3.313708498984758943, -7.999999999999989342, 4.299052783920145338 ) ) ;
#36397=CARTESIAN_POINT ( 'NONE',  ( -7.999999999999976019, -3.611371706259009353E-07, 26.51781575558936055 ) ) ;
#36403=FACE_OUTER_BOUND ( 'NONE', #10118, .T. ) ;
#36424=CARTESIAN_POINT ( 'NONE',  ( -4.898587196589407898E-16, 7.999999999999991118, 13.95530277982336465 ) ) ;
#36455=CARTESIAN_POINT ( 'NONE',  ( -3.317071493978878571, 8.008118988124991233, 27.73186528394063544 ) ) ;
#36488=CARTESIAN_POINT ( 'NONE',  ( -2.977408999572647819, 7.188101187499991163, 2.705302781871750994 ) ) ;
#36515=CARTESIAN_POINT ( 'NONE',  ( -5.082755093536317936, -5.082755093536320601, 2.049052781871754103 ) ) ;
#36530=CARTESIAN_POINT ( 'NONE',  ( 7.999999999999991118, 3.313708498984757611, 22.86155278392014623 ) ) ;
#36549=CARTESIAN_POINT ( 'NONE',  ( -4.401442555609577197E-16, 7.188101187499992051, 22.11155278187175455 ) ) ;
#36557=CARTESIAN_POINT ( 'NONE',  ( 3.313708498984756279, 7.999999999999991118, 12.54905278392014800 ) ) ;
#36569=CARTESIAN_POINT ( 'NONE',  ( 5.082755093536318824, 5.082755093536319713, 18.92405278187175455 ) ) ;
#36571=ORIENTED_EDGE ( 'NONE', *, *, #36737, .F. ) ;
#36581=CARTESIAN_POINT ( 'NONE',  ( 7.188101187499991163, 2.977408999572648707, 1.205302781871753215 ) ) ;
#36587=CARTESIAN_POINT ( 'NONE',  ( -6.068751001326191385, -5.224962297650614040, -0.3165082965516815006 ) ) ;
#36594=CARTESIAN_POINT ( 'NONE',  ( 2.977408999572646486, 7.188101187499991163, 22.39280278187175810 ) ) ;
#36612=CARTESIAN_POINT ( 'NONE',  ( 3.313708498984762496, -7.999999999999989342, 13.29905277982336465 ) ) ;
#36630=CARTESIAN_POINT ( 'NONE',  ( 3.313708498984756279, 7.999999999999991118, 15.41780278432982598 ) ) ;
#36662=CARTESIAN_POINT ( 'NONE',  ( 2.977408999572646486, 7.188101187499991163, 8.517802781871754547 ) ) ;
#36685=CARTESIAN_POINT ( 'NONE',  ( -7.188101187499990274, -2.977408999572651815, 7.955302781871751883 ) ) ;
#36707=ORIENTED_EDGE ( 'NONE', *, *, #43713, .F. ) ;
#36713=CARTESIAN_POINT ( 'NONE',  ( -5.656854249492375253, 5.656854249492375253, 9.642802779823364645 ) ) ;
#36729=CARTESIAN_POINT ( 'NONE',  ( -3.317071493978880348, -8.008118988124989457, 7.294365283940629219 ) ) ;
#36736=CARTESIAN_POINT ( 'NONE',  ( -2.977408999572647819, 7.188101187499992051, 1.205302781871753215 ) ) ;
#36737=EDGE_CURVE ( 'NONE', #38597, #4709, #27246, .T. ) ;
#36750=CARTESIAN_POINT ( 'NONE',  ( 5.656854249492374365, 5.656854249492375253, 1.955302783920143117 ) ) ;
#36767=CARTESIAN_POINT ( 'NONE',  ( 3.313708498984756279, 7.999999999999991118, 3.361552779823362425 ) ) ;
#36774=CARTESIAN_POINT ( 'NONE',  ( 7.188101187499993827, -2.977408999572645598, 26.51780278187175455 ) ) ;
#36792=CARTESIAN_POINT ( 'NONE',  ( -5.656854249492373476, -5.656854249492376141, 14.51780277982336465 ) ) ;
#36794=CARTESIAN_POINT ( 'NONE',  ( 3.313708498984762496, -7.999999999999989342, 17.98655278392014623 ) ) ;
#36813=CYLINDRICAL_SURFACE ( 'NONE', #50918, 7.999999999999991118 ) ;
#36819=EDGE_LOOP ( 'NONE', ( #62333, #36255, #37830, #65003 ) ) ;
#36821=CARTESIAN_POINT ( 'NONE',  ( 1.471067592899761672E-15, -8.008118988124991233, 25.38811528394063544 ) ) ;
#36836=EDGE_CURVE ( 'NONE', #4709, #38597, #33310, .T. ) ;
#36857=CARTESIAN_POINT ( 'NONE',  ( -5.082755093536317936, -5.082755093536320601, 1.674052781871753659 ) ) ;
#36881=CARTESIAN_POINT ( 'NONE',  ( -4.401442555609577197E-16, 7.188101187499992051, 2.986552781871751439 ) ) ;
#36882=DIRECTION ( 'NONE',  ( -0.000000000000000000, -0.000000000000000000, 1.000000000000000000 ) ) ;
#36895=CARTESIAN_POINT ( 'NONE',  ( -3.313708498984758943, -7.999999999999989342, 17.79905278392014623 ) ) ;
#36918=CARTESIAN_POINT ( 'NONE',  ( 7.188101187499992051, 8.802885111219154394E-16, 23.23655278187175455 ) ) ;
#36919=DIRECTION ( 'NONE',  ( 1.000000000000000000, 3.169619151431689753E-17, -1.182917971378671814E-16 ) ) ;
#36926=CARTESIAN_POINT ( 'NONE',  ( 7.999999999999992895, -3.313708498984756279, 12.17405278392014800 ) ) ;
#36927=CARTESIAN_POINT ( 'NONE',  ( 5.656854249492374365, 5.656854249492375253, 18.45530278392014623 ) ) ;
#36938=CARTESIAN_POINT ( 'NONE',  ( 1.320432766682872962E-15, -7.188101187499992051, 21.36155278187175455 ) ) ;
#36950=CARTESIAN_POINT ( 'NONE',  ( 5.656854249492374365, 5.656854249492375253, 15.26780277982336642 ) ) ;
#36954=CARTESIAN_POINT ( 'NONE',  ( 5.656854249492374365, 5.656854249492375253, 27.45530278392014978 ) ) ;
#36961=CARTESIAN_POINT ( 'NONE',  ( -2.977408999572647819, 7.188101187499991163, 21.08030278187175810 ) ) ;
#36980=CARTESIAN_POINT ( 'NONE',  ( -7.999999999999989342, -3.313708498984762496, 12.92405277982336287 ) ) ;
#36993=CARTESIAN_POINT ( 'NONE',  ( 7.999999999999992895, -3.313708498984756279, 18.04280278432982598 ) ) ;
#37026=CARTESIAN_POINT ( 'NONE',  ( -5.082755093536317936, -5.082755093536320601, 9.174052781871752771 ) ) ;
#37050=CARTESIAN_POINT ( 'NONE',  ( 7.188101187499993827, -2.977408999572645598, 5.517802781871753659 ) ) ;
#37079=CARTESIAN_POINT ( 'NONE',  ( -7.999999999999991118, 3.313708498984756723, 8.424052783920146226 ) ) ;
#37097=CARTESIAN_POINT ( 'NONE',  ( -8.008118988124989457, -3.317071493978883900, 8.606865283940630107 ) ) ;
#37104=CARTESIAN_POINT ( 'NONE',  ( -2.977408999572647819, -7.188101187499990274, 0.2678027818717523822 ) ) ;
#37117=CARTESIAN_POINT ( 'NONE',  ( 2.977408999572650927, -7.188101187499990274, 24.45530278187175455 ) ) ;
#37139=CARTESIAN_POINT ( 'NONE',  ( 7.188101187499993827, -2.977408999572645598, 23.51780278187175455 ) ) ;
#37160=CARTESIAN_POINT ( 'NONE',  ( -7.999999999999991118, 3.313708498984756723, 8.236552779823362869 ) ) ;
#37179=ORIENTED_EDGE ( 'NONE', *, *, #61620, .T. ) ;
#37181=EDGE_CURVE ( 'NONE', #73315, #41375, #70326, .T. ) ;
#37191=CARTESIAN_POINT ( 'NONE',  ( 8.008118988124991233, 9.807117285998411148E-16, 25.76311528394063544 ) ) ;
#37222=LINE ( 'NONE', #54954, #33418 ) ;
#37223=DIRECTION ( 'NONE',  ( -0.000000000000000000, -0.000000000000000000, 1.000000000000000000 ) ) ;
#37227=CARTESIAN_POINT ( 'NONE',  ( -5.082755093536319713, 5.082755093536319713, 28.67405278187175810 ) ) ;
#37242=EDGE_CURVE ( 'NONE', #6596, #60098, #23590, .T. ) ;
#37253=ADVANCED_BREP_SHAPE_REPRESENTATION ( '', ( #66162, #57354 ), #18781 ) ;
#37254=CARTESIAN_POINT ( 'NONE',  ( 7.188101187499993827, -2.977408999572645598, 5.517802781871753659 ) ) ;
#37272=CARTESIAN_POINT ( 'NONE',  ( -7.999999999999991118, 3.313708498984756723, 18.92405278392014978 ) ) ;
#37279=( BOUNDED_CURVE ( )  B_SPLINE_CURVE ( 2, ( #2511, #49648, #25505, #71899, #3257, #45842, #74517, #10035, #45467 ),
 .UNSPECIFIED., .F., .F. ) 
 B_SPLINE_CURVE_WITH_KNOTS ( ( 3, 2, 2, 2, 3 ),
 ( 0.6618275503331610965, 0.6684458340301022705, 0.6750641096145244546, 0.6816823851989468608, 0.6883006607833690449 ),
 .UNSPECIFIED. ) 
 CURVE ( )  GEOMETRIC_REPRESENTATION_ITEM ( )  RATIONAL_B_SPLINE_CURVE ( ( 1.000000000000000000, 0.9238795325112867385, 1.000000000000000000, 0.9238795325112867385, 1.000000000000000000, 0.9238795325112867385, 1.000000000000000000, 0.9238795325128899005, 0.9999999999983968380 ) ) 
 REPRESENTATION_ITEM ( '' )  );
#37293=CARTESIAN_POINT ( 'NONE',  ( 2.977408999572646486, 7.188101187499992051, 23.51780278187175455 ) ) ;
#37294=DIRECTION ( 'NONE',  ( -1.182917971378671814E-16, 0.000000000000000000, -1.000000000000000000 ) ) ;
#37301=CARTESIAN_POINT ( 'NONE',  ( -3.313708498984757167, 7.999999999999991118, 12.73655278392014623 ) ) ;
#37311=DIRECTION ( 'NONE',  ( -0.000000000000000000, -0.000000000000000000, -1.000000000000000000 ) ) ;
#37313=CARTESIAN_POINT ( 'NONE',  ( -5.082755093536319713, 5.082755093536319713, 16.29905278187175455 ) ) ;
#37328=CARTESIAN_POINT ( 'NONE',  ( 7.999972022862700705, 3.313736476122048025, 0.3615539032942260977 ) ) ;
#37331=CARTESIAN_POINT ( 'NONE',  ( 3.313708498984756279, 7.999999999999991118, 26.04905278392014623 ) ) ;
#37337=CARTESIAN_POINT ( 'NONE',  ( -7.188101187499992051, 0.000000000000000000, 21.36155278187175455 ) ) ;
#37352=CARTESIAN_POINT ( 'NONE',  ( 7.999999999999991118, 9.797174393178815797E-16, 9.080302779823364645 ) ) ;
#37368=CARTESIAN_POINT ( 'NONE',  ( -7.999999999999989342, -3.313708498984762496, 14.48030278432982598 ) ) ;
#37369=CARTESIAN_POINT ( 'NONE',  ( 3.313708498984762496, -7.999999999999989342, 16.29905277982336642 ) ) ;
#37387=ADVANCED_FACE ( 'NONE', ( #51667 ), #67534, .F. ) ;
#37400=CARTESIAN_POINT ( 'NONE',  ( 7.188101187499991163, 2.977408999572648707, 8.330302781871752771 ) ) ;
#37402=EDGE_LOOP ( 'NONE', ( #13484, #46370, #29504, #28413 ) ) ;
#37413=EDGE_CURVE ( 'NONE', #11426, #28973, #44903, .T. ) ;
#37416=CARTESIAN_POINT ( 'NONE',  ( -2.977408999572647819, 7.188101187499991163, 10.58030278187175455 ) ) ;
#37417=ORIENTED_EDGE ( 'NONE', *, *, #32053, .T. ) ;
#37427=CARTESIAN_POINT ( 'NONE',  ( 1.320432766682872962E-15, -7.188101187499992051, 2.236552781871754103 ) ) ;
#37442=CARTESIAN_POINT ( 'NONE',  ( -4.898587196589407898E-16, 7.999999999999991118, 27.45530277982336642 ) ) ;
#37455=CARTESIAN_POINT ( 'NONE',  ( -7.999999999999989342, -3.313708498984762496, 5.611552783920146226 ) ) ;
#37470=CARTESIAN_POINT ( 'NONE',  ( 3.317071493978883456, -8.008118988124989457, 8.981865283940631883 ) ) ;
#37478=CARTESIAN_POINT ( 'NONE',  ( -7.188101187499990274, -2.977408999572651815, 4.580302781871752771 ) ) ;
#37492=CARTESIAN_POINT ( 'NONE',  ( -4.401442555609577197E-16, 7.188101187499992051, 25.11155278187175810 ) ) ;
#37498=CARTESIAN_POINT ( 'NONE',  ( -4.041240684891906021, 6.985286989850277628, -0.000000000000000000 ) ) ;
#37502=VECTOR ( 'NONE', #9357, 1000.000000000000000 ) ;
#37513=CARTESIAN_POINT ( 'NONE',  ( 3.313708498984756279, 7.999999999999991118, 24.54905278392014978 ) ) ;
#37519=CARTESIAN_POINT ( 'NONE',  ( 7.188101187499993827, -2.977408999572645598, 20.51780278187175810 ) ) ;
#37521=CARTESIAN_POINT ( 'NONE',  ( 1.469576158976822172E-15, -7.999999999999991118, 22.39280278392014623 ) ) ;
#37537=CARTESIAN_POINT ( 'NONE',  ( -3.313708498984757167, 7.999999999999991118, 6.549052779823365533 ) ) ;
#37548=CARTESIAN_POINT ( 'NONE',  ( -3.313708498984757611, 7.999999999999991118, 5.236552783920146226 ) ) ;
#37555=VERTEX_POINT ( 'NONE', #42182 ) ;
#37567=CARTESIAN_POINT ( 'NONE',  ( 3.317071493978883456, -8.008118988124989457, 23.98186528394063899 ) ) ;
#37602=CARTESIAN_POINT ( 'NONE',  ( -7.188101187499991163, 2.977408999572646930, 27.26780278187175099 ) ) ;
#37630=CARTESIAN_POINT ( 'NONE',  ( -4.898587196589407898E-16, 7.999999999999991118, 27.45530277982336642 ) ) ;
#37646=DIRECTION ( 'NONE',  ( -0.000000000000000000, -0.000000000000000000, 1.000000000000000000 ) ) ;
#37649=CARTESIAN_POINT ( 'NONE',  ( 5.656854249492376141, -5.656854249492374365, 21.08030278392014623 ) ) ;
#37659=CARTESIAN_POINT ( 'NONE',  ( 1.469576158976822172E-15, -7.999999999999991118, 26.89280278392014623 ) ) ;
#37667=ORIENTED_EDGE ( 'NONE', *, *, #32578, .F. ) ;
#37670=CARTESIAN_POINT ( 'NONE',  ( 2.977408999572646486, 7.188101187499992051, 19.01780278187175099 ) ) ;
#37681=CARTESIAN_POINT ( 'NONE',  ( -5.656854249492373476, -5.656854249492376141, 11.70530278392014445 ) ) ;
#37691=CARTESIAN_POINT ( 'NONE',  ( -7.188101187499990274, -2.977408999572651371, 19.58030278187175455 ) ) ;
#37697=CARTESIAN_POINT ( 'NONE',  ( 0.000000000000000000, 0.000000000000000000, 30.00000000000000000 ) ) ;
#37709=CARTESIAN_POINT ( 'NONE',  ( 1.469576158976822172E-15, -7.999999999999991118, 26.89280278392014623 ) ) ;
#37716=CARTESIAN_POINT ( 'NONE',  ( 7.188101187499993827, -2.977408999572645598, 17.51780278187175455 ) ) ;
#37733=CARTESIAN_POINT ( 'NONE',  ( -4.898587196589407898E-16, 7.999999999999991118, 6.455302779823365533 ) ) ;
#37746=CARTESIAN_POINT ( 'NONE',  ( 7.999999999836578723, -5.113295603412193572E-05, 3.267801294049292871 ) ) ;
#37749=CARTESIAN_POINT ( 'NONE',  ( 7.999999999999991118, 3.313708498984757611, 13.73030278432982421 ) ) ;
#37761=AXIS2_PLACEMENT_3D ( 'NONE', #35682, #42798, #30017 ) ;
#37782=CARTESIAN_POINT ( 'NONE',  ( -7.188101187499990274, -2.977408999572651371, 7.580302781871751883 ) ) ;
#37794=CARTESIAN_POINT ( 'NONE',  ( -4.401442555609577197E-16, 7.188101187499992051, 13.48655278187175455 ) ) ;
#37805=CARTESIAN_POINT ( 'NONE',  ( 7.188101187499993827, -2.977408999572645598, 4.017802781871751883 ) ) ;
#37823=CARTESIAN_POINT ( 'NONE',  ( 3.313708498984756279, 7.999999999999991118, 27.36155277982336642 ) ) ;
#37830=ORIENTED_EDGE ( 'NONE', *, *, #53513, .F. ) ;
#37833=CARTESIAN_POINT ( 'NONE',  ( -5.656854249492373476, -5.656854249492376141, 2.705302783920143561 ) ) ;
#37859=CARTESIAN_POINT ( 'NONE',  ( -2.977408999572647819, 7.188101187499992051, 4.205302781871752771 ) ) ;
#37866=EDGE_CURVE ( 'NONE', #72561, #54725, #62718, .T. ) ;
#37870=CARTESIAN_POINT ( 'NONE',  ( 7.188101187499993827, -2.977408999572645598, 27.64280278187175810 ) ) ;
#37873=ORIENTED_EDGE ( 'NONE', *, *, #285, .F. ) ;
#37875=CARTESIAN_POINT ( 'NONE',  ( -7.999920465054277230, 1.060465953394919891, -0.000000000000000000 ) ) ;
#37888=CARTESIAN_POINT ( 'NONE',  ( 7.999999999843520726, -5.003525229023116430E-05, 24.26780136833107093 ) ) ;
#37894=CARTESIAN_POINT ( 'NONE',  ( 1.320432766682872962E-15, -7.188101187499992051, 20.23655278187175455 ) ) ;
#37905=CARTESIAN_POINT ( 'NONE',  ( 1.818965066830242394, -7.999999999999990230, -0.05573584732409991860 ) ) ;
#37913=CARTESIAN_POINT ( 'NONE',  ( 1.469576158976822172E-15, -7.999999999999991118, 8.705302779823362869 ) ) ;
#37941=CARTESIAN_POINT ( 'NONE',  ( -5.662595241051935346, 5.662595241051935346, 26.32561528394063188 ) ) ;
#37948=CARTESIAN_POINT ( 'NONE',  ( -5.652405255243663440, -4.866521301246740983, 0.0006792023777823770567 ) ) ;
#37977=CARTESIAN_POINT ( 'NONE',  ( 1.320432766682872962E-15, -7.188101187499992051, 23.23655278187175455 ) ) ;
#38002=CARTESIAN_POINT ( 'NONE',  ( -7.999999999999991118, 3.313708498984756723, 26.23655277982336642 ) ) ;
#38005=EDGE_LOOP ( 'NONE', ( #32639, #66133, #31274, #18468, #28008, #67991 ) ) ;
#38019=CARTESIAN_POINT ( 'NONE',  ( 1.469576158976822172E-15, -7.999999999999991118, 16.39280278392014978 ) ) ;
#38021=FACE_OUTER_BOUND ( 'NONE', #66819, .T. ) ;
#38041=CARTESIAN_POINT ( 'NONE',  ( 1.320432766682872962E-15, -7.188101187499992051, 12.36155278187175277 ) ) ;
#38052=CARTESIAN_POINT ( 'NONE',  ( -3.313708498984758943, -7.999999999999989342, 10.29905278392014623 ) ) ;
#38053=CARTESIAN_POINT ( 'NONE',  ( 7.999999999999991118, 0.000000000000000000, 30.00000000000000000 ) ) ;
#38066=CARTESIAN_POINT ( 'NONE',  ( 2.977408999572646486, 7.188101187499991163, 17.51780278187175455 ) ) ;
#38083=CARTESIAN_POINT ( 'NONE',  ( 3.313708498984756279, 7.999999999999991118, 27.54905278392014623 ) ) ;
#38087=LINE ( 'NONE', #73802, #7461 ) ;
#38089=CARTESIAN_POINT ( 'NONE',  ( 2.977408999572650927, -7.188101187499990274, 14.33030278187175277 ) ) ;
#38103=CARTESIAN_POINT ( 'NONE',  ( -7.999999999999989342, -3.313708498984762496, 11.42405277982336465 ) ) ;
#38118=CARTESIAN_POINT ( 'NONE',  ( 1.469576158976822172E-15, -7.999999999999991118, 2.892802783920144005 ) ) ;
#38121=CARTESIAN_POINT ( 'NONE',  ( 3.313708498984756279, 7.999999999999991118, 9.417802784329825982 ) ) ;
#38132=ORIENTED_EDGE ( 'NONE', *, *, #7614, .T. ) ;
#38139=ADVANCED_FACE ( 'NONE', ( #27540 ), #73568, .F. ) ;
#38150=CARTESIAN_POINT ( 'NONE',  ( -7.188101187499991163, 2.977408999572646930, 4.392802781871752771 ) ) ;
#38165=CARTESIAN_POINT ( 'NONE',  ( -5.082755093536317936, -5.082755093536320601, 14.04905278187175455 ) ) ;
#38168=CARTESIAN_POINT ( 'NONE',  ( 1.469576158976822172E-15, -7.999999999999991118, 5.705302779823364645 ) ) ;
#38178=CARTESIAN_POINT ( 'NONE',  ( -5.082755093536319713, 5.082755093536319713, 6.174052781871754547 ) ) ;
#38200=CARTESIAN_POINT ( 'NONE',  ( -7.999999999999989342, -3.313708498984762496, 25.11155278392014978 ) ) ;
#38207=CARTESIAN_POINT ( 'NONE',  ( -5.656854249492375253, 5.656854249492375253, 27.69905278432982598 ) ) ;
#38210=DIRECTION ( 'NONE',  ( -0.000000000000000000, -0.000000000000000000, 1.000000000000000000 ) ) ;
#38228=CARTESIAN_POINT ( 'NONE',  ( -5.082755093536319713, 5.082755093536319713, 5.799052781871753659 ) ) ;
#38239=CARTESIAN_POINT ( 'NONE',  ( -5.656854249492373476, -5.656854249492376141, 10.01780277982336465 ) ) ;
#38240=CARTESIAN_POINT ( 'NONE',  ( 7.188101187499992051, 8.802885111219154394E-16, 27.73655278187175455 ) ) ;
#38243=VERTEX_POINT ( 'NONE', #30883 ) ;
#38253=( BOUNDED_CURVE ( )  B_SPLINE_CURVE ( 2, ( #3532, #61243, #3160, #55973, #73313, #43892, #38239, #21246, #44640 ),
 .UNSPECIFIED., .F., .F. ) 
 B_SPLINE_CURVE_WITH_KNOTS ( ( 3, 2, 2, 2, 3 ),
 ( 0.6578947368421053099, 0.6644736842105263275, 0.6710526315789473450, 0.6776315789473684736, 0.6842105263157894912 ),
 .UNSPECIFIED. ) 
 CURVE ( )  GEOMETRIC_REPRESENTATION_ITEM ( )  RATIONAL_B_SPLINE_CURVE ( ( 1.000000000000000000, 0.9238795325112867385, 1.000000000000000000, 0.9238795325112867385, 1.000000000000000000, 0.9238795325112867385, 1.000000000000000000, 0.9238795325112867385, 1.000000000000000000 ) ) 
 REPRESENTATION_ITEM ( '' )  );
#38265=CARTESIAN_POINT ( 'NONE',  ( -7.188101187499992051, 0.000000000000000000, 21.36155278187175455 ) ) ;
#38284=CARTESIAN_POINT ( 'NONE',  ( 7.999999999999991118, 3.313708498984757611, 10.67405277982336465 ) ) ;
#38294=CARTESIAN_POINT ( 'NONE',  ( 7.999999999999991118, -3.647060904601942273E-05, 4.767801752109533275 ) ) ;
#38296=CARTESIAN_POINT ( 'NONE',  ( 5.656854249492374365, 5.656854249492375253, 19.95530278392014623 ) ) ;
#38303=CIRCLE ( 'NONE', #51532, 20.00000000000000355 ) ;
#38314=CARTESIAN_POINT ( 'NONE',  ( -8.008118988124989457, -3.317071493978883900, 22.10686528394063188 ) ) ;
#38333=CARTESIAN_POINT ( 'NONE',  ( -3.313708498984757611, 7.999999999999991118, 14.04905277982336465 ) ) ;
#38346=CARTESIAN_POINT ( 'NONE',  ( -7.188101187499991163, 2.977408999572646930, 22.76780278187175455 ) ) ;
#38347=DIRECTION ( 'NONE',  ( -0.000000000000000000, -0.000000000000000000, 1.000000000000000000 ) ) ;
#38351=DIRECTION ( 'NONE',  ( -0.000000000000000000, -0.000000000000000000, 1.000000000000000000 ) ) ;
#38372=CARTESIAN_POINT ( 'NONE',  ( -5.656854249492373476, -5.656854249492376141, 25.01780277982336642 ) ) ;
#38378=LINE ( 'NONE', #4417, #67665 ) ;
#38388=LINE ( 'NONE', #27422, #38396 ) ;
#38392=CARTESIAN_POINT ( 'NONE',  ( 5.656854249492374365, 5.656854249492375253, 16.95530278392014978 ) ) ;
#38396=VECTOR ( 'NONE', #15353, 1000.000000000000000 ) ;
#38415=CARTESIAN_POINT ( 'NONE',  ( -7.188101187499992051, 0.000000000000000000, 16.48655278187175810 ) ) ;
#38425=CARTESIAN_POINT ( 'NONE',  ( -7.999999999999989342, -3.313708498984762496, 7.111552783920144449 ) ) ;
#38438=CARTESIAN_POINT ( 'NONE',  ( 5.082755093536320601, -5.082755093536318824, 15.54905278187175455 ) ) ;
#38451=LINE ( 'NONE', #43723, #58861 ) ;
#38462=CARTESIAN_POINT ( 'NONE',  ( 2.977408999572650927, -7.188101187499990274, 17.33030278187175455 ) ) ;
#38478=EDGE_CURVE ( 'NONE', #51172, #51815, #67060, .T. ) ;
#38479=CARTESIAN_POINT ( 'NONE',  ( 5.656854249492374365, 5.656854249492375253, 12.26780277982336642 ) ) ;
#38481=EDGE_CURVE ( 'NONE', #4443, #3266, #52611, .T. ) ;
#38491=LINE ( 'NONE', #49418, #14716 ) ;
#38493=CARTESIAN_POINT ( 'NONE',  ( 5.656854249492374365, 5.656854249492375253, 9.324052784329824206 ) ) ;
#38500=EDGE_LOOP ( 'NONE', ( #43804, #60238, #55512, #15090 ) ) ;
#38528=CARTESIAN_POINT ( 'NONE',  ( 7.188101187499993827, -2.977408999572645598, 0.6428027818717528818 ) ) ;
#38541=CARTESIAN_POINT ( 'NONE',  ( -5.082755093536317936, -5.082755093536320601, 9.549052781871754547 ) ) ;
#38546=AXIS2_PLACEMENT_3D ( 'NONE', #65969, #37311, #25227 ) ;
#38557=CARTESIAN_POINT ( 'NONE',  ( -5.082755093536317936, -5.082755093536320601, 2.049052781871754103 ) ) ;
#38574=CARTESIAN_POINT ( 'NONE',  ( 1.469576158976822172E-15, -7.999999999999991118, 25.20530277982336642 ) ) ;
#38585=CARTESIAN_POINT ( 'NONE',  ( -7.999999999999991118, 0.000000000000000000, 1.017802783920145782 ) ) ;
#38597=VERTEX_POINT ( 'NONE', #44787 ) ;
#38620=CARTESIAN_POINT ( 'NONE',  ( 7.188101187499991163, 2.977408999572648707, 23.33030278187175455 ) ) ;
#38644=CARTESIAN_POINT ( 'NONE',  ( -5.082755093536319713, 5.082755093536319713, 21.17405278187175455 ) ) ;
#38655=FACE_OUTER_BOUND ( 'NONE', #25317, .T. ) ;
#38663=CARTESIAN_POINT ( 'NONE',  ( -7.999999999999991118, 0.000000000000000000, 8.330302779823362869 ) ) ;
#38673=CARTESIAN_POINT ( 'NONE',  ( -7.999999999999991118, 1.918013197678222425E-05, 10.01780224128419405 ) ) ;
#38675=CARTESIAN_POINT ( 'NONE',  ( -4.898587196589407898E-16, 7.999999999999991118, 20.14280278392014623 ) ) ;
#38691=CARTESIAN_POINT ( 'NONE',  ( -4.903558642999205574E-16, 8.008118988124991233, 21.63811528394063188 ) ) ;
#38692=CARTESIAN_POINT ( 'NONE',  ( -4.898587196589407898E-16, 7.999999999999991118, 23.14280278392014978 ) ) ;
#38729=CARTESIAN_POINT ( 'NONE',  ( -4.401442555609577197E-16, 7.188101187499992051, 23.98655278187175455 ) ) ;
#38753=CARTESIAN_POINT ( 'NONE',  ( -5.656854249492375253, 5.656854249492375253, 27.64280277982336642 ) ) ;
#38770=CARTESIAN_POINT ( 'NONE',  ( -7.999999999999991118, 3.313708498984756723, 11.42405278392014623 ) ) ;
#38789=CARTESIAN_POINT ( 'NONE',  ( 7.188101187499992051, 8.802885111219154394E-16, 15.73655278187175632 ) ) ;
#38813=CARTESIAN_POINT ( 'NONE',  ( 2.977408999572650927, -7.188101187499990274, 13.95530278187175277 ) ) ;
#38835=CARTESIAN_POINT ( 'NONE',  ( 1.320432766682872962E-15, -7.188101187499992051, 15.73655278187175632 ) ) ;
#38850=CARTESIAN_POINT ( 'NONE',  ( -5.656854249492373476, -5.656854249492376141, 10.01780277982336465 ) ) ;
#38851=CARTESIAN_POINT ( 'NONE',  ( -7.999985424683830004, -3.313723074300923610, 4.111553367083139676 ) ) ;
#38865=CARTESIAN_POINT ( 'NONE',  ( -4.898587196589407898E-16, 7.999999999999991118, 9.511552784329824206 ) ) ;
#38875=ORIENTED_EDGE ( 'NONE', *, *, #8908, .F. ) ;
#38895=CARTESIAN_POINT ( 'NONE',  ( 7.188101187499992051, 8.802885111219154394E-16, 0.7365527818717527708 ) ) ;
#38908=CARTESIAN_POINT ( 'NONE',  ( -4.401442555609577197E-16, 7.188101187499992051, 4.486552781871752771 ) ) ;
#38943=CARTESIAN_POINT ( 'NONE',  ( 3.313708498984762496, -7.999999999999989342, 25.48655278392014623 ) ) ;
#38949=CARTESIAN_POINT ( 'NONE',  ( 1.469576158976822172E-15, -7.999999999999991118, -0.1071972160798552454 ) ) ;
#38958=CARTESIAN_POINT ( 'NONE',  ( -7.999999999999991118, -1.759867635265925965E-05, 1.017803281814245064 ) ) ;
#38982=CARTESIAN_POINT ( 'NONE',  ( 7.188101187499991163, 2.977408999572648707, 17.33030278187175455 ) ) ;
#38985=EDGE_CURVE ( 'NONE', #49310, #6596, #24170, .T. ) ;
#39008=CARTESIAN_POINT ( 'NONE',  ( -7.188101187499990274, -2.977408999572651815, 16.95530278187175455 ) ) ;
#39026=CARTESIAN_POINT ( 'NONE',  ( 7.999999999999992895, -3.313708498984756279, 1.486552779823364201 ) ) ;
#39030=ORIENTED_EDGE ( 'NONE', *, *, #9204, .T. ) ;
#39040=CARTESIAN_POINT ( 'NONE',  ( -7.999999999995399236, -5.826008446853342637E-06, 20.51801720710344767 ) ) ;
#39057=CARTESIAN_POINT ( 'NONE',  ( -5.662595241051933570, -5.662595241051936235, 17.70061528394063188 ) ) ;
#39083=CARTESIAN_POINT ( 'NONE',  ( -3.313708498984759387, -7.999999999999989342, 2.611552779823365533 ) ) ;
#39089=CARTESIAN_POINT ( 'NONE',  ( -5.082755093536317936, -5.082755093536320601, 24.54905278187175810 ) ) ;
#39107=CARTESIAN_POINT ( 'NONE',  ( -7.999999999999991118, 0.000000000000000000, 12.83030277982336465 ) ) ;
#39113=CARTESIAN_POINT ( 'NONE',  ( -3.313708498984758943, -7.999999999999989342, 28.11155277982336642 ) ) ;
#39120=CARTESIAN_POINT ( 'NONE',  ( -7.999999999999991118, 0.000000000000000000, 14.33030277982336465 ) ) ;
#39128=CARTESIAN_POINT ( 'NONE',  ( -7.999999999999991118, 0.000000000000000000, 11.33030277982336642 ) ) ;
#39131=CARTESIAN_POINT ( 'NONE',  ( 3.313708498984762496, -7.999999999999989342, 13.48655278392014445 ) ) ;
#39154=CARTESIAN_POINT ( 'NONE',  ( -7.188101187499992051, 2.977408999572646930, 17.89280278187175455 ) ) ;
#39175=CARTESIAN_POINT ( 'NONE',  ( 5.082755093536318824, 5.082755093536319713, 9.924052781871754547 ) ) ;
#39187=AXIS2_PLACEMENT_3D ( 'NONE', #42488, #2877, #59851 ) ;
#39191=EDGE_CURVE ( 'NONE', #852, #6758, #51318, .T. ) ;
#39202=CARTESIAN_POINT ( 'NONE',  ( -7.188101187499992051, 0.000000000000000000, 15.36155278187175455 ) ) ;
#39219=CARTESIAN_POINT ( 'NONE',  ( 7.999999999999992895, -3.313708498984756279, 1.486552779823364201 ) ) ;
#39235=CARTESIAN_POINT ( 'NONE',  ( -5.656854249492375253, 5.656854249492375253, 5.199052784329824206 ) ) ;
#39236=DIRECTION ( 'NONE',  ( 1.000000000000000000, 0.000000000000000000, 0.000000000000000000 ) ) ;
#39265=CARTESIAN_POINT ( 'NONE',  ( 5.082755093536318824, 5.082755093536319713, 3.924052781871752327 ) ) ;
#39279=CARTESIAN_POINT ( 'NONE',  ( 7.188101187499993827, -2.977408999572645598, 8.517802781871754547 ) ) ;
#39293=CARTESIAN_POINT ( 'NONE',  ( 7.188101187499992051, 2.977408999572647819, 1.205302781871753215 ) ) ;
#39299=VERTEX_POINT ( 'NONE', #13162 ) ;
#39311=CARTESIAN_POINT ( 'NONE',  ( 3.313708498984756279, 7.999999999999991118, 22.86155277982337353 ) ) ;
#39322=CARTESIAN_POINT ( 'NONE',  ( 0.000000000000000000, 116.0729912458811839, 42.10166426739785095 ) ) ;
#39323=CARTESIAN_POINT ( 'NONE',  ( 5.656854249492376141, -5.656854249492374365, 0.08030278392014492117 ) ) ;
#39327=VERTEX_POINT ( 'NONE', #42582 ) ;
#39345=ORIENTED_EDGE ( 'NONE', *, *, #3689, .F. ) ;
#39352=CARTESIAN_POINT ( 'NONE',  ( -5.082755093536317936, -5.082755093536320601, 16.67405278187175810 ) ) ;
#39369=CARTESIAN_POINT ( 'NONE',  ( 7.999999999999948486, 3.313708498984800244, 7.674052779823369086 ) ) ;
#39377=CARTESIAN_POINT ( 'NONE',  ( -7.188101187499992051, 0.000000000000000000, 13.86155278187175455 ) ) ;
#39387=CARTESIAN_POINT ( 'NONE',  ( -7.999999999999991118, 3.313708498984757167, 17.42405278392013912 ) ) ;
#39395=CARTESIAN_POINT ( 'NONE',  ( 5.656854249492374365, 5.656854249492375253, 3.267802779823362425 ) ) ;
#39396=CARTESIAN_POINT ( 'NONE',  ( -5.656854249492373476, -5.656854249492376141, 20.70530278392014623 ) ) ;
#39398=ORIENTED_EDGE ( 'NONE', *, *, #3689, .T. ) ;
#39414=ORIENTED_EDGE ( 'NONE', *, *, #8491, .F. ) ;
#39425=CARTESIAN_POINT ( 'NONE',  ( -3.313708498984757611, 7.999999999999991118, 8.236552783920144449 ) ) ;
#39426=CARTESIAN_POINT ( 'NONE',  ( -4.903558642999205574E-16, 8.008118988124991233, 18.63811528394063188 ) ) ;
#39450=CARTESIAN_POINT ( 'NONE',  ( -8.000000000000033751, -3.313708498984719864, 2.424052779823363757 ) ) ;
#39453=CARTESIAN_POINT ( 'NONE',  ( -7.833566452622682696, -1.888151595330326726, -0.000000000000000000 ) ) ;
#39457=CARTESIAN_POINT ( 'NONE',  ( 5.082755093536318824, 5.082755093536319713, 25.29905278187175810 ) ) ;
#39480=EDGE_CURVE ( 'NONE', #60780, #38597, #37222, .T. ) ;
#39485=CARTESIAN_POINT ( 'NONE',  ( 7.999999999999992895, -3.313708498984756279, 20.98655277982336642 ) ) ;
#39494=CARTESIAN_POINT ( 'NONE',  ( 1.469576158976822172E-15, -7.999999999999991118, 8.705302779823362869 ) ) ;
#39505=CARTESIAN_POINT ( 'NONE',  ( -5.656854249492373476, -5.656854249492376141, 14.70530278392014800 ) ) ;
#39519=CARTESIAN_POINT ( 'NONE',  ( -5.656854249492373476, -5.656854249492376141, 28.01780277982336642 ) ) ;
#39526=ORIENTED_EDGE ( 'NONE', *, *, #66091, .F. ) ;
#39553=CARTESIAN_POINT ( 'NONE',  ( -2.977408999572647819, 7.188101187499991163, 11.70530278187175099 ) ) ;
#39556=ORIENTED_EDGE ( 'NONE', *, *, #45418, .T. ) ;
#39577=CARTESIAN_POINT ( 'NONE',  ( 5.082755093536318824, 5.082755093536319713, 8.799052781871752771 ) ) ;
#39590=CARTESIAN_POINT ( 'NONE',  ( -7.999999999999991118, 0.000000000000000000, 3.830302779823362869 ) ) ;
#39607=CARTESIAN_POINT ( 'NONE',  ( 3.313708498984756279, 7.999999999999991118, 4.917802784329824206 ) ) ;
#39637=CARTESIAN_POINT ( 'NONE',  ( 2.977408999572646486, 7.188101187499991163, 2.517802781871750550 ) ) ;
#39650=CARTESIAN_POINT ( 'NONE',  ( -2.977408999572648707, -7.188101187499990274, 6.642802781871754547 ) ) ;
#39662=CARTESIAN_POINT ( 'NONE',  ( 5.082755093536318824, 5.082755093536319713, 1.299052781871753215 ) ) ;
#39676=CARTESIAN_POINT ( 'NONE',  ( 5.656854249492374365, 5.656854249492375253, 22.76780277982336642 ) ) ;
#39681=CARTESIAN_POINT ( 'NONE',  ( 7.999999999999991118, 3.377145119393935320E-05, 0.2678037393673578515 ) ) ;
#39686=CARTESIAN_POINT ( 'NONE',  ( -5.656854249492375253, 5.656854249492375253, 23.19905278432982598 ) ) ;
#39720=CARTESIAN_POINT ( 'NONE',  ( 7.188101187499991163, 2.977408999572648707, 20.33030278187175455 ) ) ;
#39732=ORIENTED_EDGE ( 'NONE', *, *, #63680, .T. ) ;
#39741=CARTESIAN_POINT ( 'NONE',  ( -2.977408999572647819, -7.188101187499990274, 18.64280278187176521 ) ) ;
#39759=CARTESIAN_POINT ( 'NONE',  ( -5.867882488397293095, -5.445826010587458299, 1.009359473472040802 ) ) ;
#39786=CARTESIAN_POINT ( 'NONE',  ( -7.999999999999991118, -1.288204405367768053E-10, 8.517802783929960597 ) ) ;
#39787=CARTESIAN_POINT ( 'NONE',  ( 8.008118988124993010, -3.317071493978877239, 19.66936528394063544 ) ) ;
#39809=CARTESIAN_POINT ( 'NONE',  ( -3.313708498984757167, 7.999999999999991118, 8.236552783920144449 ) ) ;
#39824=CARTESIAN_POINT ( 'NONE',  ( 7.188101187499993827, -2.977408999572645598, 19.01780278187175810 ) ) ;
#39830=CARTESIAN_POINT ( 'NONE',  ( -7.999999999999991118, 9.797174393178815797E-16, 30.00000000000000000 ) ) ;
#39831=DIRECTION ( 'NONE',  ( 0.000000000000000000, 0.2588190451025145777, -0.9659258262890699775 ) ) ;
#39841=CIRCLE ( 'NONE', #62714, 7.999999999999991118 ) ;
#39851=CARTESIAN_POINT ( 'NONE',  ( 7.999999999999991118, 3.313708498984757611, 18.17405277982336642 ) ) ;
#39870=CARTESIAN_POINT ( 'NONE',  ( -3.313708498984758943, -7.999999999999989342, 13.29905278392014800 ) ) ;
#39920=CARTESIAN_POINT ( 'NONE',  ( 5.082755093536318824, 5.082755093536319713, 14.42405278187175455 ) ) ;
#39923=( BOUNDED_CURVE ( )  B_SPLINE_CURVE ( 2, ( #22296, #44959, #12102, #17763, #28342, #23052, #51350, #68704, #16259 ),
 .UNSPECIFIED., .F., .F. ) 
 B_SPLINE_CURVE_WITH_KNOTS ( ( 3, 2, 2, 2, 3 ),
 ( 0.000000000000000000, 0.006578947368421057471, 0.01315789473684211494, 0.01973684210526317415, 0.02631578947368422988 ),
 .UNSPECIFIED. ) 
 CURVE ( )  GEOMETRIC_REPRESENTATION_ITEM ( )  RATIONAL_B_SPLINE_CURVE ( ( 1.000000000000000000, 0.9238795325112867385, 1.000000000000000000, 0.9238795325112867385, 1.000000000000000000, 0.9238795325112867385, 1.000000000000000000, 0.9238795325112865164, 1.000000000000000222 ) ) 
 REPRESENTATION_ITEM ( '' )  );
#39946=CARTESIAN_POINT ( 'NONE',  ( 2.977408999572646486, 7.188101187499991163, 10.39280278187175810 ) ) ;
#39950=CARTESIAN_POINT ( 'NONE',  ( -5.656854249492375253, 5.656854249492375253, 0.6990527843298235400 ) ) ;
#39962=CARTESIAN_POINT ( 'NONE',  ( -7.999999999999991118, 3.313708498984756723, 2.236552779823365533 ) ) ;
#39963=LINE ( 'NONE', #34695, #71007 ) ;
#39978=CARTESIAN_POINT ( 'NONE',  ( -7.999999999999989342, -3.313708498984762496, 8.480302784329822430 ) ) ;
#39980=DIRECTION ( 'NONE',  ( -0.000000000000000000, -0.000000000000000000, 1.000000000000000000 ) ) ;
#39986=CARTESIAN_POINT ( 'NONE',  ( 7.188101187499992051, 8.802885111219154394E-16, 27.73655278187175455 ) ) ;
#40008=CARTESIAN_POINT ( 'NONE',  ( -7.188101187499991163, 2.977408999572646930, 2.892802781871751439 ) ) ;
#40009=ORIENTED_EDGE ( 'NONE', *, *, #74420, .T. ) ;
#40022=CARTESIAN_POINT ( 'NONE',  ( 5.082755093536320601, -5.082755093536318824, 8.424052781871752771 ) ) ;
#40032=CARTESIAN_POINT ( 'NONE',  ( -4.401442555609577197E-16, 7.188101187499992051, 25.48655278187175810 ) ) ;
#40038=CARTESIAN_POINT ( 'NONE',  ( 7.999999999996472155, 7.505344305739403062E-06, 9.267802996260090964 ) ) ;
#40049=CARTESIAN_POINT ( 'NONE',  ( -7.999999999999991118, 0.000000000000000000, 20.33030277982336642 ) ) ;
#40064=CARTESIAN_POINT ( 'NONE',  ( 3.313708498984756279, 7.999999999999991118, 22.91780278432982598 ) ) ;
#40082=FACE_OUTER_BOUND ( 'NONE', #68531, .T. ) ;
#40095=CARTESIAN_POINT ( 'NONE',  ( -7.188101187499990274, -2.977408999572651371, 18.08030278187175455 ) ) ;
#40116=CARTESIAN_POINT ( 'NONE',  ( 5.082755093536320601, -5.082755093536318824, 15.92405278187175632 ) ) ;
#40132=ADVANCED_FACE ( 'NONE', ( #59423 ), #23970, .F. ) ;
#40133=EDGE_CURVE ( 'NONE', #1239, #34597, #12706, .T. ) ;
#40138=CARTESIAN_POINT ( 'NONE',  ( 7.999999999999991118, 3.313708498984757611, 4.674052779823363757 ) ) ;
#40144=CARTESIAN_POINT ( 'NONE',  ( 7.999999999999991118, 3.313708498984758055, 10.67405277982336465 ) ) ;
#40168=CARTESIAN_POINT ( 'NONE',  ( -3.317071493978880348, -8.008118988124989457, 14.79436528394063011 ) ) ;
#40185=CARTESIAN_POINT ( 'NONE',  ( 3.313708498984762496, -7.999999999999989342, 5.986552783920146226 ) ) ;
#40186=ORIENTED_EDGE ( 'NONE', *, *, #24158, .F. ) ;
#40199=CARTESIAN_POINT ( 'NONE',  ( -7.188101187499991163, 2.977408999572646930, 16.76780278187175099 ) ) ;
#40202=DIRECTION ( 'NONE',  ( 0.000000000000000000, 0.2588190451025143557, -0.9659258262890699775 ) ) ;
#40224=CARTESIAN_POINT ( 'NONE',  ( 1.469576158976822172E-15, -7.999999999999991118, 19.20530277982336642 ) ) ;
#40243=CARTESIAN_POINT ( 'NONE',  ( 1.469576158976822172E-15, -7.999999999999991118, 13.39280278392014623 ) ) ;
#40281=CARTESIAN_POINT ( 'NONE',  ( 3.313708498984756279, 7.999999999999991118, 6.361552779823365533 ) ) ;
#40292=CARTESIAN_POINT ( 'NONE',  ( 7.188101187499993827, -2.977408999572645598, 5.142802781871752771 ) ) ;
#40316=CARTESIAN_POINT ( 'NONE',  ( -4.401442555609577197E-16, 7.188101187499992051, 7.486552781871751883 ) ) ;
#40319=CARTESIAN_POINT ( 'NONE',  ( -7.999999999999991118, 0.000000000000000000, 2.386552784329821542 ) ) ;
#40329=CARTESIAN_POINT ( 'NONE',  ( 7.999999999999991118, 9.797174393178815797E-16, 1.580302779823364201 ) ) ;
#40346=CARTESIAN_POINT ( 'NONE',  ( -5.656854249492373476, -5.656854249492376141, 5.574052784329824206 ) ) ;
#40353=CARTESIAN_POINT ( 'NONE',  ( 7.188101187499992051, 2.977408999572647819, 24.83030278187175455 ) ) ;
#40368=CARTESIAN_POINT ( 'NONE',  ( 5.656854249492376141, -5.656854249492374365, 19.58030278392014978 ) ) ;
#40380=CARTESIAN_POINT ( 'NONE',  ( -7.188101187499991163, 2.977408999572646930, 26.89280278187175455 ) ) ;
#40393=CARTESIAN_POINT ( 'NONE',  ( -2.977408999572647819, 7.188101187499991163, 6.080302781871753659 ) ) ;
#40398=CARTESIAN_POINT ( 'NONE',  ( -8.008118988124989457, -3.317071493978883900, 5.606865283940630995 ) ) ;
#40405=CARTESIAN_POINT ( 'NONE',  ( 5.082755093536320601, -5.082755093536318824, 26.42405278187175810 ) ) ;
#40414=EDGE_LOOP ( 'NONE', ( #5293, #41190, #19520 ) ) ;
#40422=CARTESIAN_POINT ( 'NONE',  ( 7.999999999999992895, -3.313708498984756279, 22.48655277982336287 ) ) ;
#40435=CARTESIAN_POINT ( 'NONE',  ( 3.313708498984762496, -7.999999999999989342, 22.35530278432982598 ) ) ;
#40440=ORIENTED_EDGE ( 'NONE', *, *, #32053, .F. ) ;
#40467=CARTESIAN_POINT ( 'NONE',  ( -5.082755093536319713, 5.082755093536319713, 19.29905278187175455 ) ) ;
#40491=CARTESIAN_POINT ( 'NONE',  ( -7.188101187499992051, 0.000000000000000000, 15.36155278187175455 ) ) ;
#40512=CARTESIAN_POINT ( 'NONE',  ( -7.999999999999991118, 0.000000000000000000, 2.330302779823365089 ) ) ;
#40514=ORIENTED_EDGE ( 'NONE', *, *, #11317, .T. ) ;
#40515=ORIENTED_EDGE ( 'NONE', *, *, #27929, .F. ) ;
#40536=CARTESIAN_POINT ( 'NONE',  ( -5.662595241051935346, 5.662595241051935346, 14.32561528394063188 ) ) ;
#40543=CARTESIAN_POINT ( 'NONE',  ( -4.401442555609577197E-16, 7.188101187499992051, 13.11155278187175277 ) ) ;
#40554=EDGE_CURVE ( 'NONE', #43701, #30305, #33442, .T. ) ;
#40559=CARTESIAN_POINT ( 'NONE',  ( 1.469576158976822172E-15, -7.999999999999991118, 8.892802783920146226 ) ) ;
#40572=CARTESIAN_POINT ( 'NONE',  ( 2.977408999572646486, 7.188101187499991163, 14.89280278187175455 ) ) ;
#40599=CARTESIAN_POINT ( 'NONE',  ( 1.469576158976822172E-15, -7.999999999999991118, 23.70530277982336642 ) ) ;
#40617=CARTESIAN_POINT ( 'NONE',  ( -4.898587196589407898E-16, 7.999999999999991118, 9.642802783920146226 ) ) ;
#40620=ORIENTED_EDGE ( 'NONE', *, *, #4001, .T. ) ;
#40634=CARTESIAN_POINT ( 'NONE',  ( 7.999999999999991118, 3.313708498984758055, 10.86155278392014800 ) ) ;
#40656=( NAMED_UNIT ( * ) PLANE_ANGLE_UNIT ( ) SI_UNIT ( $, .RADIAN. ) );
#40665=CARTESIAN_POINT ( 'NONE',  ( -2.977408999572648707, -7.188101187499990274, 7.767802781871751883 ) ) ;
#40684=CARTESIAN_POINT ( 'NONE',  ( 7.999999999999991118, 9.797174393178815797E-16, 22.58030277982336997 ) ) ;
#40689=CARTESIAN_POINT ( 'NONE',  ( 2.977408999572650927, -7.188101187499990274, 11.33030278187175632 ) ) ;
#40692=CARTESIAN_POINT ( 'NONE',  ( -7.999999999999991118, 0.000000000000000000, 0.8865527843298237620 ) ) ;
#40702=CARTESIAN_POINT ( 'NONE',  ( -3.313708498984757167, 7.999999999999991118, 5.049052779823364645 ) ) ;
#40711=ORIENTED_EDGE ( 'NONE', *, *, #51754, .T. ) ;
#40717=CARTESIAN_POINT ( 'NONE',  ( 5.656854249492374365, 5.656854249492375253, 4.824052784329824206 ) ) ;
#40721=EDGE_LOOP ( 'NONE', ( #31410, #33309, #72919, #70258, #35197, #13239, #23457 ) ) ;
#40723=CARTESIAN_POINT ( 'NONE',  ( 5.082755093536318824, 5.082755093536319713, 26.42405278187175455 ) ) ;
#40733=CARTESIAN_POINT ( 'NONE',  ( -7.999999999999991118, 3.313708498984756723, 17.42405278392014623 ) ) ;
#40744=CARTESIAN_POINT ( 'NONE',  ( -2.977408999572648707, -7.188101187499990274, 22.76780278187175455 ) ) ;
#40764=CARTESIAN_POINT ( 'NONE',  ( -5.662595241051933570, -5.662595241051936235, 1.200615283940629885 ) ) ;
#40768=CARTESIAN_POINT ( 'NONE',  ( 1.469576158976822172E-15, -7.999999999999991118, 7.205302779823365533 ) ) ;
#40770=CARTESIAN_POINT ( 'NONE',  ( 7.188101187499992051, 8.802885111219154394E-16, 26.61155278187175810 ) ) ;
#40788=CARTESIAN_POINT ( 'NONE',  ( 7.999999999999992895, -3.313708498984756279, 20.98655277982336642 ) ) ;
#40803=CARTESIAN_POINT ( 'NONE',  ( -5.656854249492375253, 5.656854249492375253, 26.19905278432982243 ) ) ;
#40819=ORIENTED_EDGE ( 'NONE', *, *, #73691, .T. ) ;
#40825=VECTOR ( 'NONE', #44303, 1000.000000000000000 ) ;
#40838=CARTESIAN_POINT ( 'NONE',  ( -5.082755093536317936, -5.082755093536320601, 12.17405278187175277 ) ) ;
#40839=ORIENTED_EDGE ( 'NONE', *, *, #585, .F. ) ;
#40864=CARTESIAN_POINT ( 'NONE',  ( 7.188101187499993827, -2.977408999572645598, 8.517802781871756324 ) ) ;
#40897=CYLINDRICAL_SURFACE ( 'NONE', #41034, 7.999999999999991118 ) ;
#40910=CARTESIAN_POINT ( 'NONE',  ( 8.008118988124991233, 9.807117285998411148E-16, 15.26311528394063011 ) ) ;
#40916=CARTESIAN_POINT ( 'NONE',  ( 7.188101187499992051, 2.977408999572647819, 8.330302781871752771 ) ) ;
#40933=CARTESIAN_POINT ( 'NONE',  ( -4.898587196589407898E-16, 7.999999999999991118, 3.642802783920144449 ) ) ;
#40939=CARTESIAN_POINT ( 'NONE',  ( 7.999999999999991118, 0.000000000000000000, 30.00000000000000000 ) ) ;
#40949=CARTESIAN_POINT ( 'NONE',  ( 7.188101187499991163, 2.977408999572648707, 16.20530278187175455 ) ) ;
#40966=CARTESIAN_POINT ( 'NONE',  ( -5.656854249492373476, -5.656854249492376141, 25.01780277982336642 ) ) ;
#40975=CARTESIAN_POINT ( 'NONE',  ( -4.898587196589407898E-16, 7.999999999999991118, 22.95530277982336642 ) ) ;
#40980=DIRECTION ( 'NONE',  ( -0.000000000000000000, -0.000000000000000000, 1.000000000000000000 ) ) ;
#40981=CARTESIAN_POINT ( 'NONE',  ( 7.999999999999991118, 9.797174393178815797E-16, 9.080302779823364645 ) ) ;
#40993=CARTESIAN_POINT ( 'NONE',  ( -5.656854249492373476, -5.656854249492376141, 7.205302783920144449 ) ) ;
#41007=DIRECTION ( 'NONE',  ( 1.000000000000000000, 0.000000000000000000, 0.000000000000000000 ) ) ;
#41034=AXIS2_PLACEMENT_3D ( 'NONE', #71029, #19347, #52589 ) ;
#41042=CARTESIAN_POINT ( 'NONE',  ( 2.977408999572646486, 7.188101187499991163, 4.017802781871751883 ) ) ;
#41065=CARTESIAN_POINT ( 'NONE',  ( 7.188101187499992051, 8.802885111219154394E-16, 10.11155278187175455 ) ) ;
#41068=CARTESIAN_POINT ( 'NONE',  ( -7.999999999999989342, -3.313708498984762496, 0.9803027843298238730 ) ) ;
#41070=CARTESIAN_POINT ( 'NONE',  ( -5.656854249492373476, -5.656854249492376141, 7.205302783920144449 ) ) ;
#41078=CARTESIAN_POINT ( 'NONE',  ( -7.999999999999991118, 0.000000000000000000, 23.51780278392014978 ) ) ;
#41111=CARTESIAN_POINT ( 'NONE',  ( 3.313708498984762496, -7.999999999999989342, 20.98655278392014978 ) ) ;
#41122=CARTESIAN_POINT ( 'NONE',  ( 5.082755093536318824, 5.082755093536319713, 26.42405278187175455 ) ) ;
#41142=CARTESIAN_POINT ( 'NONE',  ( 5.662595241051934458, 5.662595241051935346, 1.950615283940626998 ) ) ;
#41166=CARTESIAN_POINT ( 'NONE',  ( 7.999999999999991118, 3.313708498984757611, 15.17405277982336642 ) ) ;
#41180=CARTESIAN_POINT ( 'NONE',  ( 3.313708498984756279, 7.999999999999991118, 21.41780278432982598 ) ) ;
#41190=ORIENTED_EDGE ( 'NONE', *, *, #32937, .T. ) ;
#41212=CARTESIAN_POINT ( 'NONE',  ( -4.401442555609577197E-16, 7.188101187499992051, 14.61155278187175455 ) ) ;
#41237=CARTESIAN_POINT ( 'NONE',  ( 7.188101187499992051, 8.802885111219154394E-16, 11.61155278187175632 ) ) ;
#41242=FACE_OUTER_BOUND ( 'NONE', #36819, .T. ) ;
#41282=CARTESIAN_POINT ( 'NONE',  ( -8.008118988124989457, -3.317071493978883900, 16.10686528394062833 ) ) ;
#41288=CARTESIAN_POINT ( 'NONE',  ( 2.977408999572650927, -7.188101187499990274, 7.955302781871751883 ) ) ;
#41291=EDGE_CURVE ( 'NONE', #38597, #74609, #38303, .T. ) ;
#41303=CARTESIAN_POINT ( 'NONE',  ( 3.313708498984762496, -7.999999999999989342, -0.01344721607985516210 ) ) ;
#41304=ORIENTED_EDGE ( 'NONE', *, *, #8431, .F. ) ;
#41318=CARTESIAN_POINT ( 'NONE',  ( 2.977408999572650927, -7.188101187499990274, 17.33030278187175455 ) ) ;
#41330=CARTESIAN_POINT ( 'NONE',  ( 3.313708498984756279, 7.999999999999991118, 25.86155277982337353 ) ) ;
#41343=CARTESIAN_POINT ( 'NONE',  ( -7.999999999999989342, -3.313708498984762496, 17.42405277982336997 ) ) ;
#41361=CARTESIAN_POINT ( 'NONE',  ( 3.313708498984762496, -7.999999999999989342, 8.986552783920146226 ) ) ;
#41375=VERTEX_POINT ( 'NONE', #32726 ) ;
#41399=CARTESIAN_POINT ( 'NONE',  ( 7.999999999999991118, 9.797174393178815797E-16, 6.080302779823364645 ) ) ;
#41410=CARTESIAN_POINT ( 'NONE',  ( 7.188101187499991163, 2.977408999572648707, 5.330302781871753659 ) ) ;
#41435=CARTESIAN_POINT ( 'NONE',  ( -2.977408999572648707, -7.188101187499990274, 3.642802781871751883 ) ) ;
#41439=CARTESIAN_POINT ( 'NONE',  ( 1.469576158976822172E-15, -7.999999999999991118, 2.761552784329821986 ) ) ;
#41449=CARTESIAN_POINT ( 'NONE',  ( 5.656854249492374365, 5.656854249492375253, 22.95530278392014623 ) ) ;
#41469=CARTESIAN_POINT ( 'NONE',  ( 1.320432766682872962E-15, -7.188101187499992051, 25.86155278187175810 ) ) ;
#41476=CARTESIAN_POINT ( 'NONE',  ( 5.656854249492376141, -5.656854249492374365, 22.58030278392014623 ) ) ;
#41485=EDGE_CURVE ( 'NONE', #51815, #4709, #24885, .T. ) ;
#41489=CARTESIAN_POINT ( 'NONE',  ( -4.401442555609577197E-16, 7.188101187499992051, 25.11155278187175810 ) ) ;
#41504=CARTESIAN_POINT ( 'NONE',  ( 3.317071493978877683, 8.008118988124991233, 5.044365283940630107 ) ) ;
#41508=CARTESIAN_POINT ( 'NONE',  ( 3.313708498984762496, -7.999999999999989342, 7.299052779823365533 ) ) ;
#41511=CARTESIAN_POINT ( 'NONE',  ( 2.977408999572646486, 7.188101187499991163, 28.39280278187175810 ) ) ;
#41529=CARTESIAN_POINT ( 'NONE',  ( -7.999999999999991118, 3.313708498984756723, 14.23655277982336642 ) ) ;
#41543=CARTESIAN_POINT ( 'NONE',  ( 1.469576158976822172E-15, -7.999999999999991118, 16.26155278432982954 ) ) ;
#41555=( BOUNDED_CURVE ( )  B_SPLINE_CURVE ( 2, ( #48075, #58683, #30003, #41690, #38168, #66833, #31096, #13364, #2066 ),
 .UNSPECIFIED., .F., .F. ) 
 B_SPLINE_CURVE_WITH_KNOTS ( ( 3, 2, 2, 2, 3 ),
 ( 0.8157894736842106198, 0.8223684210526316374, 0.8289473684210527660, 0.8355263157894737835, 0.8421052631578948011 ),
 .UNSPECIFIED. ) 
 CURVE ( )  GEOMETRIC_REPRESENTATION_ITEM ( )  RATIONAL_B_SPLINE_CURVE ( ( 0.9999999999999986677, 0.9238795325112880708, 1.000000000000000000, 0.9238795325112867385, 1.000000000000000000, 0.9238795325112867385, 1.000000000000000000, 0.9238795325112854062, 1.000000000000001332 ) ) 
 REPRESENTATION_ITEM ( '' )  );
#41558=CARTESIAN_POINT ( 'NONE',  ( 7.999999999999991118, 9.797174393178815797E-16, 3.080302779823361981 ) ) ;
#41578=CARTESIAN_POINT ( 'NONE',  ( 5.082755093536320601, -5.082755093536318824, 14.04905278187175455 ) ) ;
#41602=CARTESIAN_POINT ( 'NONE',  ( 1.320432766682872962E-15, -7.188101187499992051, 11.23655278187175455 ) ) ;
#41627=ORIENTED_EDGE ( 'NONE', *, *, #61620, .F. ) ;
#41649=CARTESIAN_POINT ( 'NONE',  ( 5.662595241051934458, 5.662595241051935346, 16.95061528394063188 ) ) ;
#41654=CARTESIAN_POINT ( 'NONE',  ( -7.188101187499990274, -2.977408999572651815, 9.080302781871752771 ) ) ;
#41660=EDGE_CURVE ( 'NONE', #21067, #3963, #56630, .T. ) ;
#41669=CARTESIAN_POINT ( 'NONE',  ( 3.313708498984756279, 7.999999999999991118, 0.5490527839201453375 ) ) ;
#41684=CARTESIAN_POINT ( 'NONE',  ( 5.082755093536320601, -5.082755093536318824, 14.42405278187175455 ) ) ;
#41690=CARTESIAN_POINT ( 'NONE',  ( 3.313708498984762496, -7.999999999999989342, 5.799052779823364645 ) ) ;
#41691=CARTESIAN_POINT ( 'NONE',  ( 2.977408999572650927, -7.188101187499990274, 27.83030278187176165 ) ) ;
#41709=CARTESIAN_POINT ( 'NONE',  ( -4.898587196589407898E-16, 7.999999999999991118, 15.45530277982336642 ) ) ;
#41711=CARTESIAN_POINT ( 'NONE',  ( 7.999963770166947263, -3.313744728817803242, 18.17405133435311271 ) ) ;
#41712=ORIENTED_EDGE ( 'NONE', *, *, #37242, .F. ) ;
#41728=CARTESIAN_POINT ( 'NONE',  ( 3.313708498984756279, 7.999999999999991118, 6.549052783920143561 ) ) ;
#41740=CARTESIAN_POINT ( 'NONE',  ( 1.469576158976822172E-15, -7.999999999999991118, 26.70530277982336642 ) ) ;
#41764=CARTESIAN_POINT ( 'NONE',  ( -5.656854249492375253, 5.656854249492375253, 6.642802779823365533 ) ) ;
#41773=CARTESIAN_POINT ( 'NONE',  ( 7.188101187499991163, 2.977408999572648707, 3.830302781871751883 ) ) ;
#41798=CARTESIAN_POINT ( 'NONE',  ( -7.188101187499992051, 0.000000000000000000, 4.861552781871752771 ) ) ;
#41803=DIRECTION ( 'NONE',  ( 0.000000000000000000, -1.000000000000000000, 0.000000000000000000 ) ) ;
#41811=CARTESIAN_POINT ( 'NONE',  ( 7.999999999999991118, 9.797174393178815797E-16, 27.26780278392014978 ) ) ;
#41831=CARTESIAN_POINT ( 'NONE',  ( -5.082755093536317936, -5.082755093536320601, 18.17405278187175455 ) ) ;
#41842=CARTESIAN_POINT ( 'NONE',  ( 3.313708498984756279, 7.999999999999991118, 18.54905278392014623 ) ) ;
#41845=DIRECTION ( 'NONE',  ( -0.000000000000000000, -0.000000000000000000, 1.000000000000000000 ) ) ;
#41853=CARTESIAN_POINT ( 'NONE',  ( -7.188101187499990274, -2.977408999572651371, 24.08030278187175455 ) ) ;
#41868=CARTESIAN_POINT ( 'NONE',  ( -8.008118988124991233, 3.317071493978878127, 0.9193652839406296629 ) ) ;
#41875=CARTESIAN_POINT ( 'NONE',  ( 5.082755093536318824, 5.082755093536319713, 19.29905278187175455 ) ) ;
#41893=CARTESIAN_POINT ( 'NONE',  ( 5.656854249492374365, 5.656854249492375253, 15.26780277982336642 ) ) ;
#41908=CARTESIAN_POINT ( 'NONE',  ( -5.656854249492375253, 5.656854249492375253, 17.19905278432982243 ) ) ;
#41912=ORIENTED_EDGE ( 'NONE', *, *, #72199, .T. ) ;
#41929=CARTESIAN_POINT ( 'NONE',  ( -5.656854249492375253, 5.656854249492375253, 12.83030278392014623 ) ) ;
#41930=ORIENTED_EDGE ( 'NONE', *, *, #16309, .T. ) ;
#41939=CARTESIAN_POINT ( 'NONE',  ( -5.082755093536319713, 5.082755093536319713, 14.79905278187175455 ) ) ;
#41941=ORIENTED_EDGE ( 'NONE', *, *, #26417, .F. ) ;
#41960=CARTESIAN_POINT ( 'NONE',  ( 2.977408999572646486, 7.188101187499992051, 8.892802781871754547 ) ) ;
#41965=CARTESIAN_POINT ( 'NONE',  ( 5.656854249492374365, 5.656854249492375253, 3.455302783920144449 ) ) ;
#41982=CARTESIAN_POINT ( 'NONE',  ( 1.469576158976822172E-15, -7.999999999999991118, 23.70530277982336642 ) ) ;
#42004=CARTESIAN_POINT ( 'NONE',  ( 7.999999999999992895, -3.313708498984756279, 13.48655277982336465 ) ) ;
#42006=CARTESIAN_POINT ( 'NONE',  ( -3.317071493978878571, 8.008118988124991233, 6.731865283940627442 ) ) ;
#42012=CARTESIAN_POINT ( 'NONE',  ( -5.082755093536319713, 5.082755093536319713, 7.299052781871751883 ) ) ;
#42026=CARTESIAN_POINT ( 'NONE',  ( 7.999999999999991118, 9.797174393178815797E-16, 4.767802783920145338 ) ) ;
#42041=CARTESIAN_POINT ( 'NONE',  ( 5.082755093536318824, 5.082755093536319713, 11.79905278187175632 ) ) ;
#42048=CARTESIAN_POINT ( 'NONE',  ( -2.977408999572647819, -7.188101187499990274, 27.64280278187175455 ) ) ;
#42065=CARTESIAN_POINT ( 'NONE',  ( -3.313708498984758943, -7.999999999999989342, 16.11155277982336642 ) ) ;
#42129=CARTESIAN_POINT ( 'NONE',  ( -7.188101187499992051, 0.000000000000000000, 28.86155278187175810 ) ) ;
#42152=CARTESIAN_POINT ( 'NONE',  ( 1.320432766682872962E-15, -7.188101187499992051, 2.236552781871754103 ) ) ;
#42167=CARTESIAN_POINT ( 'NONE',  ( -7.999999999999991118, 3.313708498984756723, 27.92405278392015333 ) ) ;
#42182=CARTESIAN_POINT ( 'NONE',  ( 7.999999999999304556, -3.314968910423997278E-06, 15.26780269013280034 ) ) ;
#42184=CARTESIAN_POINT ( 'NONE',  ( 7.999999999999991118, 9.797174393178815797E-16, 12.26780278392014623 ) ) ;
#42189=CARTESIAN_POINT ( 'NONE',  ( 1.320432766682872962E-15, -7.188101187499992051, 22.86155278187175455 ) ) ;
#42199=CARTESIAN_POINT ( 'NONE',  ( 7.999999999999992895, -3.313708498984756279, 16.67405278392014623 ) ) ;
#42213=CARTESIAN_POINT ( 'NONE',  ( -2.977408999572647819, 7.188101187499991163, 19.20530278187175810 ) ) ;
#42225=CARTESIAN_POINT ( 'NONE',  ( -5.082755093536319713, 5.082755093536319713, 1.674052781871753659 ) ) ;
#42226=CYLINDRICAL_SURFACE ( 'NONE', #7308, 7.999999999999991118 ) ;
#42231=CARTESIAN_POINT ( 'NONE',  ( -3.317071493978880348, -8.008118988124989457, -0.2056347160593713919 ) ) ;
#42232=LINE ( 'NONE', #36222, #4627 ) ;
#42238=CARTESIAN_POINT ( 'NONE',  ( -2.977408999572648707, -7.188101187499990274, 21.64280278187176165 ) ) ;
#42257=CARTESIAN_POINT ( 'NONE',  ( 3.313708498984756279, 7.999999999999991118, 15.36155277982336642 ) ) ;
#42274=CARTESIAN_POINT ( 'NONE',  ( 7.999999999999991118, 3.313708498984757611, 18.23030278432982598 ) ) ;
#42302=CARTESIAN_POINT ( 'NONE',  ( 2.977408999572646486, 7.188101187499991163, 14.51780278187175455 ) ) ;
#42304=( BOUNDED_SURFACE ( )  B_SPLINE_SURFACE ( 1, 2, ( 
 ( #16600, #68673, #34370, #57371, #23024, #46032, #9853, #50204, #10222, #29799, #7162, #6791, #52812, #46405, #24125, #1870, #24500, #40380, #30167, #18108, #1145, #58120, #41122, #70530, #47138, #52443, #12437, #58850, #46768, #52076, #18845, #12071, #53184, #30538, #18478, #35108, #41489, #35835, #6428, #1522, #47505, #411, #64504, #29432, #64130, #6052, #58483, #41853, #23764, #64864, #11701, #12803, #34743, #17728, #17356, #69420, #23391, #7531, #13166, #35469, #59220, #40744, #24856, #69792, #63754, #36203, #63378, #69052, #57747, #53554, #70170, #29058, #780, #66725, #13899, #32407, #36938, #30901, #48985, #42951, #20694, #60309, #66346, #48614, #53920, #25964, #14650, #71251, #71620, #47874, #19571, #55046, #70894, #71996, #2611, #37691, #65970, #31652, #65225, #42213, #60692, #3353, #36569, #14275, #32026, #59942, #25228, #19209, #54671, #13530, #59582, #2979, #7896, #20311, #8637, #26343, #49363, #38066, #8258, #31271, #2232, #9012, #54299, #48245, #72381, #43711, #42585, #43328, #65601, #61064, #37313, #25599, #15030, #9387, #55420, #3729, #19943, #56538, #38438, #4480, #55794, #16896, #73498, #56913, #51235, #67845, #21069, #15776, #27103, #22181, #39920, #21441, #33537, #72764, #4111, #38813, #49748, #57286, #44094, #62548, #33913, #50119, #27470, #67103, #62928, #45205, #73876, #61441, #28226, #4856, #9767, #68217, #68589, #16136, #61813, #56166, #27852, #44838, #16514, #39553, #50861, #11252, #50484, #10131, #10878, #73134, #5225, #74246, #45575, #62179, #26728, #15399, #32787, #33169, #44464, #67477, #22553, #21805, #39175, #10505, #34282, #64783, #69336, #69712, #17645, #57662, #1438, #12360, #13085, #70450, #6711, #64422, #63668, #28598, #17274, #58406, #11993, #5600, #34658, #18396, #36120, #40665, #18026, #35027, #5969, #24419, #35394, #51608, #18766, #29719, #12720, #11621, #52733, #47054, #28971, #29355, #74625, #51991, #35753, #22939, #1067, #58039, #70090, #699, #64050, #45949, #68965, #41410, #58771, #40292, #23682, #7078, #6352, #329, #63293, #24045, #23308, #46322, #30085, #52362, #53104, #41042, #47425, #41773, #46688, #48161, #25144, #30457, #71912, #71168, #19123, #25879, #20225, #53473, #54588, #36488, #49275, #25515, #59501, #43244, #48527, #66631, #31936, #1790, #14190, #70812, #36857, #13450, #72290, #31188, #14565, #8924, #71534, #24775, #19487, #7814, #2892, #20602, #53840, #65883, #47789, #30817, #42503, #7450, #14938 ),
 ( #42129, #60601, #37227, #65141, #31564, #26256, #19859, #65519, #13813, #60224, #2523, #48898, #66260, #8550, #43620, #59865, #8178, #37602, #2151, #54959, #3268, #59141, #42865, #54214, #32321, #20978, #60976, #68495, #9297, #73782, #45116, #67010, #15687, #55333, #74153, #33446, #10415, #49659, #39457, #16056, #72676, #56445, #5138, #27381, #50028, #67385, #39089, #56078, #4764, #27756, #44747, #22457, #38729, #27016, #50767, #15309, #68128, #16423, #56817, #73415, #37977, #3638, #44003, #21351, #26636, #38346, #62093, #44375, #61353, #9680, #22091, #45477, #73044, #50400, #61726, #32700, #33820, #67762, #55709, #28131, #62456, #10784, #4023, #51144, #10045, #33081, #4388, #21719, #63202, #23958, #16796, #17933, #46228, #58315, #11903, #606, #34186, #11164, #29626, #46965, #5505, #34936, #975, #28876, #68868, #39824, #23586, #62827, #57189, #46596, #28505, #69619, #52271, #69995, #18302, #6985, #5880, #57570, #51514, #52639, #51896, #74529, #6621, #41318, #22839, #12268, #17179, #29995, #57949, #40199, #64326, #6254, #24324, #12631, #45852, #40949, #11531, #69245, #34564, #53010, #63576, #35662, #58676, #29259, #236, #23218, #17555, #35301, #1342, #40572, #63958, #47335, #24684, #8741, #41684, #9497, #31753, #30362, #38165, #32511, #64695, #66830, #47695, #61543, #37794, #70716, #55525, #60790, #4210, #44194, #12993, #26444, #7355, #49088, #19036, #9865, #43432, #26832, #21169, #9115, #36031, #60416, #42041, #15132, #32894, #66072, #3454, #59049, #14380, #54773, #18674, #27199, #53382, #3836, #49846, #37416, #72102, #1707, #55896, #61166, #43816, #3083, #72864, #49470, #26068, #67206, #38541, #32131, #20415, #66447, #72489, #14755, #15504, #70362, #20798, #55149, #27956, #39279, #40022, #27576, #5694, #28693, #69065, #10981, #50216, #44566, #33263, #33635, #73236, #61910, #28325, #56641, #21542, #4579, #63025, #34756, #62280, #39650, #10608, #50584, #46045, #57010, #57760, #40393, #51335, #34384, #56262, #74343, #16996, #73602, #73975, #67579, #21909, #57384, #15875, #22652, #4956, #11349, #45302, #34015, #38908, #10235, #51706, #53, #44940, #68317, #23036, #50962, #67947, #16241, #5323, #22280, #16615, #45672, #62647, #68686, #17369, #63391, #11715, #6065, #18121, #69805, #59232, #46419, #53197, #69433, #52456, #52092, #6444, #58136, #42225, #24867, #52825, #19220, #29445, #36581, #6801, #35121, #70542, #425, #59593, #29073, #18857, #29814, #35848 ) ),
 .UNSPECIFIED., .F., .F., .F. ) 
 B_SPLINE_SURFACE_WITH_KNOTS ( ( 2, 2 ),
 ( 3, 2, 2, 2, 2, 2, 2, 2, 2, 2, 2, 2, 2, 2, 2, 2, 2, 2, 2, 2, 2, 2, 2, 2, 2, 2, 2, 2, 2, 2, 2, 2, 2, 2, 2, 2, 2, 2, 2, 2, 2, 2, 2, 2, 2, 2, 2, 2, 2, 2, 2, 2, 2, 2, 2, 2, 2, 2, 2, 2, 2, 2, 2, 2, 2, 2, 2, 2, 2, 2, 2, 2, 2, 2, 2, 2, 2, 2, 2, 2, 2, 2, 2, 2, 2, 2, 2, 2, 2, 2, 2, 2, 2, 2, 2, 2, 2, 2, 2, 2, 2, 2, 2, 2, 2, 2, 2, 2, 2, 2, 2, 2, 2, 2, 2, 2, 2, 2, 2, 2, 2, 2, 2, 2, 2, 2, 2, 2, 2, 2, 2, 2, 2, 2, 2, 2, 2, 2, 2, 2, 2, 2, 2, 2, 2, 2, 2, 2, 2, 2, 2, 2, 3 ),
 ( 0.000000000000000000, 1.000000000000000000 ),
 ( 0.000000000000000000, 0.006578947368421052266, 0.01315789473684210453, 0.01973684210526315680, 0.02631578947368420907, 0.03289473684210526133, 0.03947368421052631360, 0.04605263157894736586, 0.05263157894736841813, 0.05921052631578947040, 0.06578947368421052266, 0.07236842105263158187, 0.07894736842105262720, 0.08552631578947368640, 0.09210526315789473173, 0.09868421052631579093, 0.1052631578947368363, 0.1118421052631578955, 0.1184210526315789408, 0.1250000000000000000, 0.1315789473684210453, 0.1381578947368421184, 0.1447368421052631637, 0.1513157894736842091, 0.1578947368421052544, 0.1644736842105263275, 0.1710526315789473728, 0.1776315789473684181, 0.1842105263157894635, 0.1907894736842105365, 0.1973684210526315819, 0.2039473684210526272, 0.2105263157894736725, 0.2171052631578947456, 0.2236842105263157909, 0.2302631578947368363, 0.2368421052631578816, 0.2434210526315789547, 0.2500000000000000000, 0.2565789473684210731, 0.2631578947368420907, 0.2697368421052631637, 0.2763157894736842368, 0.2828947368421052544, 0.2894736842105263275, 0.2960526315789473450, 0.3026315789473684181, 0.3092105263157894912, 0.3157894736842105088, 0.3223684210526315819, 0.3289473684210526550, 0.3355263157894736725, 0.3421052631578947456, 0.3486842105263157632, 0.3552631578947368363, 0.3618421052631579093, 0.3684210526315789269, 0.3750000000000000000, 0.3815789473684210731, 0.3881578947368420907, 0.3947368421052631637, 0.4013157894736842368, 0.4078947368421052544, 0.4144736842105263275, 0.4210526315789473450, 0.4276315789473684181, 0.4342105263157894912, 0.4407894736842105088, 0.4473684210526315819, 0.4539473684210526550, 0.4605263157894736725, 0.4671052631578947456, 0.4736842105263157632, 0.4802631578947368363, 0.4868421052631579093, 0.4934210526315789269, 0.5000000000000000000, 0.5065789473684210176, 0.5131578947368421462, 0.5197368421052631637, 0.5263157894736841813, 0.5328947368421053099, 0.5394736842105263275, 0.5460526315789473450, 0.5526315789473684736, 0.5592105263157894912, 0.5657894736842105088, 0.5723684210526315264, 0.5789473684210526550, 0.5855263157894736725, 0.5921052631578946901, 0.5986842105263158187, 0.6052631578947368363, 0.6118421052631578538, 0.6184210526315789824, 0.6250000000000000000, 0.6315789473684210176, 0.6381578947368421462, 0.6447368421052631637, 0.6513157894736841813, 0.6578947368421053099, 0.6644736842105263275, 0.6710526315789473450, 0.6776315789473684736, 0.6842105263157894912, 0.6907894736842105088, 0.6973684210526315264, 0.7039473684210526550, 0.7105263157894736725, 0.7171052631578946901, 0.7236842105263158187, 0.7302631578947368363, 0.7368421052631578538, 0.7434210526315789824, 0.7500000000000000000, 0.7565789473684210176, 0.7631578947368421462, 0.7697368421052631637, 0.7763157894736841813, 0.7828947368421053099, 0.7894736842105263275, 0.7960526315789473450, 0.8026315789473684736, 0.8092105263157894912, 0.8157894736842105088, 0.8223684210526315264, 0.8289473684210526550, 0.8355263157894736725, 0.8421052631578946901, 0.8486842105263158187, 0.8552631578947368363, 0.8618421052631578538, 0.8684210526315789824, 0.8750000000000000000, 0.8815789473684210176, 0.8881578947368421462, 0.8947368421052631637, 0.9013157894736841813, 0.9078947368421053099, 0.9144736842105263275, 0.9210526315789473450, 0.9276315789473684736, 0.9342105263157894912, 0.9407894736842105088, 0.9473684210526315264, 0.9539473684210526550, 0.9605263157894736725, 0.9671052631578946901, 0.9736842105263158187, 0.9802631578947368363, 0.9868421052631578538, 0.9934210526315789824, 0.9940576599040155115 ),
 .UNSPECIFIED. ) 
 GEOMETRIC_REPRESENTATION_ITEM ( )  RATIONAL_B_SPLINE_SURFACE ( (
 ( 1.000000000000000000, 0.9238795325112867385, 1.000000000000000000, 0.9238795325112867385, 1.000000000000000000, 0.9238795325112867385, 1.000000000000000000, 0.9238795325112867385, 1.000000000000000000, 0.9238795325112867385, 1.000000000000000000, 0.9238795325112867385, 1.000000000000000000, 0.9238795325112867385, 1.000000000000000000, 0.9238795325112867385, 1.000000000000000000, 0.9238795325112867385, 1.000000000000000000, 0.9238795325112867385, 1.000000000000000000, 0.9238795325112867385, 1.000000000000000000, 0.9238795325112867385, 1.000000000000000000, 0.9238795325112867385, 1.000000000000000000, 0.9238795325112867385, 1.000000000000000000, 0.9238795325112867385, 1.000000000000000000, 0.9238795325112867385, 1.000000000000000000, 0.9238795325112867385, 1.000000000000000000, 0.9238795325112867385, 1.000000000000000000, 0.9238795325112867385, 1.000000000000000000, 0.9238795325112867385, 1.000000000000000000, 0.9238795325112867385, 1.000000000000000000, 0.9238795325112867385, 1.000000000000000000, 0.9238795325112867385, 1.000000000000000000, 0.9238795325112867385, 1.000000000000000000, 0.9238795325112867385, 1.000000000000000000, 0.9238795325112867385, 1.000000000000000000, 0.9238795325112867385, 1.000000000000000000, 0.9238795325112867385, 1.000000000000000000, 0.9238795325112867385, 1.000000000000000000, 0.9238795325112867385, 1.000000000000000000, 0.9238795325112867385, 1.000000000000000000, 0.9238795325112867385, 1.000000000000000000, 0.9238795325112867385, 1.000000000000000000, 0.9238795325112867385, 1.000000000000000000, 0.9238795325112867385, 1.000000000000000000, 0.9238795325112867385, 1.000000000000000000, 0.9238795325112867385, 1.000000000000000000, 0.9238795325112867385, 1.000000000000000000, 0.9238795325112867385, 1.000000000000000000, 0.9238795325112867385, 1.000000000000000000, 0.9238795325112867385, 1.000000000000000000, 0.9238795325112867385, 1.000000000000000000, 0.9238795325112867385, 1.000000000000000000, 0.9238795325112867385, 1.000000000000000000, 0.9238795325112867385, 1.000000000000000000, 0.9238795325112867385, 1.000000000000000000, 0.9238795325112867385, 1.000000000000000000, 0.9238795325112867385, 1.000000000000000000, 0.9238795325112867385, 1.000000000000000000, 0.9238795325112867385, 1.000000000000000000, 0.9238795325112867385, 1.000000000000000000, 0.9238795325112867385, 1.000000000000000000, 0.9238795325112867385, 1.000000000000000000, 0.9238795325112867385, 1.000000000000000000, 0.9238795325112867385, 1.000000000000000000, 0.9238795325112867385, 1.000000000000000000, 0.9238795325112867385, 1.000000000000000000, 0.9238795325112867385, 1.000000000000000000, 0.9238795325112867385, 1.000000000000000000, 0.9238795325112867385, 1.000000000000000000, 0.9238795325112867385, 1.000000000000000000, 0.9238795325112867385, 1.000000000000000000, 0.9238795325112867385, 1.000000000000000000, 0.9238795325112867385, 1.000000000000000000, 0.9238795325112867385, 1.000000000000000000, 0.9238795325112867385, 1.000000000000000000, 0.9238795325112867385, 1.000000000000000000, 0.9238795325112867385, 1.000000000000000000, 0.9238795325112867385, 1.000000000000000000, 0.9238795325112867385, 1.000000000000000000, 0.9238795325112867385, 1.000000000000000000, 0.9238795325112867385, 1.000000000000000000, 0.9238795325112867385, 1.000000000000000000, 0.9238795325112867385, 1.000000000000000000, 0.9238795325112867385, 1.000000000000000000, 0.9238795325112867385, 1.000000000000000000, 0.9238795325112867385, 1.000000000000000000, 0.9238795325112867385, 1.000000000000000000, 0.9238795325112867385, 1.000000000000000000, 0.9238795325112867385, 1.000000000000000000, 0.9238795325112867385, 1.000000000000000000, 0.9238795325112867385, 1.000000000000000000, 0.9238795325112867385, 1.000000000000000000, 0.9238795325112867385, 1.000000000000000000, 0.9238795325112867385, 1.000000000000000000, 0.9238795325112867385, 1.000000000000000000, 0.9238795325112867385, 1.000000000000000000, 0.9238795325112867385, 1.000000000000000000, 0.9238795325112867385, 1.000000000000000000, 0.9238795325112867385, 1.000000000000000000, 0.9238795325112867385, 1.000000000000000000, 0.9238795325112867385, 1.000000000000000000, 0.9238795325112867385, 1.000000000000000000, 0.9238795325112867385, 1.000000000000000000, 0.9238795325112867385, 1.000000000000000000, 0.9238795325112867385, 1.000000000000000000, 0.9238795325112867385, 1.000000000000000000, 0.9238795325112867385, 1.000000000000000000, 0.9238795325112867385, 1.000000000000000000, 0.9238795325112867385, 1.000000000000000000, 0.9238795325112867385, 1.000000000000000000, 0.9238795325112867385, 1.000000000000000000, 0.9238795325112867385, 1.000000000000000000, 0.9238795325112867385, 1.000000000000000000, 0.9238795325112867385, 1.000000000000000000, 0.9238795325112867385, 1.000000000000000000, 0.9238795325112867385, 1.000000000000000000, 0.9238795325112867385, 1.000000000000000000, 0.9238795325112867385, 1.000000000000000000, 0.9238795325112867385, 1.000000000000000000, 0.9238795325112867385, 1.000000000000000000, 0.9238795325112867385, 1.000000000000000000, 0.9238795325112867385, 1.000000000000000000, 0.9238795325112867385, 1.000000000000000000, 0.9238795325112867385, 1.000000000000000000, 0.9238795325112867385, 1.000000000000000000, 0.9238795325112867385, 1.000000000000000000, 0.9238795325112867385, 1.000000000000000000, 0.9238795325112867385, 1.000000000000000000, 0.9238795325112867385, 1.000000000000000000, 0.9238795325112867385, 1.000000000000000000, 0.9238795325112867385, 1.000000000000000000, 0.9238795325112867385, 1.000000000000000000, 0.9238795325112867385, 1.000000000000000000, 0.9238795325112867385, 1.000000000000000000, 0.9238795325112867385, 1.000000000000000000, 0.9238795325112867385, 1.000000000000000000, 0.9238795325112867385, 1.000000000000000000, 0.9238795325112867385, 1.000000000000000000, 0.9238795325112867385, 1.000000000000000000, 0.9238795325112867385, 1.000000000000000000, 0.9238795325112867385, 1.000000000000000000, 0.9238795325112867385, 1.000000000000000000, 0.9238795325112867385, 1.000000000000000000, 0.9238795325112867385, 1.000000000000000000, 0.9238795325112867385, 1.000000000000000000, 0.9238795325112867385, 1.000000000000000000, 0.9238795325112867385, 1.000000000000000000, 0.9238795325112867385, 1.000000000000000000, 0.9238795325112867385, 1.000000000000000000, 0.9238795325112867385, 1.000000000000000000, 0.9238795325112867385, 1.000000000000000000, 0.9238795325112867385, 1.000000000000000000, 0.9238795325112867385, 1.000000000000000000, 0.9238795325112867385, 1.000000000000000000, 0.9238795325112867385, 1.000000000000000000, 0.9238795325112867385, 1.000000000000000000, 0.9238795325112867385, 1.000000000000000000, 0.9238795325112867385, 1.000000000000000000, 0.9238795325112867385, 1.000000000000000000, 0.9238795325112867385, 1.000000000000000000, 0.9926342558359432244, 0.9866939939076171395),
 ( 1.000000000000000000, 0.9238795325112867385, 1.000000000000000000, 0.9238795325112867385, 1.000000000000000000, 0.9238795325112867385, 1.000000000000000000, 0.9238795325112867385, 1.000000000000000000, 0.9238795325112867385, 1.000000000000000000, 0.9238795325112867385, 1.000000000000000000, 0.9238795325112867385, 1.000000000000000000, 0.9238795325112867385, 1.000000000000000000, 0.9238795325112867385, 1.000000000000000000, 0.9238795325112867385, 1.000000000000000000, 0.9238795325112867385, 1.000000000000000000, 0.9238795325112867385, 1.000000000000000000, 0.9238795325112867385, 1.000000000000000000, 0.9238795325112867385, 1.000000000000000000, 0.9238795325112867385, 1.000000000000000000, 0.9238795325112867385, 1.000000000000000000, 0.9238795325112867385, 1.000000000000000000, 0.9238795325112867385, 1.000000000000000000, 0.9238795325112867385, 1.000000000000000000, 0.9238795325112867385, 1.000000000000000000, 0.9238795325112867385, 1.000000000000000000, 0.9238795325112867385, 1.000000000000000000, 0.9238795325112867385, 1.000000000000000000, 0.9238795325112867385, 1.000000000000000000, 0.9238795325112867385, 1.000000000000000000, 0.9238795325112867385, 1.000000000000000000, 0.9238795325112867385, 1.000000000000000000, 0.9238795325112867385, 1.000000000000000000, 0.9238795325112867385, 1.000000000000000000, 0.9238795325112867385, 1.000000000000000000, 0.9238795325112867385, 1.000000000000000000, 0.9238795325112867385, 1.000000000000000000, 0.9238795325112867385, 1.000000000000000000, 0.9238795325112867385, 1.000000000000000000, 0.9238795325112867385, 1.000000000000000000, 0.9238795325112867385, 1.000000000000000000, 0.9238795325112867385, 1.000000000000000000, 0.9238795325112867385, 1.000000000000000000, 0.9238795325112867385, 1.000000000000000000, 0.9238795325112867385, 1.000000000000000000, 0.9238795325112867385, 1.000000000000000000, 0.9238795325112867385, 1.000000000000000000, 0.9238795325112867385, 1.000000000000000000, 0.9238795325112867385, 1.000000000000000000, 0.9238795325112867385, 1.000000000000000000, 0.9238795325112867385, 1.000000000000000000, 0.9238795325112867385, 1.000000000000000000, 0.9238795325112867385, 1.000000000000000000, 0.9238795325112867385, 1.000000000000000000, 0.9238795325112867385, 1.000000000000000000, 0.9238795325112867385, 1.000000000000000000, 0.9238795325112867385, 1.000000000000000000, 0.9238795325112867385, 1.000000000000000000, 0.9238795325112867385, 1.000000000000000000, 0.9238795325112867385, 1.000000000000000000, 0.9238795325112867385, 1.000000000000000000, 0.9238795325112867385, 1.000000000000000000, 0.9238795325112867385, 1.000000000000000000, 0.9238795325112867385, 1.000000000000000000, 0.9238795325112867385, 1.000000000000000000, 0.9238795325112867385, 1.000000000000000000, 0.9238795325112867385, 1.000000000000000000, 0.9238795325112867385, 1.000000000000000000, 0.9238795325112867385, 1.000000000000000000, 0.9238795325112867385, 1.000000000000000000, 0.9238795325112867385, 1.000000000000000000, 0.9238795325112867385, 1.000000000000000000, 0.9238795325112867385, 1.000000000000000000, 0.9238795325112867385, 1.000000000000000000, 0.9238795325112867385, 1.000000000000000000, 0.9238795325112867385, 1.000000000000000000, 0.9238795325112867385, 1.000000000000000000, 0.9238795325112867385, 1.000000000000000000, 0.9238795325112867385, 1.000000000000000000, 0.9238795325112867385, 1.000000000000000000, 0.9238795325112867385, 1.000000000000000000, 0.9238795325112867385, 1.000000000000000000, 0.9238795325112867385, 1.000000000000000000, 0.9238795325112867385, 1.000000000000000000, 0.9238795325112867385, 1.000000000000000000, 0.9238795325112867385, 1.000000000000000000, 0.9238795325112867385, 1.000000000000000000, 0.9238795325112867385, 1.000000000000000000, 0.9238795325112867385, 1.000000000000000000, 0.9238795325112867385, 1.000000000000000000, 0.9238795325112867385, 1.000000000000000000, 0.9238795325112867385, 1.000000000000000000, 0.9238795325112867385, 1.000000000000000000, 0.9238795325112867385, 1.000000000000000000, 0.9238795325112867385, 1.000000000000000000, 0.9238795325112867385, 1.000000000000000000, 0.9238795325112867385, 1.000000000000000000, 0.9238795325112867385, 1.000000000000000000, 0.9238795325112867385, 1.000000000000000000, 0.9238795325112867385, 1.000000000000000000, 0.9238795325112867385, 1.000000000000000000, 0.9238795325112867385, 1.000000000000000000, 0.9238795325112867385, 1.000000000000000000, 0.9238795325112867385, 1.000000000000000000, 0.9238795325112867385, 1.000000000000000000, 0.9238795325112867385, 1.000000000000000000, 0.9238795325112867385, 1.000000000000000000, 0.9238795325112867385, 1.000000000000000000, 0.9238795325112867385, 1.000000000000000000, 0.9238795325112867385, 1.000000000000000000, 0.9238795325112867385, 1.000000000000000000, 0.9238795325112867385, 1.000000000000000000, 0.9238795325112867385, 1.000000000000000000, 0.9238795325112867385, 1.000000000000000000, 0.9238795325112867385, 1.000000000000000000, 0.9238795325112867385, 1.000000000000000000, 0.9238795325112867385, 1.000000000000000000, 0.9238795325112867385, 1.000000000000000000, 0.9238795325112867385, 1.000000000000000000, 0.9238795325112867385, 1.000000000000000000, 0.9238795325112867385, 1.000000000000000000, 0.9238795325112867385, 1.000000000000000000, 0.9238795325112867385, 1.000000000000000000, 0.9238795325112867385, 1.000000000000000000, 0.9238795325112867385, 1.000000000000000000, 0.9238795325112867385, 1.000000000000000000, 0.9238795325112867385, 1.000000000000000000, 0.9238795325112867385, 1.000000000000000000, 0.9238795325112867385, 1.000000000000000000, 0.9238795325112867385, 1.000000000000000000, 0.9238795325112867385, 1.000000000000000000, 0.9238795325112867385, 1.000000000000000000, 0.9238795325112867385, 1.000000000000000000, 0.9238795325112867385, 1.000000000000000000, 0.9238795325112867385, 1.000000000000000000, 0.9238795325112867385, 1.000000000000000000, 0.9238795325112867385, 1.000000000000000000, 0.9238795325112867385, 1.000000000000000000, 0.9238795325112867385, 1.000000000000000000, 0.9238795325112867385, 1.000000000000000000, 0.9238795325112867385, 1.000000000000000000, 0.9238795325112867385, 1.000000000000000000, 0.9238795325112867385, 1.000000000000000000, 0.9238795325112867385, 1.000000000000000000, 0.9238795325112867385, 1.000000000000000000, 0.9238795325112867385, 1.000000000000000000, 0.9238795325112867385, 1.000000000000000000, 0.9238795325112867385, 1.000000000000000000, 0.9238795325112867385, 1.000000000000000000, 0.9238795325112867385, 1.000000000000000000, 0.9238795325112867385, 1.000000000000000000, 0.9238795325112867385, 1.000000000000000000, 0.9238795325112867385, 1.000000000000000000, 0.9238795325112867385, 1.000000000000000000, 0.9238795325112867385, 1.000000000000000000, 0.9238795325112867385, 1.000000000000000000, 0.9926342558359432244, 0.9866939939076171395) ) ) 
 REPRESENTATION_ITEM ( '' )  SURFACE ( )  );
#42327=CARTESIAN_POINT ( 'NONE',  ( -2.977408999572647819, -7.188101187499990274, 8.142802781871752771 ) ) ;
#42333=CARTESIAN_POINT ( 'NONE',  ( 7.999999999999989342, -2.556712563705454310E-05, 3.267802060586142865 ) ) ;
#42354=EDGE_CURVE ( 'NONE', #14756, #37555, #60422, .T. ) ;
#42358=CARTESIAN_POINT ( 'NONE',  ( -7.999999999999991118, 3.313708498984757167, 9.736552779823366421 ) ) ;
#42375=CARTESIAN_POINT ( 'NONE',  ( -3.317071493978878571, 8.008118988124991233, 8.231865283940630107 ) ) ;
#42380=CARTESIAN_POINT ( 'NONE',  ( -2.977408999572647819, -7.188101187499990274, 6.267802781871754547 ) ) ;
#42393=CARTESIAN_POINT ( 'NONE',  ( -3.313708498984757167, 7.999999999999991118, 2.236552783920143561 ) ) ;
#42397=CARTESIAN_POINT ( 'NONE',  ( 7.999999999999992895, -9.797174393178815797E-16, 0.000000000000000000 ) ) ;
#42413=DIRECTION ( 'NONE',  ( -0.000000000000000000, -0.000000000000000000, 1.000000000000000000 ) ) ;
#42415=CARTESIAN_POINT ( 'NONE',  ( 2.977408999572646486, 7.188101187499992051, 28.39280278187175810 ) ) ;
#42420=CARTESIAN_POINT ( 'NONE',  ( -8.000000000000001776, 3.313708498984746509, 26.23655277982336997 ) ) ;
#42436=CARTESIAN_POINT ( 'NONE',  ( -3.313708498984757167, 7.999999999999991118, 15.54905277982336465 ) ) ;
#42445=CARTESIAN_POINT ( 'NONE',  ( -7.999999999999991118, 0.000000000000000000, 5.517802783920146226 ) ) ;
#42447=CARTESIAN_POINT ( 'NONE',  ( -7.999999999999991118, 9.797174393178815797E-16, 30.00000000000000000 ) ) ;
#42469=CARTESIAN_POINT ( 'NONE',  ( -7.999999999994639843, -6.164467849698474977E-06, 23.51803407853789807 ) ) ;
#42488=CARTESIAN_POINT ( 'NONE',  ( 0.000000000000000000, 130.3999865490244190, 45.94057108883949070 ) ) ;
#42503=CARTESIAN_POINT ( 'NONE',  ( -5.082755093536317936, -5.082755093536320601, 0.1740527818717522990 ) ) ;
#42522=B_SPLINE_CURVE_WITH_KNOTS ( 'NONE', 3,
 ( #63158, #26301, #63529, #11853, #34520, #56770, #5457, #28459, #189, #22043, #51465, #22409, #3314 ),
 .UNSPECIFIED., .F., .F.,
 ( 4, 2, 2, 1, 2, 2, 4 ),
 ( 0.8219935333350478768, 0.8664951500012858521, 0.8887459583344048397, 0.9109967666675239384, 0.9332475750006429260, 0.9554983833337619137, 1.000000000000000000 ),
 .UNSPECIFIED. ) ;
#42530=CARTESIAN_POINT ( 'NONE',  ( 5.082755093536318824, 5.082755093536319713, 4.299052781871752771 ) ) ;
#42535=CARTESIAN_POINT ( 'NONE',  ( -7.594050593749991585, 0.000000000000000000, 29.09592778084756048 ) ) ;
#42546=CARTESIAN_POINT ( 'NONE',  ( 5.656854249492374365, 5.656854249492375253, 27.45530278392014978 ) ) ;
#42556=CARTESIAN_POINT ( 'NONE',  ( 7.999999999999932498, -3.313708498984815787, 27.17405278392014623 ) ) ;
#42566=CARTESIAN_POINT ( 'NONE',  ( 7.188101187499992051, 8.802885111219154394E-16, 21.73655278187175455 ) ) ;
#42568=CARTESIAN_POINT ( 'NONE',  ( 7.999999999999991118, 9.797174393178815797E-16, 16.76780278392014978 ) ) ;
#42575=CARTESIAN_POINT ( 'NONE',  ( -5.656854249492373476, -5.656854249492376141, 14.70530278392014800 ) ) ;
#42582=CARTESIAN_POINT ( 'NONE',  ( -7.999999999999991118, 0.000000000000000000, 21.83030277982336997 ) ) ;
#42585=CARTESIAN_POINT ( 'NONE',  ( -5.082755093536317936, -5.082755093536320601, 16.67405278187175810 ) ) ;
#42590=CARTESIAN_POINT ( 'NONE',  ( 3.313708498984762496, -7.999999999999989342, 5.986552783920146226 ) ) ;
#42599=CARTESIAN_POINT ( 'NONE',  ( -5.656854249492375253, 5.656854249492375253, 15.64280277982336642 ) ) ;
#42604=CARTESIAN_POINT ( 'NONE',  ( 7.999999999999991118, 3.313708498984757611, 24.36155278392014623 ) ) ;
#42611=CARTESIAN_POINT ( 'NONE',  ( 1.320432766682872962E-15, -7.188101187499992051, 20.23655278187175455 ) ) ;
#42619=CARTESIAN_POINT ( 'NONE',  ( -7.999999999999968914, 3.313708498984778039, 18.73655277982336287 ) ) ;
#42628=CARTESIAN_POINT ( 'NONE',  ( -3.313708498984757167, 7.999999999999991118, 17.04905277982336642 ) ) ;
#42644=CARTESIAN_POINT ( 'NONE',  ( 3.313708498984762496, -7.999999999999989342, 14.85530278432982243 ) ) ;
#42673=CARTESIAN_POINT ( 'NONE',  ( -7.188101187499991163, 2.977408999572646930, 8.892802781871754547 ) ) ;
#42696=CARTESIAN_POINT ( 'NONE',  ( -7.188101187499992051, 2.977408999572646930, 4.767802781871752771 ) ) ;
#42727=CARTESIAN_POINT ( 'NONE',  ( -5.656854249492375253, 5.656854249492375253, 5.330302783920146226 ) ) ;
#42743=CARTESIAN_POINT ( 'NONE',  ( -8.008118988124991233, 3.317071493978878127, 9.919365283940628331 ) ) ;
#42749=CARTESIAN_POINT ( 'NONE',  ( -7.188101187499992051, 2.977408999572646930, 4.392802781871752771 ) ) ;
#42761=CARTESIAN_POINT ( 'NONE',  ( -7.188101187499992051, 0.000000000000000000, 23.98655278187175455 ) ) ;
#42767=CARTESIAN_POINT ( 'NONE',  ( -1.060465953394920335, 8.000079534944177340, -0.000000000000000000 ) ) ;
#42780=CARTESIAN_POINT ( 'NONE',  ( 7.999999999999991118, 3.313708498984758055, 1.861552783920143117 ) ) ;
#42784=DIRECTION ( 'NONE',  ( 1.000000000000000000, 0.000000000000000000, 0.000000000000000000 ) ) ;
#42785=CARTESIAN_POINT ( 'NONE',  ( 2.977408999572650927, -7.188101187499990274, 21.83030278187175810 ) ) ;
#42798=DIRECTION ( 'NONE',  ( -0.000000000000000000, -0.000000000000000000, 1.000000000000000000 ) ) ;
#42802=CARTESIAN_POINT ( 'NONE',  ( -7.999999999999991118, 0.000000000000000000, 14.33030277982336465 ) ) ;
#42815=CARTESIAN_POINT ( 'NONE',  ( 7.999999999999991118, 9.797174393178815797E-16, 27.08030277982336642 ) ) ;
#42865=CARTESIAN_POINT ( 'NONE',  ( 5.082755093536318824, 5.082755093536319713, 26.79905278187175455 ) ) ;
#42884=AXIS2_PLACEMENT_3D ( 'NONE', #29367, #64061, #53115 ) ;
#42890=CARTESIAN_POINT ( 'NONE',  ( 7.188101187499992051, 8.802885111219154394E-16, 1.111552781871753215 ) ) ;
#42906=CARTESIAN_POINT ( 'NONE',  ( 7.999999999999991118, 9.797174393178815797E-16, 21.26780278392014623 ) ) ;
#42919=CARTESIAN_POINT ( 'NONE',  ( -7.999999999999976019, -3.611371706259009353E-07, 26.51781575558936055 ) ) ;
#42929=CARTESIAN_POINT ( 'NONE',  ( 5.082755093536320601, -5.082755093536318824, 23.04905278187175455 ) ) ;
#42939=CARTESIAN_POINT ( 'NONE',  ( -3.313708498984757167, 7.999999999999991118, 14.23655278392014623 ) ) ;
#42951=CARTESIAN_POINT ( 'NONE',  ( -7.188101187499990274, -2.977408999572651371, 21.08030278187175810 ) ) ;
#42957=CARTESIAN_POINT ( 'NONE',  ( -7.999999999961182162, -1.665870058181487338E-05, 5.518425684709454160 ) ) ;
#42968=CARTESIAN_POINT ( 'NONE',  ( 5.662595241051936235, -5.662595241051934458, 0.07561528394062884406 ) ) ;
#42975=CARTESIAN_POINT ( 'NONE',  ( 1.320432766682872962E-15, -7.188101187499992051, 21.73655278187175455 ) ) ;
#42993=CARTESIAN_POINT ( 'NONE',  ( 1.469576158976822172E-15, -7.999999999999991118, 10.20530277982336465 ) ) ;
#43008=CARTESIAN_POINT ( 'NONE',  ( 5.656854249492374365, 5.656854249492375253, 19.82405278432982243 ) ) ;
#43041=CARTESIAN_POINT ( 'NONE',  ( 7.188101187499992051, 8.802885111219154394E-16, 5.236552781871753659 ) ) ;
#43067=CARTESIAN_POINT ( 'NONE',  ( -4.401442555609577197E-16, 7.188101187499992051, 5.986552781871753659 ) ) ;
#43074=ORIENTED_EDGE ( 'NONE', *, *, #22473, .F. ) ;
#43075=( BOUNDED_CURVE ( )  B_SPLINE_CURVE ( 2, ( #58887, #42619, #66758, #65261, #32059, #30932, #3762, #3387, #72415 ),
 .UNSPECIFIED., .F., .F. ) 
 B_SPLINE_CURVE_WITH_KNOTS ( ( 3, 2, 2, 2, 3 ),
 ( 0.3684210526315789824, 0.3750000000000000555, 0.3815789473684211286, 0.3881578947368421462, 0.3947368421052632192 ),
 .UNSPECIFIED. ) 
 CURVE ( )  GEOMETRIC_REPRESENTATION_ITEM ( )  RATIONAL_B_SPLINE_CURVE ( ( 0.9999999999999993339, 0.9238795325112874046, 1.000000000000000000, 0.9238795325112867385, 1.000000000000000000, 0.9238795325112867385, 1.000000000000000000, 0.9238795325112860723, 1.000000000000000666 ) ) 
 REPRESENTATION_ITEM ( '' )  );
#43089=CARTESIAN_POINT ( 'NONE',  ( -7.999999999999991118, 0.000000000000000000, 25.01780278392014978 ) ) ;
#43096=CARTESIAN_POINT ( 'NONE',  ( -7.999999999999991118, 0.000000000000000000, 8.517802783920146226 ) ) ;
#43113=CARTESIAN_POINT ( 'NONE',  ( -4.903558642999205574E-16, 8.008118988124991233, 11.13811528394063188 ) ) ;
#43120=CARTESIAN_POINT ( 'NONE',  ( 7.188101187499992051, 2.977408999572647819, 3.830302781871751883 ) ) ;
#43135=CARTESIAN_POINT ( 'NONE',  ( -2.977408999572648707, -7.188101187499990274, 25.76780278187175810 ) ) ;
#43141=CARTESIAN_POINT ( 'NONE',  ( 6.406660676652354169, 4.906935342933127053, 0.000000000000000000 ) ) ;
#43155=CARTESIAN_POINT ( 'NONE',  ( -3.313708498984757611, 7.999999999999991118, 2.236552783920144005 ) ) ;
#43160=CARTESIAN_POINT ( 'NONE',  ( -2.977408999572647819, -7.188101187499990274, 21.64280278187176165 ) ) ;
#43177=CARTESIAN_POINT ( 'NONE',  ( 7.999999999999991118, 9.797174393178815797E-16, 13.76780278392014623 ) ) ;
#43178=CARTESIAN_POINT ( 'NONE',  ( -3.313708498984758943, -7.999999999999989342, 7.111552779823365533 ) ) ;
#43182=CARTESIAN_POINT ( 'NONE',  ( -7.999999999999991118, 9.797174393178815797E-16, 30.00000000000000000 ) ) ;
#43187=ORIENTED_EDGE ( 'NONE', *, *, #26521, .F. ) ;
#43208=CARTESIAN_POINT ( 'NONE',  ( -8.008118988124991233, 0.000000000000000000, 25.01311528394063544 ) ) ;
#43244=CARTESIAN_POINT ( 'NONE',  ( 7.188101187499991163, 2.977408999572648707, 2.330302781871750550 ) ) ;
#43269=CARTESIAN_POINT ( 'NONE',  ( -3.313708498984757167, 7.999999999999991118, 29.04905277982337353 ) ) ;
#43281=AXIS2_PLACEMENT_3D ( 'NONE', #31607, #48942, #65559 ) ;
#43288=CARTESIAN_POINT ( 'NONE',  ( 1.469576158976822172E-15, -7.999999999999991118, 19.39280278392014978 ) ) ;
#43309=CARTESIAN_POINT ( 'NONE',  ( -4.401442555609577197E-16, 7.188101187499992051, 19.11155278187175455 ) ) ;
#43317=CARTESIAN_POINT ( 'NONE',  ( 7.999999999999992895, -3.313708498984756279, 13.67405278392014978 ) ) ;
#43328=CARTESIAN_POINT ( 'NONE',  ( -7.188101187499990274, -2.977408999572651371, 16.58030278187175455 ) ) ;
#43346=CARTESIAN_POINT ( 'NONE',  ( -7.999999999999989342, -3.313708498984762496, 26.61155278392014978 ) ) ;
#43353=CARTESIAN_POINT ( 'NONE',  ( -2.977408999572647819, 7.188101187499991163, 24.08030278187175455 ) ) ;
#43369=CARTESIAN_POINT ( 'NONE',  ( 3.313708498984762496, -7.999999999999989342, 8.799052779823364645 ) ) ;
#43386=CARTESIAN_POINT ( 'NONE',  ( 7.999999999999991118, 9.797174393178815797E-16, 9.136552784329824206 ) ) ;
#43417=CARTESIAN_POINT ( 'NONE',  ( 7.188101187499992051, 8.802885111219154394E-16, 8.236552781871752771 ) ) ;
#43432=CARTESIAN_POINT ( 'NONE',  ( -7.188101187499992051, 0.000000000000000000, 12.36155278187175277 ) ) ;
#43433=ORIENTED_EDGE ( 'NONE', *, *, #46814, .F. ) ;
#43443=CARTESIAN_POINT ( 'NONE',  ( 5.082755093536320601, -5.082755093536318824, 3.924052781871752327 ) ) ;
#43460=CARTESIAN_POINT ( 'NONE',  ( 5.656854249492376141, -5.656854249492374365, 28.39280277982336642 ) ) ;
#43466=CARTESIAN_POINT ( 'NONE',  ( -7.999999999999991118, 6.760989533162280693E-06, 25.01780259264117134 ) ) ;
#43472=CARTESIAN_POINT ( 'NONE',  ( -7.999999999999991118, -9.344071862984236532, 28.15091120252598245 ) ) ;
#43486=ORIENTED_EDGE ( 'NONE', *, *, #73472, .T. ) ;
#43495=CARTESIAN_POINT ( 'NONE',  ( 5.082755093536318824, 5.082755093536319713, 3.924052781871752327 ) ) ;
#43500=AXIS2_PLACEMENT_3D ( 'NONE', #8010, #13283, #2726 ) ;
#43507=CARTESIAN_POINT ( 'NONE',  ( 7.188101187499992051, 8.802885111219154394E-16, 26.23655278187175810 ) ) ;
#43530=CARTESIAN_POINT ( 'NONE',  ( -5.082755093536319713, 5.082755093536319713, 22.67405278187175455 ) ) ;
#43532=CARTESIAN_POINT ( 'NONE',  ( -3.313708498984759387, -7.999999999999989342, 22.29905278392014623 ) ) ;
#43534=CYLINDRICAL_SURFACE ( 'NONE', #42884, 7.999999999999991118 ) ;
#43541=CARTESIAN_POINT ( 'NONE',  ( -4.898587196589407898E-16, 7.999999999999991118, 17.14280278392014978 ) ) ;
#43551=CARTESIAN_POINT ( 'NONE',  ( 3.313708498984756279, 7.999999999999991118, 10.86155277982336820 ) ) ;
#43562=CARTESIAN_POINT ( 'NONE',  ( 1.469576158976822172E-15, -7.999999999999991118, 10.39280278392014800 ) ) ;
#43583=CARTESIAN_POINT ( 'NONE',  ( 5.662595241051936235, -5.662595241051934458, 24.07561528394063188 ) ) ;
#43620=CARTESIAN_POINT ( 'NONE',  ( -5.082755093536317936, -5.082755093536320601, 27.54905278187175455 ) ) ;
#43622=CARTESIAN_POINT ( 'NONE',  ( 0.000000000000000000, 0.000000000000000000, 30.00000000000000000 ) ) ;
#43647=CARTESIAN_POINT ( 'NONE',  ( -7.999999999999989342, -3.313708498984762496, 27.92405277982336642 ) ) ;
#43652=CARTESIAN_POINT ( 'NONE',  ( 7.999999999999991118, 9.797174393178815797E-16, 13.58030277982336465 ) ) ;
#43665=CARTESIAN_POINT ( 'NONE',  ( 7.999999999999992895, -3.313708498984756279, 16.67405278392014623 ) ) ;
#43689=CARTESIAN_POINT ( 'NONE',  ( 2.977408999572650927, -7.188101187499990274, 16.95530278187175455 ) ) ;
#43699=CARTESIAN_POINT ( 'NONE',  ( 1.469576158976822172E-15, -7.999999999999991118, 16.39280278392014978 ) ) ;
#43701=VERTEX_POINT ( 'NONE', #21279 ) ;
#43711=CARTESIAN_POINT ( 'NONE',  ( -2.977408999572648707, -7.188101187499990274, 16.76780278187175099 ) ) ;
#43713=EDGE_CURVE ( 'NONE', #21067, #5549, #69127, .T. ) ;
#43717=CARTESIAN_POINT ( 'NONE',  ( 7.999979274741570556, -3.313729224243177729, 24.17405195469602575 ) ) ;
#43723=CARTESIAN_POINT ( 'NONE',  ( 7.999999999999991118, 0.000000000000000000, 30.00000000000000000 ) ) ;
#43728=CARTESIAN_POINT ( 'NONE',  ( -7.999999999999991118, 0.000000000000000000, 25.01780278392014978 ) ) ;
#43735=CARTESIAN_POINT ( 'NONE',  ( -5.082755093536317936, -5.082755093536320601, 15.54905278187175632 ) ) ;
#43744=CARTESIAN_POINT ( 'NONE',  ( -7.999999999999991118, 0.000000000000000000, 26.33030277982336997 ) ) ;
#43752=CARTESIAN_POINT ( 'NONE',  ( 1.469576158976822172E-15, -7.999999999999991118, 11.70530277982336642 ) ) ;
#43768=CARTESIAN_POINT ( 'NONE',  ( -7.999999999999991118, 0.000000000000000000, 11.38655278432982243 ) ) ;
#43779=EDGE_CURVE ( 'NONE', #39327, #19453, #33006, .T. ) ;
#43796=ORIENTED_EDGE ( 'NONE', *, *, #37866, .T. ) ;
#43803=CARTESIAN_POINT ( 'NONE',  ( -2.977408999572648707, -7.188101187499990274, 4.767802781871753659 ) ) ;
#43804=ORIENTED_EDGE ( 'NONE', *, *, #68544, .T. ) ;
#43816=CARTESIAN_POINT ( 'NONE',  ( 7.188101187499992051, 8.802885111219154394E-16, 10.11155278187175455 ) ) ;
#43828=CARTESIAN_POINT ( 'NONE',  ( 5.082755093536320601, -5.082755093536318824, 6.924052781871754547 ) ) ;
#43844=CARTESIAN_POINT ( 'NONE',  ( 7.999999999999992895, -3.313708498984756279, 26.98655277982336997 ) ) ;
#43855=CARTESIAN_POINT ( 'NONE',  ( -3.313708498984758943, -7.999999999999989342, -0.2009472160798553009 ) ) ;
#43857=CARTESIAN_POINT ( 'NONE',  ( 0.000000000000000000, 15.08051212944140218, 15.04081104653146994 ) ) ;
#43859=CYLINDRICAL_SURFACE ( 'NONE', #66328, 7.999999999999991118 ) ;
#43877=CARTESIAN_POINT ( 'NONE',  ( -7.188101187499992051, 2.977408999572646930, 5.892802781871753659 ) ) ;
#43886=EDGE_CURVE ( 'NONE', #44274, #4443, #22836, .T. ) ;
#43892=CARTESIAN_POINT ( 'NONE',  ( -3.313708498984759387, -7.999999999999989342, 10.11155277982336642 ) ) ;
#43893=CARTESIAN_POINT ( 'NONE',  ( -7.188101187499991163, 2.977408999572646930, 23.89280278187176165 ) ) ;
#43918=CARTESIAN_POINT ( 'NONE',  ( 7.188101187499992051, 2.977408999572647819, 25.20530278187175810 ) ) ;
#43928=CARTESIAN_POINT ( 'NONE',  ( 7.999992860684751683, 3.313715638299997490, 16.86155306956639777 ) ) ;
#43937=CARTESIAN_POINT ( 'NONE',  ( -7.999999999999991118, 0.000000000000000000, 9.830302779823364645 ) ) ;
#43947=CARTESIAN_POINT ( 'NONE',  ( 5.656854249492376141, -5.656854249492374365, 10.58030278392014800 ) ) ;
#43965=CARTESIAN_POINT ( 'NONE',  ( 5.662595241051936235, -5.662595241051934458, 21.07561528394063188 ) ) ;
#43966=CARTESIAN_POINT ( 'NONE',  ( -3.313708498984757611, 7.999999999999991118, 23.23655278392014978 ) ) ;
#44003=CARTESIAN_POINT ( 'NONE',  ( -5.082755093536317936, -5.082755093536320601, 23.04905278187175455 ) ) ;
#44029=CARTESIAN_POINT ( 'NONE',  ( 7.999999999999991118, 3.313708498984757611, 27.17405277982336997 ) ) ;
#44048=CARTESIAN_POINT ( 'NONE',  ( -7.999999999999989342, -3.313708498984762496, 16.11155278392014267 ) ) ;
#44069=CARTESIAN_POINT ( 'NONE',  ( -2.977408999572647819, 7.188101187499992051, 17.70530278187175455 ) ) ;
#44080=CARTESIAN_POINT ( 'NONE',  ( 3.313708498984756279, 7.999999999999991118, 9.549052783920146226 ) ) ;
#44094=CARTESIAN_POINT ( 'NONE',  ( -5.082755093536317936, -5.082755093536320601, 13.67405278187175455 ) ) ;
#44119=CARTESIAN_POINT ( 'NONE',  ( -5.082755093536319713, 5.082755093536319713, 15.17405278187175455 ) ) ;
#44126=ORIENTED_EDGE ( 'NONE', *, *, #17047, .F. ) ;
#44133=FACE_OUTER_BOUND ( 'NONE', #32895, .T. ) ;
#44136=CARTESIAN_POINT ( 'NONE',  ( -3.313708498984757167, 7.999999999999991118, 11.04905277982336642 ) ) ;
#44148=CARTESIAN_POINT ( 'NONE',  ( 7.999999999999991118, 9.797174393178815797E-16, 13.63655278432982421 ) ) ;
#44180=CARTESIAN_POINT ( 'NONE',  ( -7.188101187499990274, -2.977408999572651371, 9.080302781871752771 ) ) ;
#44184=CARTESIAN_POINT ( 'NONE',  ( 7.999999999999991118, 3.313708498984758055, 19.67405277982336642 ) ) ;
#44194=CARTESIAN_POINT ( 'NONE',  ( 7.188101187499993827, -2.977408999572645598, 13.01780278187175277 ) ) ;
#44208=CARTESIAN_POINT ( 'NONE',  ( -2.977408999572647819, 7.188101187499992051, 6.080302781871753659 ) ) ;
#44224=CARTESIAN_POINT ( 'NONE',  ( -7.999999999999991118, 0.000000000000000000, 24.83030277982336642 ) ) ;
#44238=CARTESIAN_POINT ( 'NONE',  ( -7.999999999999989342, -3.313708498984762496, 1.111552783920146004 ) ) ;
#44249=CARTESIAN_POINT ( 'NONE',  ( -5.656854249492375253, 5.656854249492375253, 0.8303027839201455595 ) ) ;
#44260=CARTESIAN_POINT ( 'NONE',  ( 5.082755093536318824, 5.082755093536319713, 0.9240527818717529929 ) ) ;
#44271=CARTESIAN_POINT ( 'NONE',  ( 7.188101187499992051, 8.802885111219154394E-16, 23.23655278187175455 ) ) ;
#44274=VERTEX_POINT ( 'NONE', #8217 ) ;
#44283=ORIENTED_EDGE ( 'NONE', *, *, #13983, .T. ) ;
#44293=CARTESIAN_POINT ( 'NONE',  ( 7.188101187499993827, -2.977408999572645598, 22.01780278187175810 ) ) ;
#44303=DIRECTION ( 'NONE',  ( -0.000000000000000000, -0.000000000000000000, 1.000000000000000000 ) ) ;
#44311=CARTESIAN_POINT ( 'NONE',  ( -4.898587196589407898E-16, 7.999999999999991118, 10.95530277982336642 ) ) ;
#44319=CARTESIAN_POINT ( 'NONE',  ( -7.999999999999948486, 3.313708498984799355, 2.236552779823363313 ) ) ;
#44342=CARTESIAN_POINT ( 'NONE',  ( 3.317071493978883456, -8.008118988124989457, 17.98186528394063188 ) ) ;
#44349=CARTESIAN_POINT ( 'NONE',  ( 3.499857865026532622, -7.193933550196781823, 0.0006324257780546024528 ) ) ;
#44369=CARTESIAN_POINT ( 'NONE',  ( 3.313708498984762496, -7.999999999999989342, 2.799052779823365977 ) ) ;
#44375=CARTESIAN_POINT ( 'NONE',  ( -2.977408999572647819, 7.188101187499991163, 22.58030278187175099 ) ) ;
#44378=CARTESIAN_POINT ( 'NONE',  ( 0.000000000000000000, 0.000000000000000000, 30.00000000000000000 ) ) ;
#44399=CARTESIAN_POINT ( 'NONE',  ( 7.999999999999991118, 9.797174393178815797E-16, 27.08030277982336642 ) ) ;
#44418=CARTESIAN_POINT ( 'NONE',  ( 7.999999999999991118, 9.797174393178815797E-16, 18.26780278392014623 ) ) ;
#44439=( BOUNDED_CURVE ( )  B_SPLINE_CURVE ( 2, ( #3625, #26242, #20588, #38333, #4008, #26621, #67373, #49645, #27742 ),
 .UNSPECIFIED., .F., .F. ) 
 B_SPLINE_CURVE_WITH_KNOTS ( ( 3, 2, 2, 2, 3 ),
 ( 0.5263157894736842923, 0.5328947368421054209, 0.5394736842105263275, 0.5460526315789473450, 0.5526315789473684736 ),
 .UNSPECIFIED. ) 
 CURVE ( )  GEOMETRIC_REPRESENTATION_ITEM ( )  RATIONAL_B_SPLINE_CURVE ( ( 0.9999999999999986677, 0.9238795325112880708, 1.000000000000000000, 0.9238795325112867385, 1.000000000000000000, 0.9238795325112867385, 1.000000000000000000, 0.9238795325112867385, 1.000000000000000000 ) ) 
 REPRESENTATION_ITEM ( '' )  );
#44441=CARTESIAN_POINT ( 'NONE',  ( -7.188101187499990274, -2.977408999572651815, 15.08030278187175455 ) ) ;
#44464=CARTESIAN_POINT ( 'NONE',  ( -5.082755093536319713, 5.082755093536319713, 10.29905278187175455 ) ) ;
#44469=CARTESIAN_POINT ( 'NONE',  ( 7.999999999999971578, -3.313708498984776707, 17.98655277982336997 ) ) ;
#44471=CYLINDRICAL_SURFACE ( 'NONE', #58848, 7.999999999999991118 ) ;
#44488=CARTESIAN_POINT ( 'NONE',  ( -2.977408999572648707, -7.188101187499990274, 17.14280278187175455 ) ) ;
#44491=CARTESIAN_POINT ( 'NONE',  ( 7.999973942808394689, -3.313734556176354484, 1.674051741363694168 ) ) ;
#44505=CARTESIAN_POINT ( 'NONE',  ( 5.656854249492376141, -5.656854249492374365, 8.892802779823364645 ) ) ;
#44519=CARTESIAN_POINT ( 'NONE',  ( 5.656854249492376141, -5.656854249492374365, 13.44905278432982421 ) ) ;
#44553=CARTESIAN_POINT ( 'NONE',  ( 2.977408999572650927, -7.188101187499990274, 0.4553027818717525488 ) ) ;
#44562=EDGE_CURVE ( 'NONE', #59945, #60307, #28581, .T. ) ;
#44566=CARTESIAN_POINT ( 'NONE',  ( -7.188101187499991163, 2.977408999572646930, 7.767802781871751883 ) ) ;
#44608=CARTESIAN_POINT ( 'NONE',  ( -4.898587196589407898E-16, 7.999999999999991118, 27.51155278432982598 ) ) ;
#44640=CARTESIAN_POINT ( 'NONE',  ( -7.999999999999991118, 0.000000000000000000, 9.830302779823364645 ) ) ;
#44641=CARTESIAN_POINT ( 'NONE',  ( 7.188101187499992051, 8.802885111219154394E-16, 18.73655278187175455 ) ) ;
#44667=CARTESIAN_POINT ( 'NONE',  ( -5.082755093536319713, 5.082755093536319713, 16.67405278187175810 ) ) ;
#44684=CARTESIAN_POINT ( 'NONE',  ( 7.999999999999991118, 3.313708498984757611, 6.174052779823364645 ) ) ;
#44693=ORIENTED_EDGE ( 'NONE', *, *, #41291, .T. ) ;
#44712=CARTESIAN_POINT ( 'NONE',  ( -8.008118988124991233, 3.317071493978878127, 17.41936528394063188 ) ) ;
#44747=CARTESIAN_POINT ( 'NONE',  ( -5.082755093536319713, 5.082755093536319713, 24.17405278187175455 ) ) ;
#44773=CARTESIAN_POINT ( 'NONE',  ( -5.656854249492375253, 5.656854249492375253, 26.14280277982336997 ) ) ;
#44787=CARTESIAN_POINT ( 'NONE',  ( -2.243032484811285964E-15, 18.31575019322283993, 2.966738217918089671 ) ) ;
#44792=CARTESIAN_POINT ( 'NONE',  ( -7.999999999999991118, 3.313708498984756723, 14.42405278392014800 ) ) ;
#44802=CARTESIAN_POINT ( 'NONE',  ( -6.062601303906716588, -5.219661428662635494, 1.000679062340938064 ) ) ;
#44812=CARTESIAN_POINT ( 'NONE',  ( -5.082755093536317936, -5.082755093536320601, 16.67405278187175810 ) ) ;
#44815=ORIENTED_EDGE ( 'NONE', *, *, #19750, .F. ) ;
#44838=CARTESIAN_POINT ( 'NONE',  ( -7.188101187499991163, 2.977408999572646930, 11.89280278187175277 ) ) ;
#44843=CARTESIAN_POINT ( 'NONE',  ( 5.656854249492376141, -5.656854249492374365, 17.89280277982336642 ) ) ;
#44863=CARTESIAN_POINT ( 'NONE',  ( -7.188101187499991163, 2.977408999572646930, 18.26780278187175455 ) ) ;
#44879=CARTESIAN_POINT ( 'NONE',  ( -5.656854249492375253, 5.656854249492375253, 2.142802779823364645 ) ) ;
#44895=CARTESIAN_POINT ( 'NONE',  ( 3.313708498984756279, 7.999999999999991118, 13.91780278432982421 ) ) ;
#44897=CARTESIAN_POINT ( 'NONE',  ( -5.656854249492375253, 5.656854249492375253, 5.142802779823363757 ) ) ;
#44901=EDGE_LOOP ( 'NONE', ( #40186, #39398, #14642, #29236 ) ) ;
#44903=( BOUNDED_CURVE ( )  B_SPLINE_CURVE ( 2, ( #21869, #10563, #44897, #56600, #4916, #10, #27910, #45632, #22997 ),
 .UNSPECIFIED., .F., .F. ) 
 B_SPLINE_CURVE_WITH_KNOTS ( ( 3, 2, 2, 2, 3 ),
 ( 0.8421052631578948011, 0.8486842105263159297, 0.8552631578947369473, 0.8618421052631578538, 0.8684210526315789824 ),
 .UNSPECIFIED. ) 
 CURVE ( )  GEOMETRIC_REPRESENTATION_ITEM ( )  RATIONAL_B_SPLINE_CURVE ( ( 0.9999999999999986677, 0.9238795325112880708, 1.000000000000000000, 0.9238795325112867385, 1.000000000000000000, 0.9238795325112867385, 1.000000000000000000, 0.9238795325112867385, 1.000000000000000000 ) ) 
 REPRESENTATION_ITEM ( '' )  );
#44927=CARTESIAN_POINT ( 'NONE',  ( -2.977408999572647819, 7.188101187499991163, 1.205302781871753215 ) ) ;
#44929=EDGE_LOOP ( 'NONE', ( #7232, #25733, #31460, #1440 ) ) ;
#44940=CARTESIAN_POINT ( 'NONE',  ( 7.188101187499992051, 8.802885111219154394E-16, 4.111552781871752771 ) ) ;
#44959=CARTESIAN_POINT ( 'NONE',  ( -7.999999999999991118, 3.313708498984757167, 29.23655277982336642 ) ) ;
#44969=CARTESIAN_POINT ( 'NONE',  ( -7.999999999999991118, 3.313708498984756723, 20.23655277982336642 ) ) ;
#44981=CARTESIAN_POINT ( 'NONE',  ( -5.656854249492375253, 5.656854249492375253, 3.830302783920144893 ) ) ;
#44990=CARTESIAN_POINT ( 'NONE',  ( -3.313708498984757611, 7.999999999999991118, 0.7365527839201455595 ) ) ;
#44992=( BOUNDED_CURVE ( )  B_SPLINE_CURVE ( 2, ( #48077, #30738, #36040, #59056, #6994, #42415, #54127, #2067, #25056, #19044, #18685, #41691, #1350, #42048, #25431, #35312, #19777, #53391, #71085, #30005, #65433, #1716, #13729, #24334, #52647, #36774, #70003, #71449, #63965, #12277, #58323, #23965, #46973, #66929, #8462, #2811, #32996, #60892, #61269, #43918, #60142, #9214, #21269, #20516, #9965, #61646, #4310, #54505, #49573, #55625, #26930, #48820, #20896, #9598, #71827, #15234, #32617, #37139, #8844, #20144, #72203, #66545, #3941, #26173, #14480, #31482, #43530, #49949, #50316, #25800, #73337, #72964, #14107, #44293, #67307, #42785, #3559, #43160, #66176, #14854, #38265, #15605, #38644, #55996, #31854, #60518, #27300, #65801, #54877, #37519, #3187, #49192, #37894, #32235, #55252, #26549, #72591, #5796, #45773, #45395, #68411, #51431, #51061, #57106, #68049, #34855, #10701, #62741, #11818, #39741, #11081, #51809, #21641, #156, #74443, #28793, #57861, #33735, #34108, #23132, #22014, #73702, #46144, #56737, #15978, #17094, #5419, #39008, #4682, #5056, #44667, #62374, #16711, #28424, #22750, #68785, #67681, #34485, #40116, #69161, #74074, #62011, #63122, #50683, #40491, #11450, #57491, #17470, #63496, #10336, #6167, #22374, #33361, #28052, #45040, #16340, #27677, #29176, #52191, #56362, #39377, #58966, #24239, #47252, #8004, #70279, #31011, #30648, #46517, #36317, #64968, #522, #35948, #6537, #35219, #52929, #1626, #12553, #13277, #1260, #58239, #18222, #24970, #53302, #41237, #29543, #52554, #12182, #41602, #6901, #7274, #18591, #64617, #63870, #47614, #893, #23879, #64243, #23502, #69536, #46888, #30281, #12913, #24606, #69912, #35581, #58595, #13646, #70999, #70637, #59332, #18956, #17847, #41960, #29912, #7643, #53666, #40864, #1978, #47986, #19315, #42327, #65345, #36685, #59696, #19687, #3096, #26080, #61558, #49102, #9879, #9512, #25341, #15146, #43828, #54036, #14767, #60050, #14013, #31765, #55163, #32527, #38178, #44208, #43067, #71735, #3849, #32143, #20051, #37050, #31387, #65709, #20427, #60427, #60801, #72114, #54784, #42696, #26458, #8371, #54413, #61182, #66843, #20810, #49482, #37805, #43443, #66458, #2720, #25708, #48729, #67221, #49860, #9126, #55539, #3469, #48355, #14393, #66083, #2347, #72878, #26845, #72501, #21183, #37427, #15517, #38557, #71361, #8754, #10249, #63038, #51719, #57025, #34027, #39662, #39293, #16254, #21923, #68330, #67, #4224, #62293, #16627, #50598, #34397 ),
 .UNSPECIFIED., .F., .F. ) 
 B_SPLINE_CURVE_WITH_KNOTS ( ( 3, 2, 2, 2, 2, 2, 2, 2, 2, 2, 2, 2, 2, 2, 2, 2, 2, 2, 2, 2, 2, 2, 2, 2, 2, 2, 2, 2, 2, 2, 2, 2, 2, 2, 2, 2, 2, 2, 2, 2, 2, 2, 2, 2, 2, 2, 2, 2, 2, 2, 2, 2, 2, 2, 2, 2, 2, 2, 2, 2, 2, 2, 2, 2, 2, 2, 2, 2, 2, 2, 2, 2, 2, 2, 2, 2, 2, 2, 2, 2, 2, 2, 2, 2, 2, 2, 2, 2, 2, 2, 2, 2, 2, 2, 2, 2, 2, 2, 2, 2, 2, 2, 2, 2, 2, 2, 2, 2, 2, 2, 2, 2, 2, 2, 2, 2, 2, 2, 2, 2, 2, 2, 2, 2, 2, 2, 2, 2, 2, 2, 2, 2, 2, 2, 2, 2, 2, 2, 2, 2, 2, 2, 2, 2, 2, 2, 2, 2, 2, 2, 2, 2, 3 ),
 ( 0.000000000000000000, 0.006578947368421052266, 0.01315789473684210453, 0.01973684210526315680, 0.02631578947368420907, 0.03289473684210526133, 0.03947368421052631360, 0.04605263157894736586, 0.05263157894736841813, 0.05921052631578947040, 0.06578947368421052266, 0.07236842105263158187, 0.07894736842105262720, 0.08552631578947368640, 0.09210526315789473173, 0.09868421052631579093, 0.1052631578947368363, 0.1118421052631578955, 0.1184210526315789408, 0.1250000000000000000, 0.1315789473684210453, 0.1381578947368421184, 0.1447368421052631637, 0.1513157894736842091, 0.1578947368421052544, 0.1644736842105263275, 0.1710526315789473728, 0.1776315789473684181, 0.1842105263157894635, 0.1907894736842105365, 0.1973684210526315819, 0.2039473684210526272, 0.2105263157894736725, 0.2171052631578947456, 0.2236842105263157909, 0.2302631578947368363, 0.2368421052631578816, 0.2434210526315789547, 0.2500000000000000000, 0.2565789473684210731, 0.2631578947368420907, 0.2697368421052631637, 0.2763157894736842368, 0.2828947368421052544, 0.2894736842105263275, 0.2960526315789473450, 0.3026315789473684181, 0.3092105263157894912, 0.3157894736842105088, 0.3223684210526315819, 0.3289473684210526550, 0.3355263157894736725, 0.3421052631578947456, 0.3486842105263157632, 0.3552631578947368363, 0.3618421052631579093, 0.3684210526315789269, 0.3750000000000000000, 0.3815789473684210731, 0.3881578947368420907, 0.3947368421052631637, 0.4013157894736842368, 0.4078947368421052544, 0.4144736842105263275, 0.4210526315789473450, 0.4276315789473684181, 0.4342105263157894912, 0.4407894736842105088, 0.4473684210526315819, 0.4539473684210526550, 0.4605263157894736725, 0.4671052631578947456, 0.4736842105263157632, 0.4802631578947368363, 0.4868421052631579093, 0.4934210526315789269, 0.5000000000000000000, 0.5065789473684210176, 0.5131578947368421462, 0.5197368421052631637, 0.5263157894736841813, 0.5328947368421053099, 0.5394736842105263275, 0.5460526315789473450, 0.5526315789473684736, 0.5592105263157894912, 0.5657894736842105088, 0.5723684210526315264, 0.5789473684210526550, 0.5855263157894736725, 0.5921052631578946901, 0.5986842105263158187, 0.6052631578947368363, 0.6118421052631578538, 0.6184210526315789824, 0.6250000000000000000, 0.6315789473684210176, 0.6381578947368421462, 0.6447368421052631637, 0.6513157894736841813, 0.6578947368421053099, 0.6644736842105263275, 0.6710526315789473450, 0.6776315789473684736, 0.6842105263157894912, 0.6907894736842105088, 0.6973684210526315264, 0.7039473684210526550, 0.7105263157894736725, 0.7171052631578946901, 0.7236842105263158187, 0.7302631578947368363, 0.7368421052631578538, 0.7434210526315789824, 0.7500000000000000000, 0.7565789473684210176, 0.7631578947368421462, 0.7697368421052631637, 0.7763157894736841813, 0.7828947368421053099, 0.7894736842105263275, 0.7960526315789473450, 0.8026315789473684736, 0.8092105263157894912, 0.8157894736842105088, 0.8223684210526315264, 0.8289473684210526550, 0.8355263157894736725, 0.8421052631578946901, 0.8486842105263158187, 0.8552631578947368363, 0.8618421052631578538, 0.8684210526315789824, 0.8750000000000000000, 0.8815789473684210176, 0.8881578947368421462, 0.8947368421052631637, 0.9013157894736841813, 0.9078947368421053099, 0.9144736842105263275, 0.9210526315789473450, 0.9276315789473684736, 0.9342105263157894912, 0.9407894736842105088, 0.9473684210526315264, 0.9539473684210526550, 0.9605263157894736725, 0.9671052631578946901, 0.9736842105263158187, 0.9802631578947368363, 0.9868421052631578538, 0.9934210526315789824, 0.9940576599040155115 ),
 .UNSPECIFIED. ) 
 CURVE ( )  GEOMETRIC_REPRESENTATION_ITEM ( )  RATIONAL_B_SPLINE_CURVE ( ( 1.000000000000000000, 0.9238795325112867385, 1.000000000000000000, 0.9238795325112867385, 1.000000000000000000, 0.9238795325112867385, 1.000000000000000000, 0.9238795325112867385, 1.000000000000000000, 0.9238795325112867385, 1.000000000000000000, 0.9238795325112867385, 1.000000000000000000, 0.9238795325112867385, 1.000000000000000000, 0.9238795325112867385, 1.000000000000000000, 0.9238795325112867385, 1.000000000000000000, 0.9238795325112867385, 1.000000000000000000, 0.9238795325112867385, 1.000000000000000000, 0.9238795325112867385, 1.000000000000000000, 0.9238795325112867385, 1.000000000000000000, 0.9238795325112867385, 1.000000000000000000, 0.9238795325112867385, 1.000000000000000000, 0.9238795325112867385, 1.000000000000000000, 0.9238795325112867385, 1.000000000000000000, 0.9238795325112867385, 1.000000000000000000, 0.9238795325112867385, 1.000000000000000000, 0.9238795325112867385, 1.000000000000000000, 0.9238795325112867385, 1.000000000000000000, 0.9238795325112867385, 1.000000000000000000, 0.9238795325112867385, 1.000000000000000000, 0.9238795325112867385, 1.000000000000000000, 0.9238795325112867385, 1.000000000000000000, 0.9238795325112867385, 1.000000000000000000, 0.9238795325112867385, 1.000000000000000000, 0.9238795325112867385, 1.000000000000000000, 0.9238795325112867385, 1.000000000000000000, 0.9238795325112867385, 1.000000000000000000, 0.9238795325112867385, 1.000000000000000000, 0.9238795325112867385, 1.000000000000000000, 0.9238795325112867385, 1.000000000000000000, 0.9238795325112867385, 1.000000000000000000, 0.9238795325112867385, 1.000000000000000000, 0.9238795325112867385, 1.000000000000000000, 0.9238795325112867385, 1.000000000000000000, 0.9238795325112867385, 1.000000000000000000, 0.9238795325112867385, 1.000000000000000000, 0.9238795325112867385, 1.000000000000000000, 0.9238795325112867385, 1.000000000000000000, 0.9238795325112867385, 1.000000000000000000, 0.9238795325112867385, 1.000000000000000000, 0.9238795325112867385, 1.000000000000000000, 0.9238795325112867385, 1.000000000000000000, 0.9238795325112867385, 1.000000000000000000, 0.9238795325112867385, 1.000000000000000000, 0.9238795325112867385, 1.000000000000000000, 0.9238795325112867385, 1.000000000000000000, 0.9238795325112867385, 1.000000000000000000, 0.9238795325112867385, 1.000000000000000000, 0.9238795325112867385, 1.000000000000000000, 0.9238795325112867385, 1.000000000000000000, 0.9238795325112867385, 1.000000000000000000, 0.9238795325112867385, 1.000000000000000000, 0.9238795325112867385, 1.000000000000000000, 0.9238795325112867385, 1.000000000000000000, 0.9238795325112867385, 1.000000000000000000, 0.9238795325112867385, 1.000000000000000000, 0.9238795325112867385, 1.000000000000000000, 0.9238795325112867385, 1.000000000000000000, 0.9238795325112867385, 1.000000000000000000, 0.9238795325112867385, 1.000000000000000000, 0.9238795325112867385, 1.000000000000000000, 0.9238795325112867385, 1.000000000000000000, 0.9238795325112867385, 1.000000000000000000, 0.9238795325112867385, 1.000000000000000000, 0.9238795325112867385, 1.000000000000000000, 0.9238795325112867385, 1.000000000000000000, 0.9238795325112867385, 1.000000000000000000, 0.9238795325112867385, 1.000000000000000000, 0.9238795325112867385, 1.000000000000000000, 0.9238795325112867385, 1.000000000000000000, 0.9238795325112867385, 1.000000000000000000, 0.9238795325112867385, 1.000000000000000000, 0.9238795325112867385, 1.000000000000000000, 0.9238795325112867385, 1.000000000000000000, 0.9238795325112867385, 1.000000000000000000, 0.9238795325112867385, 1.000000000000000000, 0.9238795325112867385, 1.000000000000000000, 0.9238795325112867385, 1.000000000000000000, 0.9238795325112867385, 1.000000000000000000, 0.9238795325112867385, 1.000000000000000000, 0.9238795325112867385, 1.000000000000000000, 0.9238795325112867385, 1.000000000000000000, 0.9238795325112867385, 1.000000000000000000, 0.9238795325112867385, 1.000000000000000000, 0.9238795325112867385, 1.000000000000000000, 0.9238795325112867385, 1.000000000000000000, 0.9238795325112867385, 1.000000000000000000, 0.9238795325112867385, 1.000000000000000000, 0.9238795325112867385, 1.000000000000000000, 0.9238795325112867385, 1.000000000000000000, 0.9238795325112867385, 1.000000000000000000, 0.9238795325112867385, 1.000000000000000000, 0.9238795325112867385, 1.000000000000000000, 0.9238795325112867385, 1.000000000000000000, 0.9238795325112867385, 1.000000000000000000, 0.9238795325112867385, 1.000000000000000000, 0.9238795325112867385, 1.000000000000000000, 0.9238795325112867385, 1.000000000000000000, 0.9238795325112867385, 1.000000000000000000, 0.9238795325112867385, 1.000000000000000000, 0.9238795325112867385, 1.000000000000000000, 0.9238795325112867385, 1.000000000000000000, 0.9238795325112867385, 1.000000000000000000, 0.9238795325112867385, 1.000000000000000000, 0.9238795325112867385, 1.000000000000000000, 0.9238795325112867385, 1.000000000000000000, 0.9238795325112867385, 1.000000000000000000, 0.9238795325112867385, 1.000000000000000000, 0.9238795325112867385, 1.000000000000000000, 0.9238795325112867385, 1.000000000000000000, 0.9238795325112867385, 1.000000000000000000, 0.9238795325112867385, 1.000000000000000000, 0.9238795325112867385, 1.000000000000000000, 0.9238795325112867385, 1.000000000000000000, 0.9238795325112867385, 1.000000000000000000, 0.9238795325112867385, 1.000000000000000000, 0.9238795325112867385, 1.000000000000000000, 0.9238795325112867385, 1.000000000000000000, 0.9238795325112867385, 1.000000000000000000, 0.9238795325112867385, 1.000000000000000000, 0.9238795325112867385, 1.000000000000000000, 0.9238795325112867385, 1.000000000000000000, 0.9238795325112867385, 1.000000000000000000, 0.9238795325112867385, 1.000000000000000000, 0.9238795325112867385, 1.000000000000000000, 0.9238795325112867385, 1.000000000000000000, 0.9238795325112867385, 1.000000000000000000, 0.9238795325112867385, 1.000000000000000000, 0.9238795325112867385, 1.000000000000000000, 0.9238795325112867385, 1.000000000000000000, 0.9238795325112867385, 1.000000000000000000, 0.9238795325112867385, 1.000000000000000000, 0.9238795325112867385, 1.000000000000000000, 0.9238795325112867385, 1.000000000000000000, 0.9238795325112867385, 1.000000000000000000, 0.9238795325112867385, 1.000000000000000000, 0.9238795325112867385, 1.000000000000000000, 0.9238795325112867385, 1.000000000000000000, 0.9238795325112867385, 1.000000000000000000, 0.9238795325112867385, 1.000000000000000000, 0.9238795325112867385, 1.000000000000000000, 0.9238795325112867385, 1.000000000000000000, 0.9238795325112867385, 1.000000000000000000, 0.9238795325112867385, 1.000000000000000000, 0.9238795325112867385, 1.000000000000000000, 0.9238795325112867385, 1.000000000000000000, 0.9238795325112867385, 1.000000000000000000, 0.9238795325112867385, 1.000000000000000000, 0.9926342558359432244, 0.9866939939076171395 ) ) 
 REPRESENTATION_ITEM ( '' )  );
#45017=CARTESIAN_POINT ( 'NONE',  ( 7.188101187499992051, 8.802885111219154394E-16, 21.73655278187175455 ) ) ;
#45018=ORIENTED_EDGE ( 'NONE', *, *, #42354, .T. ) ;
#45032=CARTESIAN_POINT ( 'NONE',  ( 3.313708498984756279, 7.999999999999991118, 7.861552779823362869 ) ) ;
#45039=DIRECTION ( 'NONE',  ( 0.000000000000000000, 0.000000000000000000, -1.000000000000000000 ) ) ;
#45040=CARTESIAN_POINT ( 'NONE',  ( 5.082755093536320601, -5.082755093536318824, 14.42405278187175455 ) ) ;
#45056=CARTESIAN_POINT ( 'NONE',  ( -5.656854249492375253, 5.656854249492375253, 5.142802779823363757 ) ) ;
#45061=CARTESIAN_POINT ( 'NONE',  ( -5.656854249492375253, 5.656854249492375253, 11.14280277982336642 ) ) ;
#45083=CARTESIAN_POINT ( 'NONE',  ( -8.008118988124991233, 0.000000000000000000, 20.51311528394062833 ) ) ;
#45087=CARTESIAN_POINT ( 'NONE',  ( 7.347880794884074377E-16, 114.5200769752660932, 47.89721922513225394 ) ) ;
#45110=CARTESIAN_POINT ( 'NONE',  ( 7.999999999999950262, -3.313708498984798467, 2.986552779823360204 ) ) ;
#45116=CARTESIAN_POINT ( 'NONE',  ( -5.082755093536317936, -5.082755093536320601, 26.04905278187175810 ) ) ;
#45127=CARTESIAN_POINT ( 'NONE',  ( 7.999999999999992895, -7.224685084787812073E-14, 27.26780278391845513 ) ) ;
#45140=CARTESIAN_POINT ( 'NONE',  ( 7.999999999999991118, 3.313708498984757611, 21.17405277982336642 ) ) ;
#45157=CARTESIAN_POINT ( 'NONE',  ( 5.656854249492374365, 5.656854249492375253, 22.76780277982336642 ) ) ;
#45159=CARTESIAN_POINT ( 'NONE',  ( 7.999999999999992895, -3.313708498984756279, 12.17405278392014800 ) ) ;
#45174=CARTESIAN_POINT ( 'NONE',  ( -7.999999999999992895, 4.898587196589407898E-16, 0.000000000000000000 ) ) ;
#45183=MECHANICAL_DESIGN_GEOMETRIC_PRESENTATION_REPRESENTATION('',(#54824),#62027);
#45192=EDGE_LOOP ( 'NONE', ( #32024, #33332, #40819, #43433 ) ) ;
#45205=CARTESIAN_POINT ( 'NONE',  ( 2.977408999572646486, 7.188101187499991163, 13.01780278187175277 ) ) ;
#45232=CARTESIAN_POINT ( 'NONE',  ( -2.977408999572648707, -7.188101187499990274, 18.64280278187175810 ) ) ;
#45237=CARTESIAN_POINT ( 'NONE',  ( -7.999999999999991118, 1.505321450683924536E-05, 7.017802358041144828 ) ) ;
#45246=CARTESIAN_POINT ( 'NONE',  ( -4.898587196589407898E-16, 7.999999999999991118, 1.955302779823364645 ) ) ;
#45247=CARTESIAN_POINT ( 'NONE',  ( 5.656854249492376141, -5.656854249492374365, 4.580302783920145338 ) ) ;
#45262=CARTESIAN_POINT ( 'NONE',  ( 5.656854249492374365, 5.656854249492375253, 6.324052784329821542 ) ) ;
#45285=CARTESIAN_POINT ( 'NONE',  ( 5.656854249492374365, 5.656854249492375253, 9.455302783920146226 ) ) ;
#45302=CARTESIAN_POINT ( 'NONE',  ( -5.082755093536319713, 5.082755093536319713, 4.674052781871752771 ) ) ;
#45331=CARTESIAN_POINT ( 'NONE',  ( -3.313708498984757167, 7.999999999999991118, 18.54905277982336287 ) ) ;
#45343=CARTESIAN_POINT ( 'NONE',  ( -7.999999999999991118, 3.313708498984756723, 21.79280278432983309 ) ) ;
#45363=FACE_BOUND ( 'NONE', #65953, .T. ) ;
#45375=CARTESIAN_POINT ( 'NONE',  ( -2.977408999572648707, -7.188101187499990274, 16.76780278187175099 ) ) ;
#45387=AXIS2_PLACEMENT_3D ( 'NONE', #33601, #68283, #56609 ) ;
#45388=CARTESIAN_POINT ( 'NONE',  ( -4.898587196589407898E-16, 7.999999999999991118, 7.955302779823362869 ) ) ;
#45395=CARTESIAN_POINT ( 'NONE',  ( -2.977408999572647819, 7.188101187499992051, 19.58030278187175455 ) ) ;
#45414=CARTESIAN_POINT ( 'NONE',  ( 1.469576158976822172E-15, -7.999999999999991118, 2.705302779823365533 ) ) ;
#45418=EDGE_CURVE ( 'NONE', #55503, #18628, #35003, .T. ) ;
#45419=( BOUNDED_CURVE ( )  B_SPLINE_CURVE ( 2, ( #61534, #50576, #74333, #73593, #16604, #67570, #9857, #44184, #21901 ),
 .UNSPECIFIED., .F., .F. ) 
 B_SPLINE_CURVE_WITH_KNOTS ( ( 3, 2, 2, 2, 3 ),
 ( 0.3157894736842105643, 0.3223684210526316374, 0.3289473684210526550, 0.3355263157894736725, 0.3421052631578947456 ),
 .UNSPECIFIED. ) 
 CURVE ( )  GEOMETRIC_REPRESENTATION_ITEM ( )  RATIONAL_B_SPLINE_CURVE ( ( 0.9999999999999993339, 0.9238795325112874046, 1.000000000000000000, 0.9238795325112867385, 1.000000000000000000, 0.9238795325112867385, 1.000000000000000000, 0.9238795325112867385, 1.000000000000000000 ) ) 
 REPRESENTATION_ITEM ( '' )  );
#45445=CARTESIAN_POINT ( 'NONE',  ( 1.471067592899761672E-15, -8.008118988124991233, 22.38811528394063188 ) ) ;
#45453=EDGE_CURVE ( 'NONE', #2593, #69617, #38491, .T. ) ;
#45463=CARTESIAN_POINT ( 'NONE',  ( -7.999999999999991118, 0.000000000000000000, 8.517802783920146226 ) ) ;
#45467=CARTESIAN_POINT ( 'NONE',  ( -7.999999999999991118, -1.288204405367768053E-10, 8.517802783929960597 ) ) ;
#45477=CARTESIAN_POINT ( 'NONE',  ( 7.188101187499991163, 2.977408999572648707, 22.20530278187175810 ) ) ;
#45503=CARTESIAN_POINT ( 'NONE',  ( -4.898587196589407898E-16, 7.999999999999991118, 18.45530277982336642 ) ) ;
#45523=CARTESIAN_POINT ( 'NONE',  ( 5.656854249492374365, 5.656854249492375253, 12.45530278392014623 ) ) ;
#45575=CARTESIAN_POINT ( 'NONE',  ( 1.320432766682872962E-15, -7.188101187499992051, 10.86155278187175455 ) ) ;
#45599=CARTESIAN_POINT ( 'NONE',  ( 7.188101187499991163, 2.977408999572648707, 11.70530278187175455 ) ) ;
#45602=CARTESIAN_POINT ( 'NONE',  ( -7.999985420792424584, -3.313723078192327698, 1.111553367238835799 ) ) ;
#45603=CARTESIAN_POINT ( 'NONE',  ( 3.313708498984762496, -7.999999999999989342, 1.355302784329824206 ) ) ;
#45614=CARTESIAN_POINT ( 'NONE',  ( -3.313708498984757167, 7.999999999999991118, 3.549052779823362425 ) ) ;
#45620=CARTESIAN_POINT ( 'NONE',  ( -7.999999999999991118, 0.000000000000000000, 17.33030277982336287 ) ) ;
#45631=CARTESIAN_POINT ( 'NONE',  ( -3.313708498984757167, 7.999999999999991118, 6.605302784329821542 ) ) ;
#45632=CARTESIAN_POINT ( 'NONE',  ( 7.999999999999991118, 3.313708498984758055, 4.674052779823363757 ) ) ;
#45636=CARTESIAN_POINT ( 'NONE',  ( -5.082755093536317936, -5.082755093536320601, 27.17405278187175455 ) ) ;
#45638=( BOUNDED_CURVE ( )  B_SPLINE_CURVE ( 2, ( #61104, #61482, #56951, #9807, #15816, #50160, #10175, #32451, #72426, #49405, #27891 ),
 .UNSPECIFIED., .F., .F. ) 
 B_SPLINE_CURVE_WITH_KNOTS ( ( 3, 2, 2, 2, 2, 3 ),
 ( 0.2117847674899544508, 0.2117848187026179774, 0.2184030942870707759, 0.2250213698715235744, 0.2316396454559763729, 0.2382579061490637251 ),
 .UNSPECIFIED. ) 
 CURVE ( )  GEOMETRIC_REPRESENTATION_ITEM ( )  RATIONAL_B_SPLINE_CURVE ( ( 0.9999988219584774463, 0.9999994109746808135, 1.000000000000000000, 0.9238795325112867385, 1.000000000000000000, 0.9238795325112867385, 1.000000000000000000, 0.9238795325112867385, 1.000000000000000000, 0.9238797037851605998, 0.9999996574530229942 ) ) 
 REPRESENTATION_ITEM ( '' )  );
#45658=CARTESIAN_POINT ( 'NONE',  ( -4.401442555609577197E-16, 7.188101187499992051, 1.111552781871753215 ) ) ;
#45672=CARTESIAN_POINT ( 'NONE',  ( -7.188101187499991163, 2.977408999572646930, 3.267802781871751439 ) ) ;
#45681=CARTESIAN_POINT ( 'NONE',  ( -2.977408999572647819, 7.188101187499991163, 25.58030278187175810 ) ) ;
#45700=CARTESIAN_POINT ( 'NONE',  ( 1.469576158976822172E-15, -7.999999999999991118, 20.70530277982336642 ) ) ;
#45714=CARTESIAN_POINT ( 'NONE',  ( 7.999999999999991118, 9.797174393178815797E-16, 22.63655278432982243 ) ) ;
#45732=DIRECTION ( 'NONE',  ( 0.000000000000000000, -1.000000000000000000, 0.000000000000000000 ) ) ;
#45741=FACE_OUTER_BOUND ( 'NONE', #14203, .T. ) ;
#45749=CARTESIAN_POINT ( 'NONE',  ( 2.977408999572646486, 7.188101187499991163, 20.51780278187175455 ) ) ;
#45773=CARTESIAN_POINT ( 'NONE',  ( -5.082755093536319713, 5.082755093536319713, 19.67405278187175455 ) ) ;
#45794=CARTESIAN_POINT ( 'NONE',  ( -7.999999999999991118, 0.000000000000000000, 3.830302779823362869 ) ) ;
#45820=CARTESIAN_POINT ( 'NONE',  ( 1.471067592899761672E-15, -8.008118988124991233, 11.88811528394062833 ) ) ;
#45839=CARTESIAN_POINT ( 'NONE',  ( -5.656854249492373476, -5.656854249492376141, 5.705302783920146226 ) ) ;
#45842=CARTESIAN_POINT ( 'NONE',  ( -3.313708498984759387, -7.999999999999989342, 8.799052783920146226 ) ) ;
#45852=CARTESIAN_POINT ( 'NONE',  ( 5.082755093536318824, 5.082755093536319713, 16.29905278187175455 ) ) ;
#45874=CARTESIAN_POINT ( 'NONE',  ( -1.646455035084469998, -7.866828006418148611, 0.000000000000000000 ) ) ;
#45881=CARTESIAN_POINT ( 'NONE',  ( -7.999999999999989342, -3.313708498984762496, 21.92405277982336642 ) ) ;
#45899=CARTESIAN_POINT ( 'NONE',  ( 7.999999999999991118, 3.313708498984757611, 15.36155278392014623 ) ) ;
#45904=CARTESIAN_POINT ( 'NONE',  ( 7.999999999999991118, 0.000000000000000000, 30.00000000000000000 ) ) ;
#45914=CARTESIAN_POINT ( 'NONE',  ( -7.999999999998400391, 3.416934844025491914E-06, 16.01767659775488184 ) ) ;
#45917=DIRECTION ( 'NONE',  ( -0.000000000000000000, -0.000000000000000000, 1.000000000000000000 ) ) ;
#45926=ORIENTED_EDGE ( 'NONE', *, *, #27952, .F. ) ;
#45930=CARTESIAN_POINT ( 'NONE',  ( 3.313708498984762496, -7.999999999999989342, 19.29905277982336642 ) ) ;
#45947=ORIENTED_EDGE ( 'NONE', *, *, #58389, .F. ) ;
#45949=CARTESIAN_POINT ( 'NONE',  ( 2.977408999572646486, 7.188101187499991163, 5.517802781871753659 ) ) ;
#45974=CARTESIAN_POINT ( 'NONE',  ( -7.188101187499992051, 0.000000000000000000, 7.861552781871751883 ) ) ;
#45977=CARTESIAN_POINT ( 'NONE',  ( 7.999999999999991118, 3.313708498984757611, 3.230302784329822430 ) ) ;
#45987=CARTESIAN_POINT ( 'NONE',  ( 3.313708498984762496, -7.999999999999989342, 5.799052779823364645 ) ) ;
#46003=CARTESIAN_POINT ( 'NONE',  ( -7.999999999999991118, 3.313708498984756723, 8.292802784329824206 ) ) ;
#46022=CARTESIAN_POINT ( 'NONE',  ( -3.313708498984758943, -7.999999999999989342, 20.79905278392014978 ) ) ;
#46032=CARTESIAN_POINT ( 'NONE',  ( 2.977408999572646486, 7.188101187499991163, 28.01780278187175455 ) ) ;
#46045=CARTESIAN_POINT ( 'NONE',  ( -7.188101187499992051, 0.000000000000000000, 6.361552781871754547 ) ) ;
#46072=CARTESIAN_POINT ( 'NONE',  ( 1.469576158976822172E-15, -7.999999999999991118, 19.20530277982336642 ) ) ;
#46080=ORIENTED_EDGE ( 'NONE', *, *, #19126, .F. ) ;
#46086=CARTESIAN_POINT ( 'NONE',  ( -5.656854249492373476, -5.656854249492376141, 23.57405278432982598 ) ) ;
#46101=ORIENTED_EDGE ( 'NONE', *, *, #16261, .F. ) ;
#46121=CARTESIAN_POINT ( 'NONE',  ( -4.401442555609577197E-16, 7.188101187499992051, 19.11155278187175455 ) ) ;
#46144=CARTESIAN_POINT ( 'NONE',  ( 5.082755093536320601, -5.082755093536318824, 17.42405278187175810 ) ) ;
#46164=CARTESIAN_POINT ( 'NONE',  ( 3.313708498984762496, -7.999999999999989342, 4.299052779823363757 ) ) ;
#46191=CARTESIAN_POINT ( 'NONE',  ( 5.662595241051936235, -5.662595241051934458, 15.07561528394063011 ) ) ;
#46194=EDGE_CURVE ( 'NONE', #31087, #8699, #32757, .T. ) ;
#46199=CARTESIAN_POINT ( 'NONE',  ( -5.082755093536319713, 5.082755093536319713, 17.79905278187175455 ) ) ;
#46210=EDGE_CURVE ( 'NONE', #18628, #52951, #17109, .T. ) ;
#46214=CARTESIAN_POINT ( 'NONE',  ( 7.999999999999991118, 9.797174393178815797E-16, 10.76780278392014800 ) ) ;
#46228=CARTESIAN_POINT ( 'NONE',  ( 1.320432766682872962E-15, -7.188101187499992051, 20.23655278187175455 ) ) ;
#46244=CARTESIAN_POINT ( 'NONE',  ( -4.794452594515416166, -6.420665270977717221, -0.000000000000000000 ) ) ;
#46251=CARTESIAN_POINT ( 'NONE',  ( -7.999999999999991118, 3.313708498984756723, 21.73655277982336287 ) ) ;
#46268=CARTESIAN_POINT ( 'NONE',  ( 3.313708498984756279, 7.999999999999991118, 22.86155277982336997 ) ) ;
#46270=CARTESIAN_POINT ( 'NONE',  ( 1.469576158976822172E-15, -7.999999999999991118, 5.892802783920146226 ) ) ;
#46285=VECTOR ( 'NONE', #64258, 1000.000000000000000 ) ;
#46303=CARTESIAN_POINT ( 'NONE',  ( -7.999999999961189268, -1.665725685002260109E-05, 4.018425631117963803 ) ) ;
#46306=( BOUNDED_CURVE ( )  B_SPLINE_CURVE ( 2, ( #24102, #47113, #28657, #11680, #35450, #16, #52791, #34717, #39986, #64108, #63730, #11315, #5658, #6029, #45636, #63355, #69400, #17708, #52423, #29776, #22618, #1126, #40723, #17333, #7140, #34349, #70149, #23003, #41469, #18457, #12052, #758, #64483, #68651, #35815, #12780, #57346, #58830, #69029, #40353, #57723, #35085, #30148, #29034, #388, #23370, #58096, #65952, #8991, #36181, #32006, #31629, #47485, #37293, #14257, #1498, #36918, #7509, #42929, #19186, #42189, #54650, #60288, #66325, #65203, #13510, #25946, #54277, #36549, #59200, #53534, #13145, #42566, #7877, #8240, #19550, #2213, #64843, #48592, #30514, #1850, #8614, #2959, #48963, #71600, #59926, #65579, #25207, #24836, #47853, #70874, #14630, #71975, #20289, #59560, #71230, #19921, #30881, #53900, #24479, #43309, #37670, #48222, #60669, #13874, #70508, #25577, #31251, #2589, #18827, #41831, #50094, #33512, #39154, #46199, #44069, #72741, #4831, #33149, #21045, #15004, #27444, #20670, #43689, #15748, #16116, #44812, #67823, #38415, #56143, #66701, #50460, #62156, #10480, #21783, #73475, #38789, #73109, #55772, #32384, #55398, #21417, #49342, #44441, #69215, #26707, #49726, #67452, #67079, #4452, #56515, #28846, #51869, #4088, #210, #9364, #23188, #17526, #27082, #61792, #3708, #9742, #10110, #15378, #40543, #61416, #63548, #11873, #55025, #3332, #26321, #72359, #38041, #61040, #32764, #71047, #46937, #47306, #65019, #35274, #52242, #13330, #69965, #29229, #30332, #1312, #576, #17903, #18273, #57917, #946, #58647, #6954, #18646, #36002, #34909, #47666, #24295, #36366, #12605, #2032, #59019, #63927, #53718, #7328, #70331, #12964, #41654, #6226, #48038, #53351, #65397, #64664, #12237, #58287, #40916, #35632, #29965, #24656, #41288, #6590, #1676, #70688, #23558, #19006, #52978, #42012, #64298, #29597, #46569, #59382, #19367, #23928, #7693, #52610, #30700, #25018, #42380, #69590, #31819, #14443, #43877, #38228, #54840, #8059, #3149, #26894, #60107, #8425, #26135, #31442, #66506, #26509, #61234, #66893, #37478, #72554, #42749, #20859, #37859, #60478, #49535, #43495, #43120, #49154, #54468, #49910, #2775, #72164, #3901, #20475, #14817, #15199, #13694, #9562, #60856, #32577, #72924, #25761, #9176, #55586, #3520, #65765, #21234, #48782, #31060, #32195, #55215, #54088, #71416, #71789, #36736, #20108, #8808, #44260, #59747, #2398, #25396, #48410, #19740, #14068, #37104, #66139, #68378, #21602 ),
 .UNSPECIFIED., .F., .F. ) 
 B_SPLINE_CURVE_WITH_KNOTS ( ( 3, 2, 2, 2, 2, 2, 2, 2, 2, 2, 2, 2, 2, 2, 2, 2, 2, 2, 2, 2, 2, 2, 2, 2, 2, 2, 2, 2, 2, 2, 2, 2, 2, 2, 2, 2, 2, 2, 2, 2, 2, 2, 2, 2, 2, 2, 2, 2, 2, 2, 2, 2, 2, 2, 2, 2, 2, 2, 2, 2, 2, 2, 2, 2, 2, 2, 2, 2, 2, 2, 2, 2, 2, 2, 2, 2, 2, 2, 2, 2, 2, 2, 2, 2, 2, 2, 2, 2, 2, 2, 2, 2, 2, 2, 2, 2, 2, 2, 2, 2, 2, 2, 2, 2, 2, 2, 2, 2, 2, 2, 2, 2, 2, 2, 2, 2, 2, 2, 2, 2, 2, 2, 2, 2, 2, 2, 2, 2, 2, 2, 2, 2, 2, 2, 2, 2, 2, 2, 2, 2, 2, 2, 2, 2, 2, 2, 2, 2, 2, 2, 2, 2, 3 ),
 ( 0.000000000000000000, 0.006578947368421052266, 0.01315789473684210453, 0.01973684210526315680, 0.02631578947368420907, 0.03289473684210526133, 0.03947368421052631360, 0.04605263157894736586, 0.05263157894736841813, 0.05921052631578947040, 0.06578947368421052266, 0.07236842105263158187, 0.07894736842105262720, 0.08552631578947368640, 0.09210526315789473173, 0.09868421052631579093, 0.1052631578947368363, 0.1118421052631578955, 0.1184210526315789408, 0.1250000000000000000, 0.1315789473684210453, 0.1381578947368421184, 0.1447368421052631637, 0.1513157894736842091, 0.1578947368421052544, 0.1644736842105263275, 0.1710526315789473728, 0.1776315789473684181, 0.1842105263157894635, 0.1907894736842105365, 0.1973684210526315819, 0.2039473684210526272, 0.2105263157894736725, 0.2171052631578947456, 0.2236842105263157909, 0.2302631578947368363, 0.2368421052631578816, 0.2434210526315789547, 0.2500000000000000000, 0.2565789473684210731, 0.2631578947368420907, 0.2697368421052631637, 0.2763157894736842368, 0.2828947368421052544, 0.2894736842105263275, 0.2960526315789473450, 0.3026315789473684181, 0.3092105263157894912, 0.3157894736842105088, 0.3223684210526315819, 0.3289473684210526550, 0.3355263157894736725, 0.3421052631578947456, 0.3486842105263157632, 0.3552631578947368363, 0.3618421052631579093, 0.3684210526315789269, 0.3750000000000000000, 0.3815789473684210731, 0.3881578947368420907, 0.3947368421052631637, 0.4013157894736842368, 0.4078947368421052544, 0.4144736842105263275, 0.4210526315789473450, 0.4276315789473684181, 0.4342105263157894912, 0.4407894736842105088, 0.4473684210526315819, 0.4539473684210526550, 0.4605263157894736725, 0.4671052631578947456, 0.4736842105263157632, 0.4802631578947368363, 0.4868421052631579093, 0.4934210526315789269, 0.5000000000000000000, 0.5065789473684210176, 0.5131578947368421462, 0.5197368421052631637, 0.5263157894736841813, 0.5328947368421053099, 0.5394736842105263275, 0.5460526315789473450, 0.5526315789473684736, 0.5592105263157894912, 0.5657894736842105088, 0.5723684210526315264, 0.5789473684210526550, 0.5855263157894736725, 0.5921052631578946901, 0.5986842105263158187, 0.6052631578947368363, 0.6118421052631578538, 0.6184210526315789824, 0.6250000000000001110, 0.6315789473684210176, 0.6381578947368421462, 0.6447368421052631637, 0.6513157894736841813, 0.6578947368421053099, 0.6644736842105263275, 0.6710526315789473450, 0.6776315789473684736, 0.6842105263157894912, 0.6907894736842105088, 0.6973684210526315264, 0.7039473684210526550, 0.7105263157894736725, 0.7171052631578946901, 0.7236842105263158187, 0.7302631578947368363, 0.7368421052631578538, 0.7434210526315789824, 0.7500000000000000000, 0.7565789473684210176, 0.7631578947368421462, 0.7697368421052631637, 0.7763157894736841813, 0.7828947368421053099, 0.7894736842105263275, 0.7960526315789473450, 0.8026315789473684736, 0.8092105263157894912, 0.8157894736842105088, 0.8223684210526315264, 0.8289473684210526550, 0.8355263157894736725, 0.8421052631578946901, 0.8486842105263158187, 0.8552631578947368363, 0.8618421052631578538, 0.8684210526315789824, 0.8749999999999998890, 0.8815789473684210176, 0.8881578947368421462, 0.8947368421052631637, 0.9013157894736841813, 0.9078947368421053099, 0.9144736842105263275, 0.9210526315789473450, 0.9276315789473684736, 0.9342105263157894912, 0.9407894736842105088, 0.9473684210526315264, 0.9539473684210526550, 0.9605263157894736725, 0.9671052631578946901, 0.9736842105263158187, 0.9802631578947368363, 0.9868421052631578538, 0.9934210526315789824, 0.9940576549107595916 ),
 .UNSPECIFIED. ) 
 CURVE ( )  GEOMETRIC_REPRESENTATION_ITEM ( )  RATIONAL_B_SPLINE_CURVE ( ( 1.000000000000000000, 0.9238795325112867385, 1.000000000000000000, 0.9238795325112867385, 1.000000000000000000, 0.9238795325112867385, 1.000000000000000000, 0.9238795325112867385, 1.000000000000000000, 0.9238795325112867385, 1.000000000000000000, 0.9238795325112867385, 1.000000000000000000, 0.9238795325112867385, 1.000000000000000000, 0.9238795325112867385, 1.000000000000000000, 0.9238795325112867385, 1.000000000000000000, 0.9238795325112867385, 1.000000000000000000, 0.9238795325112867385, 1.000000000000000000, 0.9238795325112867385, 1.000000000000000000, 0.9238795325112867385, 1.000000000000000000, 0.9238795325112867385, 1.000000000000000000, 0.9238795325112867385, 1.000000000000000000, 0.9238795325112867385, 1.000000000000000000, 0.9238795325112867385, 1.000000000000000000, 0.9238795325112867385, 1.000000000000000000, 0.9238795325112867385, 1.000000000000000000, 0.9238795325112867385, 1.000000000000000000, 0.9238795325112867385, 1.000000000000000000, 0.9238795325112867385, 1.000000000000000000, 0.9238795325112867385, 1.000000000000000000, 0.9238795325112867385, 1.000000000000000000, 0.9238795325112867385, 1.000000000000000000, 0.9238795325112867385, 1.000000000000000000, 0.9238795325112867385, 1.000000000000000000, 0.9238795325112867385, 1.000000000000000000, 0.9238795325112867385, 1.000000000000000000, 0.9238795325112867385, 1.000000000000000000, 0.9238795325112867385, 1.000000000000000000, 0.9238795325112867385, 1.000000000000000000, 0.9238795325112867385, 1.000000000000000000, 0.9238795325112867385, 1.000000000000000000, 0.9238795325112867385, 1.000000000000000000, 0.9238795325112867385, 1.000000000000000000, 0.9238795325112867385, 1.000000000000000000, 0.9238795325112867385, 1.000000000000000000, 0.9238795325112867385, 1.000000000000000000, 0.9238795325112867385, 1.000000000000000000, 0.9238795325112867385, 1.000000000000000000, 0.9238795325112867385, 1.000000000000000000, 0.9238795325112867385, 1.000000000000000000, 0.9238795325112867385, 1.000000000000000000, 0.9238795325112867385, 1.000000000000000000, 0.9238795325112867385, 1.000000000000000000, 0.9238795325112867385, 1.000000000000000000, 0.9238795325112867385, 1.000000000000000000, 0.9238795325112867385, 1.000000000000000000, 0.9238795325112867385, 1.000000000000000000, 0.9238795325112867385, 1.000000000000000000, 0.9238795325112867385, 1.000000000000000000, 0.9238795325112867385, 1.000000000000000000, 0.9238795325112867385, 1.000000000000000000, 0.9238795325112867385, 1.000000000000000000, 0.9238795325112867385, 1.000000000000000000, 0.9238795325112867385, 1.000000000000000000, 0.9238795325112867385, 1.000000000000000000, 0.9238795325112867385, 1.000000000000000000, 0.9238795325112867385, 1.000000000000000000, 0.9238795325112867385, 1.000000000000000000, 0.9238795325112867385, 1.000000000000000000, 0.9238795325112867385, 1.000000000000000000, 0.9238795325112867385, 1.000000000000000000, 0.9238795325112867385, 1.000000000000000000, 0.9238795325112867385, 1.000000000000000000, 0.9238795325112867385, 1.000000000000000000, 0.9238795325112867385, 1.000000000000000000, 0.9238795325112867385, 1.000000000000000000, 0.9238795325112867385, 1.000000000000000000, 0.9238795325112867385, 1.000000000000000000, 0.9238795325112867385, 1.000000000000000000, 0.9238795325112867385, 1.000000000000000000, 0.9238795325112867385, 1.000000000000000000, 0.9238795325112867385, 1.000000000000000000, 0.9238795325112867385, 1.000000000000000000, 0.9238795325112867385, 1.000000000000000000, 0.9238795325112867385, 1.000000000000000000, 0.9238795325112867385, 1.000000000000000000, 0.9238795325112867385, 1.000000000000000000, 0.9238795325112867385, 1.000000000000000000, 0.9238795325112867385, 1.000000000000000000, 0.9238795325112867385, 1.000000000000000000, 0.9238795325112867385, 1.000000000000000000, 0.9238795325112867385, 1.000000000000000000, 0.9238795325112867385, 1.000000000000000000, 0.9238795325112867385, 1.000000000000000000, 0.9238795325112867385, 1.000000000000000000, 0.9238795325112867385, 1.000000000000000000, 0.9238795325112867385, 1.000000000000000000, 0.9238795325112867385, 1.000000000000000000, 0.9238795325112867385, 1.000000000000000000, 0.9238795325112867385, 1.000000000000000000, 0.9238795325112867385, 1.000000000000000000, 0.9238795325112867385, 1.000000000000000000, 0.9238795325112867385, 1.000000000000000000, 0.9238795325112867385, 1.000000000000000000, 0.9238795325112867385, 1.000000000000000000, 0.9238795325112867385, 1.000000000000000000, 0.9238795325112867385, 1.000000000000000000, 0.9238795325112867385, 1.000000000000000000, 0.9238795325112867385, 1.000000000000000000, 0.9238795325112867385, 1.000000000000000000, 0.9238795325112867385, 1.000000000000000000, 0.9238795325112867385, 1.000000000000000000, 0.9238795325112867385, 1.000000000000000000, 0.9238795325112867385, 1.000000000000000000, 0.9238795325112867385, 1.000000000000000000, 0.9238795325112867385, 1.000000000000000000, 0.9238795325112867385, 1.000000000000000000, 0.9238795325112867385, 1.000000000000000000, 0.9238795325112867385, 1.000000000000000000, 0.9238795325112867385, 1.000000000000000000, 0.9238795325112867385, 1.000000000000000000, 0.9238795325112867385, 1.000000000000000000, 0.9238795325112867385, 1.000000000000000000, 0.9238795325112867385, 1.000000000000000000, 0.9238795325112867385, 1.000000000000000000, 0.9238795325112867385, 1.000000000000000000, 0.9238795325112867385, 1.000000000000000000, 0.9238795325112867385, 1.000000000000000000, 0.9238795325112867385, 1.000000000000000000, 0.9238795325112867385, 1.000000000000000000, 0.9238795325112867385, 1.000000000000000000, 0.9238795325112867385, 1.000000000000000000, 0.9238795325112867385, 1.000000000000000000, 0.9238795325112867385, 1.000000000000000000, 0.9238795325112867385, 1.000000000000000000, 0.9238795325112867385, 1.000000000000000000, 0.9238795325112867385, 1.000000000000000000, 0.9238795325112867385, 1.000000000000000000, 0.9238795325112867385, 1.000000000000000000, 0.9238795325112867385, 1.000000000000000000, 0.9238795325112867385, 1.000000000000000000, 0.9238795325112867385, 1.000000000000000000, 0.9238795325112867385, 1.000000000000000000, 0.9238795325112867385, 1.000000000000000000, 0.9238795325112867385, 1.000000000000000000, 0.9238795325112867385, 1.000000000000000000, 0.9238795325112867385, 1.000000000000000000, 0.9238795325112867385, 1.000000000000000000, 0.9238795325112867385, 1.000000000000000000, 0.9238795325112867385, 1.000000000000000000, 0.9238795325112867385, 1.000000000000000000, 0.9238795325112867385, 1.000000000000000000, 0.9238795325112867385, 1.000000000000000000, 0.9238795325112867385, 1.000000000000000000, 0.9238795325112867385, 1.000000000000000000, 0.9238795325112867385, 1.000000000000000000, 0.9238795325112867385, 1.000000000000000000, 0.9238795325112867385, 1.000000000000000000, 0.9926343136094674113, 0.9866940870930933638 ) ) 
 REPRESENTATION_ITEM ( '' )  );
#46322=CARTESIAN_POINT ( 'NONE',  ( -7.188101187499991163, 2.977408999572646930, 4.392802781871752771 ) ) ;
#46345=CARTESIAN_POINT ( 'NONE',  ( -7.188101187499992051, 0.000000000000000000, 12.36155278187175277 ) ) ;
#46348=CARTESIAN_POINT ( 'NONE',  ( -3.313708498984758943, -7.999999999999989342, 2.667802784329821986 ) ) ;
#46350=CARTESIAN_POINT ( 'NONE',  ( 7.999999999999920064, -1.061780717098090627E-06, 7.767802753882760314 ) ) ;
#46359=CARTESIAN_POINT ( 'NONE',  ( -5.656854249492373476, -5.656854249492376141, 4.017802779823362869 ) ) ;
#46370=ORIENTED_EDGE ( 'NONE', *, *, #58389, .T. ) ;
#46376=CARTESIAN_POINT ( 'NONE',  ( 1.469576158976822172E-15, -7.999999999999991118, 7.261552784329822430 ) ) ;
#46380=EDGE_LOOP ( 'NONE', ( #32533, #66412, #35225, #7341 ) ) ;
#46394=CARTESIAN_POINT ( 'NONE',  ( 7.999999999999991118, 9.797174393178815797E-16, 21.26780278392014623 ) ) ;
#46405=CARTESIAN_POINT ( 'NONE',  ( -2.977408999572648707, -7.188101187499990274, 27.26780278187175099 ) ) ;
#46419=CARTESIAN_POINT ( 'NONE',  ( 2.977408999572650927, -7.188101187499990274, 2.330302781871754991 ) ) ;
#46424=CARTESIAN_POINT ( 'NONE',  ( -3.317071493978878571, 8.008118988124991233, 3.731865283940628775 ) ) ;
#46431=CARTESIAN_POINT ( 'NONE',  ( 7.188101187499991163, 2.977408999572648707, 25.20530278187175810 ) ) ;
#46447=CARTESIAN_POINT ( 'NONE',  ( 7.999999999999991118, 3.313708498984757611, 24.17405277982336642 ) ) ;
#46460=CARTESIAN_POINT ( 'NONE',  ( -7.999999999999991118, 3.313708498984756723, 26.29280278432983309 ) ) ;
#46470=EDGE_CURVE ( 'NONE', #60307, #39327, #29691, .T. ) ;
#46491=CARTESIAN_POINT ( 'NONE',  ( 7.188101187499991163, 2.977408999572648707, 15.83030278187175277 ) ) ;
#46517=CARTESIAN_POINT ( 'NONE',  ( 7.188101187499992051, 8.802885111219154394E-16, 13.11155278187175277 ) ) ;
#46521=CARTESIAN_POINT ( 'NONE',  ( -8.000000000000010658, -3.313708498984740736, 20.42405277982336642 ) ) ;
#46538=CARTESIAN_POINT ( 'NONE',  ( 3.313708498984762496, -7.999999999999989342, 2.799052779823366421 ) ) ;
#46563=CARTESIAN_POINT ( 'NONE',  ( -3.317071493978878571, 8.008118988124991233, 15.73186528394062833 ) ) ;
#46569=CARTESIAN_POINT ( 'NONE',  ( 2.977408999572646486, 7.188101187499992051, 7.017802781871750994 ) ) ;
#46581=CARTESIAN_POINT ( 'NONE',  ( -3.313708498984757167, 7.999999999999991118, 3.736552783920145338 ) ) ;
#46584=B_SPLINE_CURVE_WITH_KNOTS ( 'NONE', 1,
 ( #49900, #50637 ),
 .UNSPECIFIED., .F., .F.,
 ( 2, 2 ),
 ( 0.000000000000000000, 1.000000000000000000 ),
 .UNSPECIFIED. ) ;
#46596=CARTESIAN_POINT ( 'NONE',  ( -2.977408999572648707, -7.188101187499990274, 18.64280278187175810 ) ) ;
#46600=CARTESIAN_POINT ( 'NONE',  ( -7.999999999835898379, -3.436314075762838161E-05, 19.01908381112063751 ) ) ;
#46604=CARTESIAN_POINT ( 'NONE',  ( 5.656854249492376141, -5.656854249492374365, 4.392802779823363757 ) ) ;
#46617=CARTESIAN_POINT ( 'NONE',  ( -5.778038727434721800, -5.550035267211852030, 0.000000000000000000 ) ) ;
#46623=CARTESIAN_POINT ( 'NONE',  ( -7.999999999999989342, -3.313708498984762496, 18.92405277982336642 ) ) ;
#46630=CARTESIAN_POINT ( 'NONE',  ( -5.656854249492373476, -5.656854249492376141, 8.517802779823362869 ) ) ;
#46642=CARTESIAN_POINT ( 'NONE',  ( 1.469576158976822172E-15, -7.999999999999991118, 4.392802783920145338 ) ) ;
#46656=CARTESIAN_POINT ( 'NONE',  ( 0.000000000000000000, 0.000000000000000000, 30.00000000000000000 ) ) ;
#46678=CARTESIAN_POINT ( 'NONE',  ( -7.999999999999991118, 0.000000000000000000, 6.830302779823365533 ) ) ;
#46688=CARTESIAN_POINT ( 'NONE',  ( 7.188101187499992051, 8.802885111219154394E-16, 3.736552781871751883 ) ) ;
#46710=CARTESIAN_POINT ( 'NONE',  ( 5.082755093536320601, -5.082755093536318824, 12.92405278187175277 ) ) ;
#46713=CARTESIAN_POINT ( 'NONE',  ( -6.062585341144163031, -5.219679969245603957, -0.4430702215468678706 ) ) ;
#46714=VERTEX_POINT ( 'NONE', #69156 ) ;
#46724=CARTESIAN_POINT ( 'NONE',  ( -4.898587196589407898E-16, 7.999999999999991118, 27.64280278392014978 ) ) ;
#46757=CARTESIAN_POINT ( 'NONE',  ( -7.999999999999991118, 0.000000000000000000, 17.51780278392014623 ) ) ;
#46768=CARTESIAN_POINT ( 'NONE',  ( 1.320432766682872962E-15, -7.188101187499992051, 25.86155278187175810 ) ) ;
#46788=CARTESIAN_POINT ( 'NONE',  ( 1.471067592899761672E-15, -8.008118988124991233, 5.888115283940630995 ) ) ;
#46795=CARTESIAN_POINT ( 'NONE',  ( -7.188101187499990274, -2.977408999572651371, 27.45530278187175810 ) ) ;
#46812=CARTESIAN_POINT ( 'NONE',  ( 7.999999999999992895, -3.313708498984756279, 14.98655277982336642 ) ) ;
#46814=EDGE_CURVE ( 'NONE', #22615, #35470, #32561, .T. ) ;
#46828=CARTESIAN_POINT ( 'NONE',  ( 7.999999999999992895, -3.313708498984756279, 22.54280278432982954 ) ) ;
#46833=AXIS2_PLACEMENT_3D ( 'NONE', #25184, #37646, #20647 ) ;
#46855=ADVANCED_FACE ( 'NONE', ( #20606 ), #27020, .F. ) ;
#46863=CARTESIAN_POINT ( 'NONE',  ( 5.082755093536318824, 5.082755093536319713, 12.92405278187175277 ) ) ;
#46888=CARTESIAN_POINT ( 'NONE',  ( 7.188101187499992051, 8.802885111219154394E-16, 10.11155278187175455 ) ) ;
#46892=CARTESIAN_POINT ( 'NONE',  ( 3.313708498984762496, -7.999999999999989342, 20.79905277982336642 ) ) ;
#46901=CYLINDRICAL_SURFACE ( 'NONE', #4121, 7.999999999999991118 ) ;
#46932=CARTESIAN_POINT ( 'NONE',  ( -8.008118988124991233, 3.317071493978878127, 15.91936528394063011 ) ) ;
#46937=CARTESIAN_POINT ( 'NONE',  ( -7.188101187499992051, 0.000000000000000000, 11.98655278187175277 ) ) ;
#46945=ADVANCED_FACE ( 'NONE', ( #68872 ), #34939, .F. ) ;
#46950=CARTESIAN_POINT ( 'NONE',  ( -5.656854249492375253, 5.656854249492375253, 2.330302783920143561 ) ) ;
#46965=CARTESIAN_POINT ( 'NONE',  ( -2.977408999572647819, 7.188101187499991163, 19.58030278187175455 ) ) ;
#46968=DIRECTION ( 'NONE',  ( 1.000000000000000000, 0.000000000000000000, 0.000000000000000000 ) ) ;
#46973=CARTESIAN_POINT ( 'NONE',  ( -7.188101187499992051, 0.000000000000000000, 25.86155278187175810 ) ) ;
#46977=DIRECTION ( 'NONE',  ( 1.000000000000000000, 0.000000000000000000, 0.000000000000000000 ) ) ;
#46982=CARTESIAN_POINT ( 'NONE',  ( 0.09215390349082859534, -8.002426153057021097, 0.000000000000000000 ) ) ;
#46989=CARTESIAN_POINT ( 'NONE',  ( 7.999999999999992895, -3.313708498984756279, 14.98655277982336642 ) ) ;
#47007=CARTESIAN_POINT ( 'NONE',  ( 3.313708498984762496, -7.999999999999989342, 7.486552783920144449 ) ) ;
#47029=ADVANCED_FACE ( 'NONE', ( #17182 ), #16799, .T. ) ;
#47054=CARTESIAN_POINT ( 'NONE',  ( 7.188101187499993827, -2.977408999572645598, 6.642802781871754547 ) ) ;
#47078=CARTESIAN_POINT ( 'NONE',  ( -5.082755093536319713, 5.082755093536319713, 3.174052781871751439 ) ) ;
#47081=CARTESIAN_POINT ( 'NONE',  ( -4.898587196589407898E-16, 7.999999999999991118, 2.011552784329821542 ) ) ;
#47090=CARTESIAN_POINT ( 'NONE',  ( 7.999999999999991118, 3.313708498984757611, 27.36155278392014978 ) ) ;
#47102=CARTESIAN_POINT ( 'NONE',  ( -6.062581705673323107, -5.219684191697756326, -0.2078801478342257869 ) ) ;
#47110=ORIENTED_EDGE ( 'NONE', *, *, #55686, .T. ) ;
#47113=CARTESIAN_POINT ( 'NONE',  ( -7.188101187499992051, 2.977408999572646930, 28.39280278187175810 ) ) ;
#47126=CARTESIAN_POINT ( 'NONE',  ( -3.313708498984757167, 7.999999999999991118, 21.73655278392014978 ) ) ;
#47138=CARTESIAN_POINT ( 'NONE',  ( 7.188101187499992051, 8.802885111219154394E-16, 26.23655278187175810 ) ) ;
#47153=AXIS2_PLACEMENT_3D ( 'NONE', #27212, #50229, #21555 ) ;
#47154=CARTESIAN_POINT ( 'NONE',  ( -3.317071493978878571, 8.008118988124991233, 5.231865283940630995 ) ) ;
#47180=CARTESIAN_POINT ( 'NONE',  ( -5.656854249492375253, 5.656854249492375253, 17.14280277982336287 ) ) ;
#47188=( BOUNDED_CURVE ( )  B_SPLINE_CURVE ( 2, ( #57967, #73431, #1359, #13378, #63975, #6638, #40966, #70379, #52287 ),
 .UNSPECIFIED., .F., .F. ) 
 B_SPLINE_CURVE_WITH_KNOTS ( ( 3, 2, 2, 2, 3 ),
 ( 0.1315789473684210453, 0.1381578947368421184, 0.1447368421052631637, 0.1513157894736842368, 0.1578947368421052821 ),
 .UNSPECIFIED. ) 
 CURVE ( )  GEOMETRIC_REPRESENTATION_ITEM ( )  RATIONAL_B_SPLINE_CURVE ( ( 1.000000000000000000, 0.9238795325112867385, 1.000000000000000000, 0.9238795325112867385, 1.000000000000000000, 0.9238795325112867385, 1.000000000000000000, 0.9238795325112864054, 1.000000000000000222 ) ) 
 REPRESENTATION_ITEM ( '' )  );
#47195=CARTESIAN_POINT ( 'NONE',  ( 3.313708498984762496, -7.999999999999989342, 16.35530278432982243 ) ) ;
#47216=CARTESIAN_POINT ( 'NONE',  ( -7.999999999999991118, 3.313708498984757167, 12.92405278392014800 ) ) ;
#47228=CARTESIAN_POINT ( 'NONE',  ( -7.188101187499990274, -2.977408999572651371, 10.58030278187175455 ) ) ;
#47252=CARTESIAN_POINT ( 'NONE',  ( -2.977408999572647819, 7.188101187499992051, 13.58030278187175455 ) ) ;
#47295=EDGE_CURVE ( 'NONE', #43701, #16032, #38087, .T. ) ;
#47296=B_SPLINE_CURVE_WITH_KNOTS ( 'NONE', 3,
 ( #42397, #49173, #48427, #71430, #43141, #66524, #2792, #55233, #66156, #42767, #66910, #37498, #48799, #65783, #26914, #72183, #37875, #8825 ),
 .UNSPECIFIED., .F., .F.,
 ( 4, 2, 2, 2, 2, 2, 2, 2, 4 ),
 ( 0.000000000000000000, 0.06250000000000000000, 0.1250000000000000000, 0.1875000000000000000, 0.2500000000000000000, 0.3125000000000000000, 0.3750000000000000000, 0.4375000000000000000, 0.5000000000000000000 ),
 .UNSPECIFIED. ) ;
#47301=CARTESIAN_POINT ( 'NONE',  ( 8.008118988124991233, 9.807117285998411148E-16, 12.26311528394063011 ) ) ;
#47306=CARTESIAN_POINT ( 'NONE',  ( -7.188101187499992051, 2.977408999572646930, 11.89280278187175277 ) ) ;
#47309=EDGE_CURVE ( 'NONE', #60564, #21067, #13244, .T. ) ;
#47321=CARTESIAN_POINT ( 'NONE',  ( -5.656854249492373476, -5.656854249492376141, -0.2946972160798554397 ) ) ;
#47335=CARTESIAN_POINT ( 'NONE',  ( 7.188101187499991163, 2.977408999572648707, 14.70530278187175455 ) ) ;
#47338=CARTESIAN_POINT ( 'NONE',  ( 7.999999999752645863, -6.290875383172500320E-05, 1.767801038436179750 ) ) ;
#47361=CARTESIAN_POINT ( 'NONE',  ( 3.313708498984762496, -7.999999999999989342, 17.79905277982336642 ) ) ;
#47377=CARTESIAN_POINT ( 'NONE',  ( -7.999999999999991118, 3.313708498984756723, 9.924052783920146226 ) ) ;
#47381=ORIENTED_EDGE ( 'NONE', *, *, #32937, .F. ) ;
#47411=CARTESIAN_POINT ( 'NONE',  ( 7.999999999932789763, 3.279097096261179525E-05, 13.76780373625499010 ) ) ;
#47425=CARTESIAN_POINT ( 'NONE',  ( 5.082755093536318824, 5.082755093536319713, 3.924052781871752327 ) ) ;
#47428=ORIENTED_EDGE ( 'NONE', *, *, #4710, .T. ) ;
#47451=CARTESIAN_POINT ( 'NONE',  ( 1.320432766682872962E-15, -7.188101187499992051, 6.736552781871754547 ) ) ;
#47455=ORIENTED_EDGE ( 'NONE', *, *, #5667, .T. ) ;
#47465=CARTESIAN_POINT ( 'NONE',  ( -3.313708498984758943, -7.999999999999989342, 26.79905278392014623 ) ) ;
#47485=CARTESIAN_POINT ( 'NONE',  ( -4.401442555609577197E-16, 7.188101187499992051, 23.61155278187175455 ) ) ;
#47492=CARTESIAN_POINT ( 'NONE',  ( -7.999999999999991118, 0.000000000000000000, 19.01780278392014623 ) ) ;
#47505=CARTESIAN_POINT ( 'NONE',  ( 7.188101187499992051, 8.802885111219154394E-16, 24.73655278187175810 ) ) ;
#47517=DIRECTION ( 'NONE',  ( -0.000000000000000000, -0.000000000000000000, 1.000000000000000000 ) ) ;
#47521=CARTESIAN_POINT ( 'NONE',  ( 3.317071493978877683, 8.008118988124991233, 3.544365283940628775 ) ) ;
#47528=CARTESIAN_POINT ( 'NONE',  ( -4.401442555609577197E-16, 7.188101187499992051, 19.48655278187175455 ) ) ;
#47535=ORIENTED_EDGE ( 'NONE', *, *, #49440, .F. ) ;
#47543=CARTESIAN_POINT ( 'NONE',  ( 0.000000000000000000, 117.6259055164962462, 36.30610930966346217 ) ) ;
#47547=CARTESIAN_POINT ( 'NONE',  ( 5.656854249492376141, -5.656854249492374365, 17.89280277982336642 ) ) ;
#47560=CARTESIAN_POINT ( 'NONE',  ( -5.656854249492375253, 5.656854249492375253, 15.69905278432982776 ) ) ;
#47590=CARTESIAN_POINT ( 'NONE',  ( 1.320432766682872962E-15, -7.188101187499992051, 12.36155278187175277 ) ) ;
#47600=ADVANCED_FACE ( 'NONE', ( #3485 ), #48393, .F. ) ;
#47614=CARTESIAN_POINT ( 'NONE',  ( -5.082755093536319713, 5.082755093536319713, 10.67405278187175455 ) ) ;
#47618=CARTESIAN_POINT ( 'NONE',  ( -3.313708498984759387, -7.999999999999989342, 20.61155277982336997 ) ) ;
#47634=AXIS2_PLACEMENT_3D ( 'NONE', #59393, #7339, #19019 ) ;
#47661=CARTESIAN_POINT ( 'NONE',  ( -5.662595241051933570, -5.662595241051936235, 10.20061528394063188 ) ) ;
#47666=CARTESIAN_POINT ( 'NONE',  ( -4.401442555609577197E-16, 7.188101187499992051, 10.11155278187175455 ) ) ;
#47681=CARTESIAN_POINT ( 'NONE',  ( 7.999999999999991118, 3.313708498984757611, 1.861552783920143117 ) ) ;
#47695=CARTESIAN_POINT ( 'NONE',  ( -5.082755093536319713, 5.082755093536319713, 13.67405278187175455 ) ) ;
#47697=CARTESIAN_POINT ( 'NONE',  ( -7.999999999999991118, 0.000000000000000000, 3.830302779823362869 ) ) ;
#47707=DIRECTION ( 'NONE',  ( -0.000000000000000000, -0.000000000000000000, 1.000000000000000000 ) ) ;
#47724=CARTESIAN_POINT ( 'NONE',  ( -3.313708498984758943, -7.999999999999989342, 13.11155277982336465 ) ) ;
#47735=CARTESIAN_POINT ( 'NONE',  ( -4.898587196589407898E-16, 7.999999999999991118, 27.45530277982336642 ) ) ;
#47740=CARTESIAN_POINT ( 'NONE',  ( -4.898587196589407898E-16, 7.999999999999991118, 6.642802783920143561 ) ) ;
#47741=ORIENTED_EDGE ( 'NONE', *, *, #8431, .T. ) ;
#47789=CARTESIAN_POINT ( 'NONE',  ( 1.320432766682872962E-15, -7.188101187499992051, 0.3615527818717524378 ) ) ;
#47814=CARTESIAN_POINT ( 'NONE',  ( 1.320432766682872962E-15, -7.188101187499992051, 3.736552781871751883 ) ) ;
#47831=CARTESIAN_POINT ( 'NONE',  ( 5.656854249492374365, 5.656854249492375253, 25.95530278392014623 ) ) ;
#47853=CARTESIAN_POINT ( 'NONE',  ( 7.188101187499993827, -2.977408999572645598, 20.14280278187176165 ) ) ;
#47862=CARTESIAN_POINT ( 'NONE',  ( 7.999999999999992895, -3.313708498984756279, 15.17405278392014623 ) ) ;
#47874=CARTESIAN_POINT ( 'NONE',  ( 7.188101187499993827, -2.977408999572645598, 20.14280278187176165 ) ) ;
#47876=EDGE_CURVE ( 'NONE', #26401, #65370, #38378, .T. ) ;
#47891=CARTESIAN_POINT ( 'NONE',  ( -4.898587196589407898E-16, 7.999999999999991118, 23.14280278392014978 ) ) ;
#47898=CARTESIAN_POINT ( 'NONE',  ( -5.082755093536319713, 5.082755093536319713, 19.67405278187175455 ) ) ;
#47915=CARTESIAN_POINT ( 'NONE',  ( 5.656854249492374365, 5.656854249492375253, 13.76780277982336465 ) ) ;
#47929=CARTESIAN_POINT ( 'NONE',  ( -3.313708498984757167, 7.999999999999991118, 15.60530278432982421 ) ) ;
#47940=VERTEX_POINT ( 'NONE', #43652 ) ;
#47963=CARTESIAN_POINT ( 'NONE',  ( 5.082755093536318824, 5.082755093536319713, 11.42405278187175455 ) ) ;
#47986=CARTESIAN_POINT ( 'NONE',  ( 2.977408999572650927, -7.188101187499990274, 8.330302781871752771 ) ) ;
#48032=CARTESIAN_POINT ( 'NONE',  ( 1.471067592899761672E-15, -8.008118988124991233, 8.888115283940630107 ) ) ;
#48038=CARTESIAN_POINT ( 'NONE',  ( -7.188101187499992051, 2.977408999572646930, 8.892802781871754547 ) ) ;
#48052=CARTESIAN_POINT ( 'NONE',  ( 7.999999999999992895, -3.313708498984756279, 0.1740527839201450044 ) ) ;
#48071=CARTESIAN_POINT ( 'NONE',  ( -5.656854249492375253, 5.656854249492375253, 2.330302783920143561 ) ) ;
#48075=CARTESIAN_POINT ( 'NONE',  ( 7.999999999999991118, 9.797174393178815797E-16, 6.080302779823364645 ) ) ;
#48077=CARTESIAN_POINT ( 'NONE',  ( -7.188101187499992051, 0.000000000000000000, 28.86155278187175810 ) ) ;
#48094=CARTESIAN_POINT ( 'NONE',  ( -4.898587196589407898E-16, 7.999999999999991118, 12.45530277982336642 ) ) ;
#48096=PLANE ( 'NONE',  #23340 ) ;
#48126=CARTESIAN_POINT ( 'NONE',  ( -8.008118988124989457, -3.317071493978883900, 26.60686528394063188 ) ) ;
#48161=CARTESIAN_POINT ( 'NONE',  ( 7.188101187499993827, -2.977408999572645598, 3.642802781871751883 ) ) ;
#48172=DIRECTION ( 'NONE',  ( 1.000000000000000000, 0.000000000000000000, 0.000000000000000000 ) ) ;
#48186=CARTESIAN_POINT ( 'NONE',  ( 1.320432766682872962E-15, -7.188101187499992051, 5.236552781871753659 ) ) ;
#48192=DIRECTION ( 'NONE',  ( 0.000000000000000000, -0.000000000000000000, -1.000000000000000000 ) ) ;
#48200=CARTESIAN_POINT ( 'NONE',  ( 5.656854249492376141, -5.656854249492374365, 22.58030278392014623 ) ) ;
#48222=CARTESIAN_POINT ( 'NONE',  ( 5.082755093536318824, 5.082755093536319713, 18.92405278187175455 ) ) ;
#48233=CARTESIAN_POINT ( 'NONE',  ( -3.313708498984758943, -7.999999999999989342, 14.79905278392014978 ) ) ;
#48245=CARTESIAN_POINT ( 'NONE',  ( 2.977408999572650927, -7.188101187499990274, 16.95530278187175455 ) ) ;
#48262=CARTESIAN_POINT ( 'NONE',  ( -3.313708498984757167, 7.999999999999991118, 26.23655278392014623 ) ) ;
#48269=CARTESIAN_POINT ( 'NONE',  ( 7.188101187499992051, 8.802885111219154394E-16, 19.11155278187175455 ) ) ;
#48288=CARTESIAN_POINT ( 'NONE',  ( -3.313708498984757167, 7.999999999999991118, 15.54905277982336465 ) ) ;
#48302=CARTESIAN_POINT ( 'NONE',  ( 3.313708498984756279, 7.999999999999991118, 19.91780278432982954 ) ) ;
#48303=CARTESIAN_POINT ( 'NONE',  ( -5.447323953993864265, -4.689931814214729044, 0.5319290643893268555 ) ) ;
#48332=CARTESIAN_POINT ( 'NONE',  ( -5.082755093536319713, 5.082755093536319713, 4.299052781871752771 ) ) ;
#48355=CARTESIAN_POINT ( 'NONE',  ( -4.401442555609577197E-16, 7.188101187499992051, 2.986552781871751439 ) ) ;
#48381=CARTESIAN_POINT ( 'NONE',  ( -3.313708498984759387, -7.999999999999989342, 1.111552779823364201 ) ) ;
#48393=( BOUNDED_SURFACE ( )  B_SPLINE_SURFACE ( 1, 2, ( 
 ( #61198, #67609, #15906, #4241, #49118, #9528, #10266, #27228, #8771, #56290, #15533, #33293, #43460, #72892, #21199, #14783, #60441, #60818, #9894, #21570, #61574, #4608, #37442, #37823, #20444, #27603, #15163, #43844, #50614, #54801, #3113, #26097, #21939, #66100, #32543, #3867, #14410, #55554, #31781, #26862, #67237, #72130, #49877, #66475, #50244, #9141, #38574, #73266, #32159, #55180, #44224, #32924, #26475, #72518, #20827, #66857, #23433, #46447, #57789, #27986, #17025, #69465, #6097, #62309, #35151, #69092, #63794, #22306, #51736, #86, #68346, #39311, #39676, #63420, #454, #40422, #57415, #52485, #29475, #16643, #63053, #52122, #11748, #29103, #56669, #28721, #822, #57040, #23063, #17773, #62675, #40788, #28352, #5721, #45700, #11378, #74371, #11010, #40049, #44969, #34412, #34043, #12113, #6472, #17398, #68714, #33663, #5351, #4985, #34786, #46072, #67975, #58166, #16270, #10636, #50991, #74003, #45331, #51361, #22682, #8301, #54340, #59261, #30942, #47547, #59985, #59622, #24898, #29843, #65642, #64544, #58895, #47180, #42628, #18521, #53962, #23809, #7573, #19246, #2275, #53228, #24539, #70571, #52855, #31312, #35511, #1187, #64903, #7204, #48288, #70934, #42257, #41893, #41166, #53599, #46812, #35878, #65269, #18151, #1910, #69836, #18887, #1560, #41529, #30208, #13207, #71293, #36246, #47915, #7937, #64176, #13574, #30577, #36612, #12841, #58524, #12480, #36980, #19614, #70212, #13938, #6831, #24168, #25269, #38479, #3396, #3771, #26004, #15815, #71664, #43752, #66011, #19984, #38103, #8678, #66766, #72425, #44136, #50159, #55838, #60731, #73176, #67146, #27143, #60351, #4154, #42993, #21483, #38850, #15070, #31693, #9053, #54713, #32067, #61854, #20734, #61103, #21113, #37352, #49404, #44505, #43369, #48655, #15441, #14692, #10174, #61481, #55089, #49790, #9806, #25640, #3020, #49028, #72036, #67517, #32828, #20352, #72804, #9433, #33210, #26380, #2651, #32450, #55459, #14317, #66386, #37733, #26772, #5636, #29010, #68258, #6009, #51274, #45987, #12031, #62219, #34693, #74284, #50901, #62586, #22981, #40702, #4893, #28267, #10545, #56950, #33577, #56580, #62966, #16553, #63334, #17686, #46359, #5267, #39590, #63706, #27890, #45614, #56206, #68628, #57325, #67885, #22594, #52029, #69003, #57701, #28636, #17310, #73915, #22219, #16937, #39962, #44879, #27514, #45246, #11291, #366, #23348, #40329, #39219, #34322, #69375, #11659, #73540, #4519, #51650, #50524, #10918, #20105 ),
 ( #21848, #33952, #16176, #42167, #1829, #70852, #46724, #18807, #42546, #47090, #41811, #19165, #58441, #7853, #18434, #47465, #35793, #1475, #64462, #6750, #7119, #65558, #24456, #52767, #47831, #71209, #59180, #58807, #23719, #1105, #69749, #53511, #70489, #35064, #2190, #58077, #30859, #59540, #64821, #7489, #18063, #24816, #19527, #6388, #13123, #65180, #30126, #29394, #13492, #36159, #41078, #25187, #24081, #70128, #29753, #53880, #41449, #36530, #52401, #30494, #48200, #737, #12761, #53142, #64088, #12398, #35431, #25555, #19901, #55006, #71951, #67057, #59905, #60265, #42906, #32742, #37649, #66303, #15356, #2566, #48569, #71579, #9721, #50074, #31981, #26298, #55751, #31231, #4068, #73087, #3311, #65926, #20264, #14230, #43288, #21395, #8968, #49319, #32363, #37272, #60647, #27061, #54628, #8219, #26682, #25925, #44418, #49706, #14610, #61018, #21023, #36895, #8592, #31606, #2937, #13853, #72719, #48941, #9344, #72335, #38392, #20650, #54255, #43665, #66677, #14982, #38019, #55377, #3683, #44048, #61395, #4808, #17223, #62500, #57234, #23261, #73456, #45899, #10829, #62136, #73826, #34233, #51941, #16096, #39505, #21764, #68170, #44792, #67805, #74196, #27802, #74574, #28925, #57612, #16468, #50816, #279, #39131, #40243, #39870, #62872, #33864, #10089, #22501, #67433, #22133, #5546, #61771, #45523, #15729, #56863, #45159, #10458, #5180, #28176, #63246, #51188, #68539, #28548, #38770, #16843, #11205, #51555, #56491, #4430, #33127, #5922, #11572, #33489, #34605, #27425, #56122, #22887, #68913, #50440, #47377, #69661, #60453, #40617, #12672, #34978, #63619, #7031, #52314, #35705, #41361, #14043, #20082, #25737, #29667, #43096, #37079, #71766, #29304, #48758, #30039, #31415, #17974, #66113, #52683, #58720, #47007, #53054, #1018, #40993, #18347, #54816, #1386, #64000, #60082, #8783, #71390, #70038, #57994, #12315, #6298, #65741, #24370, #46270, #14421, #69289, #37455, #31795, #19715, #42727, #650, #8402, #3127, #17600, #54442, #2750, #64371, #11946, #23635, #46642, #35347, #58359, #6664, #23997, #49511, #44981, #20838, #33305, #56682, #61585, #21582, #4619, #55565, #26874, #49888, #32172, #62321, #37833, #55192, #67251, #9541, #27617, #72142, #72530, #3498, #67986, #72903, #3878, #50627, #14795, #60831, #9155, #21953, #10647, #44238, #38585, #16281, #15545, #26110, #9904, #27240, #26486, #21211, #73645, #15918, #39323, #50256, #38949, #43855, #66868, #32935, #55941, #15176, #20454 ),
 ( #43472, #33678, #73278, #49130, #38207, #4252, #44608, #61211, #66485, #32555, #67622, #56303, #61950, #10278, #12496, #64191, #28366, #23076, #12126, #46460, #40803, #16655, #63435, #35526, #17039, #58180, #17790, #62686, #51750, #29489, #63810, #22317, #69853, #29116, #23823, #57053, #11762, #34799, #51375, #74016, #74385, #23446, #35164, #467, #17412, #4999, #27998, #22696, #46086, #6485, #69479, #52499, #39686, #57804, #51007, #40064, #6111, #837, #45714, #46828, #63069, #40435, #5735, #69106, #34427, #68726, #98, #45343, #52135, #11391, #18165, #41180, #68360, #28733, #11024, #57429, #34058, #5366, #70946, #58538, #25656, #6845, #31327, #8317, #65286, #7952, #70226, #48302, #43008, #14336, #19261, #65656, #7586, #20000, #19630, #59636, #64559, #48672, #24554, #18901, #7221, #2664, #53242, #13952, #29859, #42274, #53978, #36993, #13224, #59276, #30592, #12855, #66028, #18536, #35894, #24913, #41908, #60000, #52871, #30224, #58911, #71679, #53611, #36261, #54355, #47195, #41543, #1573, #1202, #24184, #1925, #13592, #47560, #47929, #70584, #36630, #30957, #64916, #2288, #25284, #71310, #42644, #61497, #50174, #73192, #37368, #9819, #9450, #61120, #26396, #49045, #44895, #14711, #37749, #44148, #49422, #44519, #73557, #27530, #32467, #20752, #21866, #9072, #61869, #32843, #55853, #55475, #54732, #67163, #67902, #72444, #4170, #31709, #15458, #60369, #3787, #15086, #32084, #43768, #27157, #8694, #21500, #60749, #67531, #3039, #15831, #26787, #49804, #66782, #72052, #26022, #50542, #10192, #55104, #33223, #20369, #56221, #3412, #38865, #38121, #38493, #72820, #43386, #66403, #21127, #4535, #33593, #11308, #73931, #39978, #68645, #46003, #6022, #34707, #56968, #29026, #69021, #52045, #27909, #57716, #10562, #381, #46376, #62985, #50917, #5283, #22236, #28285, #69391, #45631, #16954, #22996, #45262, #22610, #23361, #62604, #62235, #17325, #33972, #17699, #40346, #51291, #9, #63348, #39235, #68274, #16570, #39607, #40717, #11673, #10934, #16194, #5650, #56598, #34341, #4915, #74302, #57341, #28651, #51666, #22971, #33940, #5255, #52758, #51639, #45977, #34310, #29743, #5626, #18053, #41439, #46348, #6378, #64078, #40319, #11649, #34684, #16926, #47081, #22582, #6740, #356, #10907, #23337, #12021, #45603, #5999, #58431, #727, #41068, #40692, #69365, #39950, #62955, #29000, #17676, #74273, #56939, #11280, #52018, #12388, #35422, #23709, #68617, #57690, #1094, #46713, #28256, #24071 ) ),
 .UNSPECIFIED., .F., .F., .F. ) 
 B_SPLINE_SURFACE_WITH_KNOTS ( ( 2, 1, 2 ),
 ( 3, 2, 2, 2, 2, 2, 2, 2, 2, 2, 2, 2, 2, 2, 2, 2, 2, 2, 2, 2, 2, 2, 2, 2, 2, 2, 2, 2, 2, 2, 2, 2, 2, 2, 2, 2, 2, 2, 2, 2, 2, 2, 2, 2, 2, 2, 2, 2, 2, 2, 2, 2, 2, 2, 2, 2, 2, 2, 2, 2, 2, 2, 2, 2, 2, 2, 2, 2, 2, 2, 2, 2, 2, 2, 2, 2, 2, 2, 2, 2, 2, 2, 2, 2, 2, 2, 2, 2, 2, 2, 2, 2, 2, 2, 2, 2, 2, 2, 2, 2, 2, 2, 2, 2, 2, 2, 2, 2, 2, 2, 2, 2, 2, 2, 2, 2, 2, 2, 2, 2, 2, 2, 2, 2, 2, 2, 2, 2, 2, 2, 2, 2, 2, 2, 2, 2, 2, 2, 2, 2, 2, 2, 2, 2, 2, 2, 2, 2, 2, 2, 2, 2, 2, 2, 3 ),
 ( 0.000000000000000000, 1.000000000000000000, 1.100000000000000089 ),
 ( -0.01003998210305807881, 0.000000000000000000, 0.006578947368421052266, 0.01315789473684210453, 0.01973684210526315680, 0.02631578947368420907, 0.03289473684210526133, 0.03947368421052631360, 0.04605263157894736586, 0.05263157894736841813, 0.05921052631578947040, 0.06578947368421052266, 0.07236842105263158187, 0.07894736842105262720, 0.08552631578947368640, 0.09210526315789473173, 0.09868421052631579093, 0.1052631578947368363, 0.1118421052631578955, 0.1184210526315789408, 0.1250000000000000000, 0.1315789473684210453, 0.1381578947368421184, 0.1447368421052631637, 0.1513157894736842091, 0.1578947368421052544, 0.1644736842105263275, 0.1710526315789473728, 0.1776315789473684181, 0.1842105263157894635, 0.1907894736842105365, 0.1973684210526315819, 0.2039473684210526272, 0.2105263157894736725, 0.2171052631578947456, 0.2236842105263157909, 0.2302631578947368363, 0.2368421052631578816, 0.2434210526315789547, 0.2500000000000000000, 0.2565789473684210731, 0.2631578947368420907, 0.2697368421052631637, 0.2763157894736842368, 0.2828947368421052544, 0.2894736842105263275, 0.2960526315789473450, 0.3026315789473684181, 0.3092105263157894912, 0.3157894736842105088, 0.3223684210526315819, 0.3289473684210526550, 0.3355263157894736725, 0.3421052631578947456, 0.3486842105263157632, 0.3552631578947368363, 0.3618421052631579093, 0.3684210526315789269, 0.3750000000000000000, 0.3815789473684210731, 0.3881578947368420907, 0.3947368421052631637, 0.4013157894736842368, 0.4078947368421052544, 0.4144736842105263275, 0.4210526315789473450, 0.4276315789473684181, 0.4342105263157894912, 0.4407894736842105088, 0.4473684210526315819, 0.4539473684210526550, 0.4605263157894736725, 0.4671052631578947456, 0.4736842105263157632, 0.4802631578947368363, 0.4868421052631579093, 0.4934210526315789269, 0.5000000000000000000, 0.5065789473684210176, 0.5131578947368421462, 0.5197368421052631637, 0.5263157894736841813, 0.5328947368421053099, 0.5394736842105263275, 0.5460526315789473450, 0.5526315789473684736, 0.5592105263157894912, 0.5657894736842105088, 0.5723684210526315264, 0.5789473684210526550, 0.5855263157894736725, 0.5921052631578946901, 0.5986842105263158187, 0.6052631578947368363, 0.6118421052631578538, 0.6184210526315789824, 0.6250000000000000000, 0.6315789473684210176, 0.6381578947368421462, 0.6447368421052631637, 0.6513157894736841813, 0.6578947368421053099, 0.6644736842105263275, 0.6710526315789473450, 0.6776315789473684736, 0.6842105263157894912, 0.6907894736842105088, 0.6973684210526315264, 0.7039473684210526550, 0.7105263157894736725, 0.7171052631578946901, 0.7236842105263158187, 0.7302631578947368363, 0.7368421052631578538, 0.7434210526315789824, 0.7500000000000000000, 0.7565789473684210176, 0.7631578947368421462, 0.7697368421052631637, 0.7763157894736841813, 0.7828947368421053099, 0.7894736842105263275, 0.7960526315789473450, 0.8026315789473684736, 0.8092105263157894912, 0.8157894736842105088, 0.8223684210526315264, 0.8289473684210526550, 0.8355263157894736725, 0.8421052631578946901, 0.8486842105263158187, 0.8552631578947368363, 0.8618421052631578538, 0.8684210526315789824, 0.8750000000000000000, 0.8815789473684210176, 0.8881578947368421462, 0.8947368421052631637, 0.9013157894736841813, 0.9078947368421053099, 0.9144736842105263275, 0.9210526315789473450, 0.9276315789473684736, 0.9342105263157894912, 0.9407894736842105088, 0.9473684210526315264, 0.9539473684210526550, 0.9605263157894736725, 0.9671052631578946901, 0.9736842105263158187, 0.9802631578947368363, 0.9868421052631578538, 0.9934210526315789824, 0.9940576339661463257, 1.003998210305807826 ),
 .UNSPECIFIED. ) 
 GEOMETRIC_REPRESENTATION_ITEM ( )  RATIONAL_B_SPLINE_SURFACE ( (
 ( 1.000000000000000000, 1.000000000000000000, 1.000000000000000000, 0.9238795325112867385, 1.000000000000000000, 0.9238795325112867385, 1.000000000000000000, 0.9238795325112867385, 1.000000000000000000, 0.9238795325112867385, 1.000000000000000000, 0.9238795325112867385, 1.000000000000000000, 0.9238795325112867385, 1.000000000000000000, 0.9238795325112867385, 1.000000000000000000, 0.9238795325112867385, 1.000000000000000000, 0.9238795325112867385, 1.000000000000000000, 0.9238795325112867385, 1.000000000000000000, 0.9238795325112867385, 1.000000000000000000, 0.9238795325112867385, 1.000000000000000000, 0.9238795325112867385, 1.000000000000000000, 0.9238795325112867385, 1.000000000000000000, 0.9238795325112867385, 1.000000000000000000, 0.9238795325112867385, 1.000000000000000000, 0.9238795325112867385, 1.000000000000000000, 0.9238795325112867385, 1.000000000000000000, 0.9238795325112867385, 1.000000000000000000, 0.9238795325112867385, 1.000000000000000000, 0.9238795325112867385, 1.000000000000000000, 0.9238795325112867385, 1.000000000000000000, 0.9238795325112867385, 1.000000000000000000, 0.9238795325112867385, 1.000000000000000000, 0.9238795325112867385, 1.000000000000000000, 0.9238795325112867385, 1.000000000000000000, 0.9238795325112867385, 1.000000000000000000, 0.9238795325112867385, 1.000000000000000000, 0.9238795325112867385, 1.000000000000000000, 0.9238795325112867385, 1.000000000000000000, 0.9238795325112867385, 1.000000000000000000, 0.9238795325112867385, 1.000000000000000000, 0.9238795325112867385, 1.000000000000000000, 0.9238795325112867385, 1.000000000000000000, 0.9238795325112867385, 1.000000000000000000, 0.9238795325112867385, 1.000000000000000000, 0.9238795325112867385, 1.000000000000000000, 0.9238795325112867385, 1.000000000000000000, 0.9238795325112867385, 1.000000000000000000, 0.9238795325112867385, 1.000000000000000000, 0.9238795325112867385, 1.000000000000000000, 0.9238795325112867385, 1.000000000000000000, 0.9238795325112867385, 1.000000000000000000, 0.9238795325112867385, 1.000000000000000000, 0.9238795325112867385, 1.000000000000000000, 0.9238795325112867385, 1.000000000000000000, 0.9238795325112867385, 1.000000000000000000, 0.9238795325112867385, 1.000000000000000000, 0.9238795325112867385, 1.000000000000000000, 0.9238795325112867385, 1.000000000000000000, 0.9238795325112867385, 1.000000000000000000, 0.9238795325112867385, 1.000000000000000000, 0.9238795325112867385, 1.000000000000000000, 0.9238795325112867385, 1.000000000000000000, 0.9238795325112867385, 1.000000000000000000, 0.9238795325112867385, 1.000000000000000000, 0.9238795325112867385, 1.000000000000000000, 0.9238795325112867385, 1.000000000000000000, 0.9238795325112867385, 1.000000000000000000, 0.9238795325112867385, 1.000000000000000000, 0.9238795325112867385, 1.000000000000000000, 0.9238795325112867385, 1.000000000000000000, 0.9238795325112867385, 1.000000000000000000, 0.9238795325112867385, 1.000000000000000000, 0.9238795325112867385, 1.000000000000000000, 0.9238795325112867385, 1.000000000000000000, 0.9238795325112867385, 1.000000000000000000, 0.9238795325112867385, 1.000000000000000000, 0.9238795325112867385, 1.000000000000000000, 0.9238795325112867385, 1.000000000000000000, 0.9238795325112867385, 1.000000000000000000, 0.9238795325112867385, 1.000000000000000000, 0.9238795325112867385, 1.000000000000000000, 0.9238795325112867385, 1.000000000000000000, 0.9238795325112867385, 1.000000000000000000, 0.9238795325112867385, 1.000000000000000000, 0.9238795325112867385, 1.000000000000000000, 0.9238795325112867385, 1.000000000000000000, 0.9238795325112867385, 1.000000000000000000, 0.9238795325112867385, 1.000000000000000000, 0.9238795325112867385, 1.000000000000000000, 0.9238795325112867385, 1.000000000000000000, 0.9238795325112867385, 1.000000000000000000, 0.9238795325112867385, 1.000000000000000000, 0.9238795325112867385, 1.000000000000000000, 0.9238795325112867385, 1.000000000000000000, 0.9238795325112867385, 1.000000000000000000, 0.9238795325112867385, 1.000000000000000000, 0.9238795325112867385, 1.000000000000000000, 0.9238795325112867385, 1.000000000000000000, 0.9238795325112867385, 1.000000000000000000, 0.9238795325112867385, 1.000000000000000000, 0.9238795325112867385, 1.000000000000000000, 0.9238795325112867385, 1.000000000000000000, 0.9238795325112867385, 1.000000000000000000, 0.9238795325112867385, 1.000000000000000000, 0.9238795325112867385, 1.000000000000000000, 0.9238795325112867385, 1.000000000000000000, 0.9238795325112867385, 1.000000000000000000, 0.9238795325112867385, 1.000000000000000000, 0.9238795325112867385, 1.000000000000000000, 0.9238795325112867385, 1.000000000000000000, 0.9238795325112867385, 1.000000000000000000, 0.9238795325112867385, 1.000000000000000000, 0.9238795325112867385, 1.000000000000000000, 0.9238795325112867385, 1.000000000000000000, 0.9238795325112867385, 1.000000000000000000, 0.9238795325112867385, 1.000000000000000000, 0.9238795325112867385, 1.000000000000000000, 0.9238795325112867385, 1.000000000000000000, 0.9238795325112867385, 1.000000000000000000, 0.9238795325112867385, 1.000000000000000000, 0.9238795325112867385, 1.000000000000000000, 0.9238795325112867385, 1.000000000000000000, 0.9238795325112867385, 1.000000000000000000, 0.9238795325112867385, 1.000000000000000000, 0.9238795325112867385, 1.000000000000000000, 0.9238795325112867385, 1.000000000000000000, 0.9238795325112867385, 1.000000000000000000, 0.9238795325112867385, 1.000000000000000000, 0.9238795325112867385, 1.000000000000000000, 0.9238795325112867385, 1.000000000000000000, 0.9238795325112867385, 1.000000000000000000, 0.9238795325112867385, 1.000000000000000000, 0.9238795325112867385, 1.000000000000000000, 0.9238795325112867385, 1.000000000000000000, 0.9238795325112867385, 1.000000000000000000, 0.9238795325112867385, 1.000000000000000000, 0.9238795325112867385, 1.000000000000000000, 0.9238795325112867385, 1.000000000000000000, 0.9238795325112867385, 1.000000000000000000, 0.9238795325112867385, 1.000000000000000000, 0.9238795325112867385, 1.000000000000000000, 0.9238795325112867385, 1.000000000000000000, 0.9238795325112867385, 1.000000000000000000, 0.9238795325112867385, 1.000000000000000000, 0.9238795325112867385, 1.000000000000000000, 0.9238795325112867385, 1.000000000000000000, 0.9238795325112867385, 1.000000000000000000, 0.9238795325112867385, 1.000000000000000000, 0.9238795325112867385, 1.000000000000000000, 0.9238795325112867385, 1.000000000000000000, 0.9238795325112867385, 1.000000000000000000, 0.9238795325112867385, 1.000000000000000000, 0.9238795325112867385, 1.000000000000000000, 0.9238795325112867385, 1.000000000000000000, 0.9238795325112867385, 1.000000000000000000, 0.9238795325112867385, 1.000000000000000000, 0.9238795325112867385, 1.000000000000000000, 0.9238795325112867385, 1.000000000000000000, 0.9238795325112867385, 1.000000000000000000, 0.9926345559451579259, 0.9866944779689741374, 0.9866944779689741374, 0.9866944779689741374),
 ( 1.000000000000000000, 1.000000000000000000, 1.000000000000000000, 0.9238795325112867385, 1.000000000000000000, 0.9238795325112867385, 1.000000000000000000, 0.9238795325112867385, 1.000000000000000000, 0.9238795325112867385, 1.000000000000000000, 0.9238795325112867385, 1.000000000000000000, 0.9238795325112867385, 1.000000000000000000, 0.9238795325112867385, 1.000000000000000000, 0.9238795325112867385, 1.000000000000000000, 0.9238795325112867385, 1.000000000000000000, 0.9238795325112867385, 1.000000000000000000, 0.9238795325112867385, 1.000000000000000000, 0.9238795325112867385, 1.000000000000000000, 0.9238795325112867385, 1.000000000000000000, 0.9238795325112867385, 1.000000000000000000, 0.9238795325112867385, 1.000000000000000000, 0.9238795325112867385, 1.000000000000000000, 0.9238795325112867385, 1.000000000000000000, 0.9238795325112867385, 1.000000000000000000, 0.9238795325112867385, 1.000000000000000000, 0.9238795325112867385, 1.000000000000000000, 0.9238795325112867385, 1.000000000000000000, 0.9238795325112867385, 1.000000000000000000, 0.9238795325112867385, 1.000000000000000000, 0.9238795325112867385, 1.000000000000000000, 0.9238795325112867385, 1.000000000000000000, 0.9238795325112867385, 1.000000000000000000, 0.9238795325112867385, 1.000000000000000000, 0.9238795325112867385, 1.000000000000000000, 0.9238795325112867385, 1.000000000000000000, 0.9238795325112867385, 1.000000000000000000, 0.9238795325112867385, 1.000000000000000000, 0.9238795325112867385, 1.000000000000000000, 0.9238795325112867385, 1.000000000000000000, 0.9238795325112867385, 1.000000000000000000, 0.9238795325112867385, 1.000000000000000000, 0.9238795325112867385, 1.000000000000000000, 0.9238795325112867385, 1.000000000000000000, 0.9238795325112867385, 1.000000000000000000, 0.9238795325112867385, 1.000000000000000000, 0.9238795325112867385, 1.000000000000000000, 0.9238795325112867385, 1.000000000000000000, 0.9238795325112867385, 1.000000000000000000, 0.9238795325112867385, 1.000000000000000000, 0.9238795325112867385, 1.000000000000000000, 0.9238795325112867385, 1.000000000000000000, 0.9238795325112867385, 1.000000000000000000, 0.9238795325112867385, 1.000000000000000000, 0.9238795325112867385, 1.000000000000000000, 0.9238795325112867385, 1.000000000000000000, 0.9238795325112867385, 1.000000000000000000, 0.9238795325112867385, 1.000000000000000000, 0.9238795325112867385, 1.000000000000000000, 0.9238795325112867385, 1.000000000000000000, 0.9238795325112867385, 1.000000000000000000, 0.9238795325112867385, 1.000000000000000000, 0.9238795325112867385, 1.000000000000000000, 0.9238795325112867385, 1.000000000000000000, 0.9238795325112867385, 1.000000000000000000, 0.9238795325112867385, 1.000000000000000000, 0.9238795325112867385, 1.000000000000000000, 0.9238795325112867385, 1.000000000000000000, 0.9238795325112867385, 1.000000000000000000, 0.9238795325112867385, 1.000000000000000000, 0.9238795325112867385, 1.000000000000000000, 0.9238795325112867385, 1.000000000000000000, 0.9238795325112867385, 1.000000000000000000, 0.9238795325112867385, 1.000000000000000000, 0.9238795325112867385, 1.000000000000000000, 0.9238795325112867385, 1.000000000000000000, 0.9238795325112867385, 1.000000000000000000, 0.9238795325112867385, 1.000000000000000000, 0.9238795325112867385, 1.000000000000000000, 0.9238795325112867385, 1.000000000000000000, 0.9238795325112867385, 1.000000000000000000, 0.9238795325112867385, 1.000000000000000000, 0.9238795325112867385, 1.000000000000000000, 0.9238795325112867385, 1.000000000000000000, 0.9238795325112867385, 1.000000000000000000, 0.9238795325112867385, 1.000000000000000000, 0.9238795325112867385, 1.000000000000000000, 0.9238795325112867385, 1.000000000000000000, 0.9238795325112867385, 1.000000000000000000, 0.9238795325112867385, 1.000000000000000000, 0.9238795325112867385, 1.000000000000000000, 0.9238795325112867385, 1.000000000000000000, 0.9238795325112867385, 1.000000000000000000, 0.9238795325112867385, 1.000000000000000000, 0.9238795325112867385, 1.000000000000000000, 0.9238795325112867385, 1.000000000000000000, 0.9238795325112867385, 1.000000000000000000, 0.9238795325112867385, 1.000000000000000000, 0.9238795325112867385, 1.000000000000000000, 0.9238795325112867385, 1.000000000000000000, 0.9238795325112867385, 1.000000000000000000, 0.9238795325112867385, 1.000000000000000000, 0.9238795325112867385, 1.000000000000000000, 0.9238795325112867385, 1.000000000000000000, 0.9238795325112867385, 1.000000000000000000, 0.9238795325112867385, 1.000000000000000000, 0.9238795325112867385, 1.000000000000000000, 0.9238795325112867385, 1.000000000000000000, 0.9238795325112867385, 1.000000000000000000, 0.9238795325112867385, 1.000000000000000000, 0.9238795325112867385, 1.000000000000000000, 0.9238795325112867385, 1.000000000000000000, 0.9238795325112867385, 1.000000000000000000, 0.9238795325112867385, 1.000000000000000000, 0.9238795325112867385, 1.000000000000000000, 0.9238795325112867385, 1.000000000000000000, 0.9238795325112867385, 1.000000000000000000, 0.9238795325112867385, 1.000000000000000000, 0.9238795325112867385, 1.000000000000000000, 0.9238795325112867385, 1.000000000000000000, 0.9238795325112867385, 1.000000000000000000, 0.9238795325112867385, 1.000000000000000000, 0.9238795325112867385, 1.000000000000000000, 0.9238795325112867385, 1.000000000000000000, 0.9238795325112867385, 1.000000000000000000, 0.9238795325112867385, 1.000000000000000000, 0.9238795325112867385, 1.000000000000000000, 0.9238795325112867385, 1.000000000000000000, 0.9238795325112867385, 1.000000000000000000, 0.9238795325112867385, 1.000000000000000000, 0.9238795325112867385, 1.000000000000000000, 0.9238795325112867385, 1.000000000000000000, 0.9238795325112867385, 1.000000000000000000, 0.9238795325112867385, 1.000000000000000000, 0.9238795325112867385, 1.000000000000000000, 0.9238795325112867385, 1.000000000000000000, 0.9238795325112867385, 1.000000000000000000, 0.9238795325112867385, 1.000000000000000000, 0.9238795325112867385, 1.000000000000000000, 0.9238795325112867385, 1.000000000000000000, 0.9238795325112867385, 1.000000000000000000, 0.9238795325112867385, 1.000000000000000000, 0.9238795325112867385, 1.000000000000000000, 0.9238795325112867385, 1.000000000000000000, 0.9238795325112867385, 1.000000000000000000, 0.9238795325112867385, 1.000000000000000000, 0.9238795325112867385, 1.000000000000000000, 0.9238795325112867385, 1.000000000000000000, 0.9238795325112867385, 1.000000000000000000, 0.9238795325112867385, 1.000000000000000000, 0.9238795325112867385, 1.000000000000000000, 0.9238795325112867385, 1.000000000000000000, 0.9238795325112867385, 1.000000000000000000, 0.9238795325112867385, 1.000000000000000000, 0.9238795325112867385, 1.000000000000000000, 0.9238795325112867385, 1.000000000000000000, 0.9238795325112867385, 1.000000000000000000, 0.9238795325112867385, 1.000000000000000000, 0.9926345559451579259, 0.9866944779689741374, 0.9866944779689741374, 0.9866944779689741374),
 ( 1.000000000000000000, 1.000000000000000000, 1.000000000000000000, 0.9238795325112867385, 1.000000000000000000, 0.9238795325112867385, 1.000000000000000000, 0.9238795325112867385, 1.000000000000000000, 0.9238795325112867385, 1.000000000000000000, 0.9238795325112867385, 1.000000000000000000, 0.9238795325112867385, 1.000000000000000000, 0.9238795325112867385, 1.000000000000000000, 0.9238795325112867385, 1.000000000000000000, 0.9238795325112867385, 1.000000000000000000, 0.9238795325112867385, 1.000000000000000000, 0.9238795325112867385, 1.000000000000000000, 0.9238795325112867385, 1.000000000000000000, 0.9238795325112867385, 1.000000000000000000, 0.9238795325112867385, 1.000000000000000000, 0.9238795325112867385, 1.000000000000000000, 0.9238795325112867385, 1.000000000000000000, 0.9238795325112867385, 1.000000000000000000, 0.9238795325112867385, 1.000000000000000000, 0.9238795325112867385, 1.000000000000000000, 0.9238795325112867385, 1.000000000000000000, 0.9238795325112867385, 1.000000000000000000, 0.9238795325112867385, 1.000000000000000000, 0.9238795325112867385, 1.000000000000000000, 0.9238795325112867385, 1.000000000000000000, 0.9238795325112867385, 1.000000000000000000, 0.9238795325112867385, 1.000000000000000000, 0.9238795325112867385, 1.000000000000000000, 0.9238795325112867385, 1.000000000000000000, 0.9238795325112867385, 1.000000000000000000, 0.9238795325112867385, 1.000000000000000000, 0.9238795325112867385, 1.000000000000000000, 0.9238795325112867385, 1.000000000000000000, 0.9238795325112867385, 1.000000000000000000, 0.9238795325112867385, 1.000000000000000000, 0.9238795325112867385, 1.000000000000000000, 0.9238795325112867385, 1.000000000000000000, 0.9238795325112867385, 1.000000000000000000, 0.9238795325112867385, 1.000000000000000000, 0.9238795325112867385, 1.000000000000000000, 0.9238795325112867385, 1.000000000000000000, 0.9238795325112867385, 1.000000000000000000, 0.9238795325112867385, 1.000000000000000000, 0.9238795325112867385, 1.000000000000000000, 0.9238795325112867385, 1.000000000000000000, 0.9238795325112867385, 1.000000000000000000, 0.9238795325112867385, 1.000000000000000000, 0.9238795325112867385, 1.000000000000000000, 0.9238795325112867385, 1.000000000000000000, 0.9238795325112867385, 1.000000000000000000, 0.9238795325112867385, 1.000000000000000000, 0.9238795325112867385, 1.000000000000000000, 0.9238795325112867385, 1.000000000000000000, 0.9238795325112867385, 1.000000000000000000, 0.9238795325112867385, 1.000000000000000000, 0.9238795325112867385, 1.000000000000000000, 0.9238795325112867385, 1.000000000000000000, 0.9238795325112867385, 1.000000000000000000, 0.9238795325112867385, 1.000000000000000000, 0.9238795325112867385, 1.000000000000000000, 0.9238795325112867385, 1.000000000000000000, 0.9238795325112867385, 1.000000000000000000, 0.9238795325112867385, 1.000000000000000000, 0.9238795325112867385, 1.000000000000000000, 0.9238795325112867385, 1.000000000000000000, 0.9238795325112867385, 1.000000000000000000, 0.9238795325112867385, 1.000000000000000000, 0.9238795325112867385, 1.000000000000000000, 0.9238795325112867385, 1.000000000000000000, 0.9238795325112867385, 1.000000000000000000, 0.9238795325112867385, 1.000000000000000000, 0.9238795325112867385, 1.000000000000000000, 0.9238795325112867385, 1.000000000000000000, 0.9238795325112867385, 1.000000000000000000, 0.9238795325112867385, 1.000000000000000000, 0.9238795325112867385, 1.000000000000000000, 0.9238795325112867385, 1.000000000000000000, 0.9238795325112867385, 1.000000000000000000, 0.9238795325112867385, 1.000000000000000000, 0.9238795325112867385, 1.000000000000000000, 0.9238795325112867385, 1.000000000000000000, 0.9238795325112867385, 1.000000000000000000, 0.9238795325112867385, 1.000000000000000000, 0.9238795325112867385, 1.000000000000000000, 0.9238795325112867385, 1.000000000000000000, 0.9238795325112867385, 1.000000000000000000, 0.9238795325112867385, 1.000000000000000000, 0.9238795325112867385, 1.000000000000000000, 0.9238795325112867385, 1.000000000000000000, 0.9238795325112867385, 1.000000000000000000, 0.9238795325112867385, 1.000000000000000000, 0.9238795325112867385, 1.000000000000000000, 0.9238795325112867385, 1.000000000000000000, 0.9238795325112867385, 1.000000000000000000, 0.9238795325112867385, 1.000000000000000000, 0.9238795325112867385, 1.000000000000000000, 0.9238795325112867385, 1.000000000000000000, 0.9238795325112867385, 1.000000000000000000, 0.9238795325112867385, 1.000000000000000000, 0.9238795325112867385, 1.000000000000000000, 0.9238795325112867385, 1.000000000000000000, 0.9238795325112867385, 1.000000000000000000, 0.9238795325112867385, 1.000000000000000000, 0.9238795325112867385, 1.000000000000000000, 0.9238795325112867385, 1.000000000000000000, 0.9238795325112867385, 1.000000000000000000, 0.9238795325112867385, 1.000000000000000000, 0.9238795325112867385, 1.000000000000000000, 0.9238795325112867385, 1.000000000000000000, 0.9238795325112867385, 1.000000000000000000, 0.9238795325112867385, 1.000000000000000000, 0.9238795325112867385, 1.000000000000000000, 0.9238795325112867385, 1.000000000000000000, 0.9238795325112867385, 1.000000000000000000, 0.9238795325112867385, 1.000000000000000000, 0.9238795325112867385, 1.000000000000000000, 0.9238795325112867385, 1.000000000000000000, 0.9238795325112867385, 1.000000000000000000, 0.9238795325112867385, 1.000000000000000000, 0.9238795325112867385, 1.000000000000000000, 0.9238795325112867385, 1.000000000000000000, 0.9238795325112867385, 1.000000000000000000, 0.9238795325112867385, 1.000000000000000000, 0.9238795325112867385, 1.000000000000000000, 0.9238795325112867385, 1.000000000000000000, 0.9238795325112867385, 1.000000000000000000, 0.9238795325112867385, 1.000000000000000000, 0.9238795325112867385, 1.000000000000000000, 0.9238795325112867385, 1.000000000000000000, 0.9238795325112867385, 1.000000000000000000, 0.9238795325112867385, 1.000000000000000000, 0.9238795325112867385, 1.000000000000000000, 0.9238795325112867385, 1.000000000000000000, 0.9238795325112867385, 1.000000000000000000, 0.9238795325112867385, 1.000000000000000000, 0.9238795325112867385, 1.000000000000000000, 0.9238795325112867385, 1.000000000000000000, 0.9238795325112867385, 1.000000000000000000, 0.9238795325112867385, 1.000000000000000000, 0.9238795325112867385, 1.000000000000000000, 0.9238795325112867385, 1.000000000000000000, 0.9238795325112867385, 1.000000000000000000, 0.9238795325112867385, 1.000000000000000000, 0.9238795325112867385, 1.000000000000000000, 0.9238795325112867385, 1.000000000000000000, 0.9238795325112867385, 1.000000000000000000, 0.9238795325112867385, 1.000000000000000000, 0.9238795325112867385, 1.000000000000000000, 0.9238795325112867385, 1.000000000000000000, 0.9238795325112867385, 1.000000000000000000, 0.9238795325112867385, 1.000000000000000000, 0.9238795325112867385, 1.000000000000000000, 0.9926345559451579259, 0.9866944779689741374, 0.9866944779689741374, 0.9866944779689741374) ) ) 
 REPRESENTATION_ITEM ( '' )  SURFACE ( )  );
#48404=CARTESIAN_POINT ( 'NONE',  ( 8.008118988124993010, -3.317071493978877239, 10.66936528394063011 ) ) ;
#48410=CARTESIAN_POINT ( 'NONE',  ( 5.082755093536320601, -5.082755093536318824, 0.5490527818717526598 ) ) ;
#48423=CARTESIAN_POINT ( 'NONE',  ( -4.401442555609577197E-16, 7.188101187499992051, 23.61155278187175455 ) ) ;
#48427=CARTESIAN_POINT ( 'NONE',  ( 7.796785530332603464, 2.081694232947989054, -0.000000000000000000 ) ) ;
#48447=CARTESIAN_POINT ( 'NONE',  ( 3.313708498984762496, -7.999999999999989342, 4.299052779823362869 ) ) ;
#48465=CARTESIAN_POINT ( 'NONE',  ( -3.313708498984758943, -7.999999999999989342, 14.61155277982336465 ) ) ;
#48496=CARTESIAN_POINT ( 'NONE',  ( -3.317071493978878571, 8.008118988124991233, 24.73186528394063544 ) ) ;
#48524=DIRECTION ( 'NONE',  ( -1.621639297089430499E-05, 1.883468370551372626E-05, 0.9999999996911416167 ) ) ;
#48527=CARTESIAN_POINT ( 'NONE',  ( 7.188101187499992051, 8.802885111219154394E-16, 2.236552781871750550 ) ) ;
#48552=CARTESIAN_POINT ( 'NONE',  ( 5.082755093536318824, 5.082755093536319713, 1.299052781871753215 ) ) ;
#48569=CARTESIAN_POINT ( 'NONE',  ( -5.656854249492373476, -5.656854249492376141, 20.70530278392014623 ) ) ;
#48592=CARTESIAN_POINT ( 'NONE',  ( -5.082755093536317936, -5.082755093536320601, 21.17405278187175455 ) ) ;
#48601=EDGE_CURVE ( 'NONE', #8103, #62523, #20165, .T. ) ;
#48605=CARTESIAN_POINT ( 'NONE',  ( 1.469576158976822172E-15, -7.999999999999991118, 13.39280278392014623 ) ) ;
#48614=CARTESIAN_POINT ( 'NONE',  ( -2.977408999572647819, 7.188101187499991163, 20.70530278187175455 ) ) ;
#48631=CARTESIAN_POINT ( 'NONE',  ( -5.656854249492373476, -5.656854249492376141, 23.70530278392014978 ) ) ;
#48638=CARTESIAN_POINT ( 'NONE',  ( 2.977408999572646486, 7.188101187499991163, 19.39280278187176165 ) ) ;
#48652=DIRECTION ( 'NONE',  ( -0.000000000000000000, -0.000000000000000000, 1.000000000000000000 ) ) ;
#48655=CARTESIAN_POINT ( 'NONE',  ( 1.469576158976822172E-15, -7.999999999999991118, 8.705302779823362869 ) ) ;
#48672=CARTESIAN_POINT ( 'NONE',  ( -7.999999999999989342, -3.313708498984762496, 18.98030278432982954 ) ) ;
#48703=CARTESIAN_POINT ( 'NONE',  ( -2.977408999572647819, 7.188101187499991163, 5.705302781871753659 ) ) ;
#48704=ORIENTED_EDGE ( 'NONE', *, *, #73472, .F. ) ;
#48706=( BOUNDED_CURVE ( )  B_SPLINE_CURVE ( 2, ( #55328, #45110, #68123, #44369, #67380, #39083, #16417, #39450, #62450 ),
 .UNSPECIFIED., .F., .F. ) 
 B_SPLINE_CURVE_WITH_KNOTS ( ( 3, 2, 2, 2, 3 ),
 ( 0.9210526315789474561, 0.9276315789473685847, 0.9342105263157896022, 0.9407894736842106198, 0.9473684210526316374 ),
 .UNSPECIFIED. ) 
 CURVE ( )  GEOMETRIC_REPRESENTATION_ITEM ( )  RATIONAL_B_SPLINE_CURVE ( ( 0.9999999999999986677, 0.9238795325112880708, 1.000000000000000000, 0.9238795325112867385, 1.000000000000000000, 0.9238795325112867385, 1.000000000000000000, 0.9238795325112854062, 1.000000000000001332 ) ) 
 REPRESENTATION_ITEM ( '' )  );
#48728=EDGE_CURVE ( 'NONE', #31087, #21048, #73512, .T. ) ;
#48729=CARTESIAN_POINT ( 'NONE',  ( -5.082755093536317936, -5.082755093536320601, 3.549052781871751883 ) ) ;
#48757=DIRECTION ( 'NONE',  ( -0.000000000000000000, -0.000000000000000000, 1.000000000000000000 ) ) ;
#48758=CARTESIAN_POINT ( 'NONE',  ( -4.898587196589407898E-16, 7.999999999999991118, 8.142802783920144449 ) ) ;
#48776=CARTESIAN_POINT ( 'NONE',  ( -8.008118988124989457, -3.317071493978883900, 10.10686528394063188 ) ) ;
#48782=CARTESIAN_POINT ( 'NONE',  ( 1.320432766682872962E-15, -7.188101187499992051, 1.861552781871753881 ) ) ;
#48794=CARTESIAN_POINT ( 'NONE',  ( -2.977408999572647819, 7.188101187499991163, 23.70530278187175810 ) ) ;
#48799=CARTESIAN_POINT ( 'NONE',  ( -4.906935342930776045, 6.406660676655467235, 0.000000000000000000 ) ) ;
#48820=CARTESIAN_POINT ( 'NONE',  ( -2.977408999572647819, 7.188101187499992051, 24.08030278187175099 ) ) ;
#48822=CARTESIAN_POINT ( 'NONE',  ( 7.999999999999991118, 9.797174393178815797E-16, 22.76780278392014623 ) ) ;
#48838=CARTESIAN_POINT ( 'NONE',  ( 5.656854249492376141, -5.656854249492374365, 8.892802779823364645 ) ) ;
#48857=SHAPE_REPRESENTATION ( 'clamping lever', ( #57354 ), #18781 ) ;
#48866=CARTESIAN_POINT ( 'NONE',  ( -5.662595241051933570, -5.662595241051936235, 25.20061528394063544 ) ) ;
#48886=ORIENTED_EDGE ( 'NONE', *, *, #4001, .F. ) ;
#48898=CARTESIAN_POINT ( 'NONE',  ( 2.977408999572650927, -7.188101187499990274, 27.83030278187176165 ) ) ;
#48913=VECTOR ( 'NONE', #21987, 1000.000000000000000 ) ;
#48924=CARTESIAN_POINT ( 'NONE',  ( -7.999999999999989342, -3.313708498984762496, 24.92405277982336997 ) ) ;
#48941=CARTESIAN_POINT ( 'NONE',  ( -3.313708498984757167, 7.999999999999991118, 17.23655278392014978 ) ) ;
#48942=DIRECTION ( 'NONE',  ( -0.000000000000000000, -0.000000000000000000, 1.000000000000000000 ) ) ;
#48963=CARTESIAN_POINT ( 'NONE',  ( -2.977408999572647819, 7.188101187499992051, 20.70530278187175810 ) ) ;
#48972=CARTESIAN_POINT ( 'NONE',  ( -5.656854249492373476, -5.656854249492376141, 16.20530278392014978 ) ) ;
#48981=ORIENTED_EDGE ( 'NONE', *, *, #30709, .T. ) ;
#48985=CARTESIAN_POINT ( 'NONE',  ( -5.082755093536317936, -5.082755093536320601, 21.17405278187175455 ) ) ;
#49005=CARTESIAN_POINT ( 'NONE',  ( -3.313708498984757167, 7.999999999999991118, 23.23655278392014623 ) ) ;
#49012=CARTESIAN_POINT ( 'NONE',  ( 7.188101187499991163, 2.977408999572648707, 23.70530278187175810 ) ) ;
#49028=CARTESIAN_POINT ( 'NONE',  ( 5.656854249492374365, 5.656854249492375253, 7.767802779823362869 ) ) ;
#49045=CARTESIAN_POINT ( 'NONE',  ( -4.898587196589407898E-16, 7.999999999999991118, 14.01155278432982421 ) ) ;
#49050=( BOUNDED_CURVE ( )  B_SPLINE_CURVE ( 2, ( #8632, #55040, #31645, #72375, #61434, #10125, #9761, #55788, #27097 ),
 .UNSPECIFIED., .F., .F. ) 
 B_SPLINE_CURVE_WITH_KNOTS ( ( 3, 2, 2, 2, 3 ),
 ( 0.5789473684210527660, 0.5855263157894737835, 0.5921052631578946901, 0.5986842105263158187, 0.6052631578947368363 ),
 .UNSPECIFIED. ) 
 CURVE ( )  GEOMETRIC_REPRESENTATION_ITEM ( )  RATIONAL_B_SPLINE_CURVE ( ( 0.9999999999999986677, 0.9238795325112880708, 1.000000000000000000, 0.9238795325112867385, 1.000000000000000000, 0.9238795325112867385, 1.000000000000000000, 0.9238795325112867385, 1.000000000000000000 ) ) 
 REPRESENTATION_ITEM ( '' )  );
#49076=CARTESIAN_POINT ( 'NONE',  ( -5.082755093536319713, 5.082755093536319713, 7.299052781871751883 ) ) ;
#49088=CARTESIAN_POINT ( 'NONE',  ( -2.977408999572648707, -7.188101187499990274, 12.64280278187175277 ) ) ;
#49102=CARTESIAN_POINT ( 'NONE',  ( 2.977408999572646486, 7.188101187499992051, 7.392802781871750994 ) ) ;
#49118=CARTESIAN_POINT ( 'NONE',  ( -5.656854249492375253, 5.656854249492375253, 29.14280277982336642 ) ) ;
#49130=CARTESIAN_POINT ( 'NONE',  ( -7.999999999999991118, 3.313708498984756723, 27.79280278432983309 ) ) ;
#49154=CARTESIAN_POINT ( 'NONE',  ( 7.188101187499992051, 8.802885111219154394E-16, 3.736552781871751883 ) ) ;
#49168=CARTESIAN_POINT ( 'NONE',  ( -7.188101187499991163, 2.977408999572646930, 26.89280278187175455 ) ) ;
#49173=CARTESIAN_POINT ( 'NONE',  ( 7.999999999999994671, 1.060658008479643977, 0.000000000000000000 ) ) ;
#49187=CARTESIAN_POINT ( 'NONE',  ( 8.000000000000014211, -3.313708498984734518, 22.48655277982336997 ) ) ;
#49192=CARTESIAN_POINT ( 'NONE',  ( 2.977408999572650927, -7.188101187499990274, 20.33030278187175810 ) ) ;
#49198=CARTESIAN_POINT ( 'NONE',  ( 7.999999999999991118, 9.797174393178815797E-16, 25.58030277982336997 ) ) ;
#49204=CARTESIAN_POINT ( 'NONE',  ( -5.656854249492373476, -5.656854249492376141, -0.2946972160798554397 ) ) ;
#49213=CARTESIAN_POINT ( 'NONE',  ( -5.656854249492375253, 5.656854249492375253, 8.142802779823362869 ) ) ;
#49218=CARTESIAN_POINT ( 'NONE',  ( -7.999988082670040690, 3.313720416314709816, 14.42405230710402186 ) ) ;
#49240=CARTESIAN_POINT ( 'NONE',  ( 8.008118988124993010, -3.317071493978877239, 27.16936528394063544 ) ) ;
#49275=CARTESIAN_POINT ( 'NONE',  ( -4.401442555609577197E-16, 7.188101187499992051, 2.611552781871750994 ) ) ;
#49301=CARTESIAN_POINT ( 'NONE',  ( 3.313708498984756279, 7.999999999999991118, 27.36155277982336642 ) ) ;
#49310=VERTEX_POINT ( 'NONE', #45620 ) ;
#49319=CARTESIAN_POINT ( 'NONE',  ( -7.999999999999989342, -3.313708498984762496, 19.11155278392014623 ) ) ;
#49322=AXIS2_PLACEMENT_3D ( 'NONE', #60429, #66460, #2722 ) ;
#49342=CARTESIAN_POINT ( 'NONE',  ( -5.082755093536317936, -5.082755093536320601, 15.17405278187175455 ) ) ;
#49352=CARTESIAN_POINT ( 'NONE',  ( -3.313708498984757167, 7.999999999999991118, 15.73655278392014267 ) ) ;
#49353=CARTESIAN_POINT ( 'NONE',  ( -7.999999999999991118, 3.313708498984757167, 18.92405278392014978 ) ) ;
#49363=CARTESIAN_POINT ( 'NONE',  ( -4.401442555609577197E-16, 7.188101187499992051, 17.61155278187175810 ) ) ;
#49371=CARTESIAN_POINT ( 'NONE',  ( 0.000000000000000000, 0.000000000000000000, 30.00000000000000000 ) ) ;
#49381=CARTESIAN_POINT ( 'NONE',  ( -4.898587196589407898E-16, 7.999999999999991118, 26.14280278392014623 ) ) ;
#49388=CARTESIAN_POINT ( 'NONE',  ( -4.401442555609577197E-16, 7.188101187499992051, 13.48655278187175455 ) ) ;
#49404=CARTESIAN_POINT ( 'NONE',  ( 7.999999999999992895, -3.313708498984756279, 8.986552779823366421 ) ) ;
#49405=CARTESIAN_POINT ( 'NONE',  ( 7.999994293450985339, 3.313714205533765611, 21.36155301224097158 ) ) ;
#49414=ORIENTED_EDGE ( 'NONE', *, *, #20996, .F. ) ;
#49418=CARTESIAN_POINT ( 'NONE',  ( -7.188101187499992051, 0.000000000000000000, 28.67405278187175810 ) ) ;
#49422=CARTESIAN_POINT ( 'NONE',  ( 7.999999999999992895, -3.313708498984756279, 13.54280278432982598 ) ) ;
#49440=EDGE_CURVE ( 'NONE', #27289, #19989, #34034, .T. ) ;
#49450=VERTEX_POINT ( 'NONE', #14614 ) ;
#49457=CARTESIAN_POINT ( 'NONE',  ( 7.188101187499992051, 8.802885111219154394E-16, 6.736552781871754547 ) ) ;
#49470=CARTESIAN_POINT ( 'NONE',  ( 2.977408999572650927, -7.188101187499990274, 9.830302781871752771 ) ) ;
#49479=DIRECTION ( 'NONE',  ( -0.000000000000000000, -0.000000000000000000, 1.000000000000000000 ) ) ;
#49482=CARTESIAN_POINT ( 'NONE',  ( 7.188101187499992051, 8.802885111219154394E-16, 4.111552781871752771 ) ) ;
#49505=CARTESIAN_POINT ( 'NONE',  ( 7.999999999999992895, -3.313708498984756279, 25.67405278392014978 ) ) ;
#49511=CARTESIAN_POINT ( 'NONE',  ( -7.999999999999991118, 3.313708498984756723, 3.924052783920144893 ) ) ;
#49535=CARTESIAN_POINT ( 'NONE',  ( 2.977408999572646486, 7.188101187499992051, 4.017802781871751883 ) ) ;
#49550=CARTESIAN_POINT ( 'NONE',  ( -7.188101187499992051, 0.000000000000000000, 25.48655278187175810 ) ) ;
#49567=CARTESIAN_POINT ( 'NONE',  ( 7.999999999843520726, -5.003525229023116430E-05, 24.26780136833107093 ) ) ;
#49573=CARTESIAN_POINT ( 'NONE',  ( -7.188101187499992051, 0.000000000000000000, 24.36155278187175810 ) ) ;
#49594=CARTESIAN_POINT ( 'NONE',  ( -7.999999999999989342, -3.313708498984762496, 6.924052779823366421 ) ) ;
#49602=CARTESIAN_POINT ( 'NONE',  ( 7.999999999999991118, 3.313708498984758055, 1.674052779823364423 ) ) ;
#49625=CARTESIAN_POINT ( 'NONE',  ( -3.317071493978880348, -8.008118988124989457, 26.79436528394063188 ) ) ;
#49645=CARTESIAN_POINT ( 'NONE',  ( 7.999999999999991118, 3.313708498984758055, 13.67405277982336465 ) ) ;
#49648=CARTESIAN_POINT ( 'NONE',  ( 7.999999999999992895, -3.313708498984756279, 9.174052783920146226 ) ) ;
#49659=CARTESIAN_POINT ( 'NONE',  ( 2.977408999572646486, 7.188101187499991163, 25.39280278187176165 ) ) ;
#49661=CARTESIAN_POINT ( 'NONE',  ( -5.656854249492375253, 5.656854249492375253, 15.83030278392014800 ) ) ;
#49687=CARTESIAN_POINT ( 'NONE',  ( 3.313708498984762496, -7.999999999999989342, 25.29905277982336642 ) ) ;
#49706=CARTESIAN_POINT ( 'NONE',  ( 7.999999999999992895, -3.313708498984756279, 18.17405278392014623 ) ) ;
#49726=CARTESIAN_POINT ( 'NONE',  ( -5.082755093536319713, 5.082755093536319713, 14.79905278187175455 ) ) ;
#49737=CARTESIAN_POINT ( 'NONE',  ( -3.313708498984757167, 7.999999999999991118, 6.736552783920144449 ) ) ;
#49748=CARTESIAN_POINT ( 'NONE',  ( 1.320432766682872962E-15, -7.188101187499992051, 13.86155278187175455 ) ) ;
#49773=CARTESIAN_POINT ( 'NONE',  ( -7.188101187499992051, 0.000000000000000000, 13.86155278187175455 ) ) ;
#49790=CARTESIAN_POINT ( 'NONE',  ( -5.656854249492375253, 5.656854249492375253, 8.142802779823362869 ) ) ;
#49802=DIRECTION ( 'NONE',  ( 0.000000000000000000, 0.000000000000000000, 1.000000000000000000 ) ) ;
#49804=CARTESIAN_POINT ( 'NONE',  ( 7.999999999999992895, -3.313708498984756279, 10.54280278432982598 ) ) ;
#49821=CARTESIAN_POINT ( 'NONE',  ( -5.656854249492373476, -5.656854249492376141, 19.01780277982336642 ) ) ;
#49833=CARTESIAN_POINT ( 'NONE',  ( 5.082755093536320601, -5.082755093536318824, 9.549052781871754547 ) ) ;
#49846=CARTESIAN_POINT ( 'NONE',  ( -5.082755093536319713, 5.082755093536319713, 10.67405278187175455 ) ) ;
#49860=CARTESIAN_POINT ( 'NONE',  ( -7.188101187499992051, 0.000000000000000000, 3.361552781871751883 ) ) ;
#49877=CARTESIAN_POINT ( 'NONE',  ( 7.999999999999991118, 9.797174393178815797E-16, 25.58030277982336997 ) ) ;
#49882=LINE ( 'NONE', #66862, #25327 ) ;
#49888=CARTESIAN_POINT ( 'NONE',  ( 3.313708498984762496, -7.999999999999989342, 2.986552783920144449 ) ) ;
#49900=CARTESIAN_POINT ( 'NONE',  ( -7.188101187499992051, 0.000000000000000000, 28.86155278187175810 ) ) ;
#49910=CARTESIAN_POINT ( 'NONE',  ( 5.082755093536320601, -5.082755093536318824, 3.549052781871751883 ) ) ;
#49923=CARTESIAN_POINT ( 'NONE',  ( 1.320432766682872962E-15, -7.188101187499992051, 25.86155278187175810 ) ) ;
#49949=CARTESIAN_POINT ( 'NONE',  ( -2.977408999572647819, 7.188101187499992051, 22.58030278187175455 ) ) ;
#49967=CARTESIAN_POINT ( 'NONE',  ( -7.999999999999991118, 0.000000000000000000, 6.830302779823365533 ) ) ;
#49994=CARTESIAN_POINT ( 'NONE',  ( 5.662595241051936235, -5.662595241051934458, 18.07561528394063188 ) ) ;
#50012=AXIS2_PLACEMENT_3D ( 'NONE', #66928, #45039, #26929 ) ;
#50018=B_SPLINE_CURVE_WITH_KNOTS ( 'NONE', 3,
 ( #68125, #16419, #39453, #62452, #5134, #28127, #22454, #65790, #7351 ),
 .UNSPECIFIED., .F., .F.,
 ( 4, 2, 2, 1, 4 ),
 ( 0.5000000000000000000, 0.5566067453737802984, 0.5707584317172254007, 0.5849101180606703920, 0.6132134907475605967 ),
 .UNSPECIFIED. ) ;
#50028=CARTESIAN_POINT ( 'NONE',  ( 1.320432766682872962E-15, -7.188101187499992051, 24.73655278187175810 ) ) ;
#50053=CARTESIAN_POINT ( 'NONE',  ( -3.313708498984757167, 7.999999999999991118, 27.54905277982337353 ) ) ;
#50055=CARTESIAN_POINT ( 'NONE',  ( -7.999999999999991118, 0.000000000000000000, 9.830302779823364645 ) ) ;
#50074=CARTESIAN_POINT ( 'NONE',  ( -7.999999999999991118, 3.313708498984756723, 20.42405278392014978 ) ) ;
#50094=CARTESIAN_POINT ( 'NONE',  ( -7.188101187499990274, -2.977408999572651815, 18.08030278187175455 ) ) ;
#50108=CARTESIAN_POINT ( 'NONE',  ( -7.999999999999991118, 0.000000000000000000, 7.017802783920144449 ) ) ;
#50119=CARTESIAN_POINT ( 'NONE',  ( -7.188101187499991163, 2.977408999572646930, 13.39280278187175455 ) ) ;
#50143=CARTESIAN_POINT ( 'NONE',  ( 2.977408999572650927, -7.188101187499990274, 18.83030278187175099 ) ) ;
#50159=CARTESIAN_POINT ( 'NONE',  ( -4.898587196589407898E-16, 7.999999999999991118, 10.95530277982336642 ) ) ;
#50160=CARTESIAN_POINT ( 'NONE',  ( -3.313708498984757611, 7.999999999999991118, 21.73655278392014623 ) ) ;
#50174=CARTESIAN_POINT ( 'NONE',  ( -3.313708498984758943, -7.999999999999989342, 14.66780278432982598 ) ) ;
#50204=CARTESIAN_POINT ( 'NONE',  ( 7.188101187499991163, 2.977408999572648707, 27.83030278187176165 ) ) ;
#50216=CARTESIAN_POINT ( 'NONE',  ( -7.188101187499992051, 0.000000000000000000, 7.861552781871751883 ) ) ;
#50229=DIRECTION ( 'NONE',  ( 0.000000000000000000, 0.000000000000000000, -1.000000000000000000 ) ) ;
#50244=CARTESIAN_POINT ( 'NONE',  ( 5.656854249492376141, -5.656854249492374365, 25.39280277982336642 ) ) ;
#50256=CARTESIAN_POINT ( 'NONE',  ( 3.313708498984762496, -7.999999999999989342, -0.01344721607985516210 ) ) ;
#50257=CARTESIAN_POINT ( 'NONE',  ( 0.000000000000000000, 15.08051212944140218, 15.04081104653146994 ) ) ;
#50262=ADVANCED_FACE ( 'NONE', ( #66215 ), #36813, .F. ) ;
#50265=CARTESIAN_POINT ( 'NONE',  ( -7.999999999999981348, 3.313708498984767381, 24.73655277982336287 ) ) ;
#50293=CARTESIAN_POINT ( 'NONE',  ( -7.188101187499991163, 2.977408999572646930, 17.89280278187175455 ) ) ;
#50316=CARTESIAN_POINT ( 'NONE',  ( -4.401442555609577197E-16, 7.188101187499992051, 22.48655278187175455 ) ) ;
#50325=CARTESIAN_POINT ( 'NONE',  ( 3.459103461385761413, -7.213501455148458419, -0.0001169852011744028255 ) ) ;
#50333=CARTESIAN_POINT ( 'NONE',  ( -4.898587196589407898E-16, 7.999999999999991118, 6.455302779823365533 ) ) ;
#50349=CARTESIAN_POINT ( 'NONE',  ( -7.999999999835898379, -3.436314075762838161E-05, 19.01908381112063751 ) ) ;
#50362=CARTESIAN_POINT ( 'NONE',  ( 8.008118988124991233, 9.807117285998411148E-16, 18.26311528394063188 ) ) ;
#50377=ORIENTED_EDGE ( 'NONE', *, *, #7143, .T. ) ;
#50400=CARTESIAN_POINT ( 'NONE',  ( 7.188101187499993827, -2.977408999572645598, 22.01780278187175810 ) ) ;
#50402=FACE_OUTER_BOUND ( 'NONE', #70405, .T. ) ;
#50407=FACE_OUTER_BOUND ( 'NONE', #46380, .T. ) ;
#50423=CARTESIAN_POINT ( 'NONE',  ( 2.977408999572650927, -7.188101187499990274, 0.8303027818717529929 ) ) ;
#50440=CARTESIAN_POINT ( 'NONE',  ( -7.999999999999991118, 0.000000000000000000, 10.01780278392014623 ) ) ;
#50460=CARTESIAN_POINT ( 'NONE',  ( -2.977408999572647819, 7.188101187499992051, 16.20530278187175099 ) ) ;
#50484=CARTESIAN_POINT ( 'NONE',  ( 5.082755093536318824, 5.082755093536319713, 11.42405278187175455 ) ) ;
#50495=AXIS2_PLACEMENT_3D ( 'NONE', #30684, #36350, #23541 ) ;
#50509=CARTESIAN_POINT ( 'NONE',  ( 1.320432766682872962E-15, -7.188101187499992051, 18.73655278187175455 ) ) ;
#50524=CARTESIAN_POINT ( 'NONE',  ( -6.062585341144163031, -5.219679969245603957, 1.000679773946673290 ) ) ;
#50542=CARTESIAN_POINT ( 'NONE',  ( -3.313708498984758943, -7.999999999999989342, 10.16780278432982598 ) ) ;
#50569=CARTESIAN_POINT ( 'NONE',  ( 3.313708498984756279, 7.999999999999991118, 16.86155277982336642 ) ) ;
#50572=CARTESIAN_POINT ( 'NONE',  ( -5.082755093536317936, -5.082755093536320601, 1.674052781871753659 ) ) ;
#50576=CARTESIAN_POINT ( 'NONE',  ( -7.999999999999968914, 3.313708498984778039, 20.23655277982336287 ) ) ;
#50584=CARTESIAN_POINT ( 'NONE',  ( -7.188101187499990274, -2.977408999572651371, 6.455302781871754547 ) ) ;
#50598=CARTESIAN_POINT ( 'NONE',  ( -5.272366635369878374, -4.893143551702761052, 0.5406094755204297053 ) ) ;
#50614=CARTESIAN_POINT ( 'NONE',  ( 5.656854249492376141, -5.656854249492374365, 26.89280277982336642 ) ) ;
#50627=CARTESIAN_POINT ( 'NONE',  ( 7.999999999999992895, -3.313708498984756279, 1.674052783920142895 ) ) ;
#50637=CARTESIAN_POINT ( 'NONE',  ( -7.999999999999991118, 0.000000000000000000, 29.33030277982336642 ) ) ;
#50660=CARTESIAN_POINT ( 'NONE',  ( 7.188101187499992051, 8.802885111219154394E-16, 20.23655278187175099 ) ) ;
#50680=CARTESIAN_POINT ( 'NONE',  ( 7.999999999999991118, 9.797174393178815797E-16, 7.580302779823366421 ) ) ;
#50683=CARTESIAN_POINT ( 'NONE',  ( -7.188101187499990274, -2.977408999572651815, 15.45530278187175632 ) ) ;
#50685=CARTESIAN_POINT ( 'NONE',  ( -7.999999999929542582, -2.214810345207895024E-05, 22.01864141485938831 ) ) ;
#50703=CARTESIAN_POINT ( 'NONE',  ( 5.656854249492376141, -5.656854249492374365, 1.392802779823364201 ) ) ;
#50710=CARTESIAN_POINT ( 'NONE',  ( -7.999999999999989342, -3.313708498984762496, 14.61155278392014800 ) ) ;
#50715=CARTESIAN_POINT ( 'NONE',  ( -7.999999999999989342, -3.313708498984762496, 10.11155278392014623 ) ) ;
#50734=CARTESIAN_POINT ( 'NONE',  ( -5.662595241051933570, -5.662595241051936235, 22.20061528394063188 ) ) ;
#50765=ORIENTED_EDGE ( 'NONE', *, *, #585, .T. ) ;
#50767=CARTESIAN_POINT ( 'NONE',  ( 5.082755093536318824, 5.082755093536319713, 23.79905278187175455 ) ) ;
#50795=CARTESIAN_POINT ( 'NONE',  ( 3.313708498984762496, -7.999999999999989342, 23.79905277982336642 ) ) ;
#50816=CARTESIAN_POINT ( 'NONE',  ( 7.999999999999992895, -3.313708498984756279, 13.67405278392014978 ) ) ;
#50818=EDGE_LOOP ( 'NONE', ( #51389, #39732, #31832, #40515 ) ) ;
#50828=CARTESIAN_POINT ( 'NONE',  ( 7.999999999999991118, 9.797174393178815797E-16, 28.58030277982336642 ) ) ;
#50848=DIRECTION ( 'NONE',  ( 0.000000000000000000, -1.000000000000000000, 0.000000000000000000 ) ) ;
#50849=AXIS2_PLACEMENT_3D ( 'NONE', #69380, #71583, #31611 ) ;
#50859=EDGE_LOOP ( 'NONE', ( #47381, #22937, #44126 ) ) ;
#50861=CARTESIAN_POINT ( 'NONE',  ( -4.401442555609577197E-16, 7.188101187499992051, 11.61155278187175632 ) ) ;
#50886=CARTESIAN_POINT ( 'NONE',  ( 5.082755093536318824, 5.082755093536319713, 16.29905278187175455 ) ) ;
#50890=ORIENTED_EDGE ( 'NONE', *, *, #12287, .F. ) ;
#50901=CARTESIAN_POINT ( 'NONE',  ( -7.999999999999991118, 0.000000000000000000, 5.330302779823363757 ) ) ;
#50917=CARTESIAN_POINT ( 'NONE',  ( -5.656854249492373476, -5.656854249492376141, 7.074052784329822430 ) ) ;
#50918=AXIS2_PLACEMENT_3D ( 'NONE', #70769, #19083, #8138 ) ;
#50920=CARTESIAN_POINT ( 'NONE',  ( 0.000000000000000000, 0.000000000000000000, 30.00000000000000000 ) ) ;
#50943=CARTESIAN_POINT ( 'NONE',  ( -7.999984110674186688, 3.313724388310563373, 9.924052148183214683 ) ) ;
#50962=CARTESIAN_POINT ( 'NONE',  ( 2.977408999572650927, -7.188101187499990274, 3.830302781871751883 ) ) ;
#50991=CARTESIAN_POINT ( 'NONE',  ( -7.999999999999991118, 3.313708498984756723, 18.73655277982336642 ) ) ;
#51000=ORIENTED_EDGE ( 'NONE', *, *, #33764, .T. ) ;
#51007=CARTESIAN_POINT ( 'NONE',  ( -4.898587196589407898E-16, 7.999999999999991118, 23.01155278432982598 ) ) ;
#51041=CARTESIAN_POINT ( 'NONE',  ( 5.082755093536320601, -5.082755093536318824, 18.54905278187175455 ) ) ;
#51061=CARTESIAN_POINT ( 'NONE',  ( 5.082755093536318824, 5.082755093536319713, 19.29905278187175455 ) ) ;
#51081=CARTESIAN_POINT ( 'NONE',  ( 7.999999999999992895, -3.313708498984756279, 4.486552779823363757 ) ) ;
#51086=CARTESIAN_POINT ( 'NONE',  ( -3.313708498984757611, 7.999999999999991118, 11.04905277982336642 ) ) ;
#51111=CARTESIAN_POINT ( 'NONE',  ( -5.662595241051935346, 5.662595241051935346, 18.82561528394063188 ) ) ;
#51144=CARTESIAN_POINT ( 'NONE',  ( -2.977408999572647819, 7.188101187499991163, 21.08030278187175810 ) ) ;
#51151=LINE ( 'NONE', #39830, #23295 ) ;
#51169=CARTESIAN_POINT ( 'NONE',  ( 3.313708498984762496, -7.999999999999989342, 19.29905277982336642 ) ) ;
#51172=VERTEX_POINT ( 'NONE', #67541 ) ;
#51188=CARTESIAN_POINT ( 'NONE',  ( -5.656854249492373476, -5.656854249492376141, 11.70530278392014445 ) ) ;
#51235=CARTESIAN_POINT ( 'NONE',  ( -7.188101187499992051, 0.000000000000000000, 14.98655278187175455 ) ) ;
#51260=CARTESIAN_POINT ( 'NONE',  ( -2.977408999572648707, -7.188101187499990274, 11.14280278187175810 ) ) ;
#51262=CARTESIAN_POINT ( 'NONE',  ( 5.656854249492376141, -5.656854249492374365, 1.580302783920146226 ) ) ;
#51265=CARTESIAN_POINT ( 'NONE',  ( -7.999999999971585396, 1.424435121157765920E-05, 7.017269882810325932 ) ) ;
#51274=CARTESIAN_POINT ( 'NONE',  ( 5.656854249492376141, -5.656854249492374365, 5.892802779823364645 ) ) ;
#51291=CARTESIAN_POINT ( 'NONE',  ( -7.999999999999989342, -3.313708498984762496, 5.480302784329825094 ) ) ;
#51294=DIRECTION ( 'NONE',  ( -0.000000000000000000, -0.000000000000000000, 1.000000000000000000 ) ) ;
#51318=LINE ( 'NONE', #74328, #68349 ) ;
#51321=CARTESIAN_POINT ( 'NONE',  ( 5.082755093536320601, -5.082755093536318824, 2.049052781871754103 ) ) ;
#51335=CARTESIAN_POINT ( 'NONE',  ( -4.401442555609577197E-16, 7.188101187499992051, 5.986552781871753659 ) ) ;
#51350=CARTESIAN_POINT ( 'NONE',  ( 5.656854249492374365, 5.656854249492375253, 28.76780277982336642 ) ) ;
#51361=CARTESIAN_POINT ( 'NONE',  ( -4.898587196589407898E-16, 7.999999999999991118, 18.45530277982336642 ) ) ;
#51370=( BOUNDED_SURFACE ( )  B_SPLINE_SURFACE ( 1, 2, ( 
 ( #23416, #52837, #34769, #70194, #18502, #41511, #68696, #63778, #69817, #64154, #63034, #29458, #23791, #11359, #52467, #46795, #74352, #11729, #804, #18133, #5703, #69445, #22662, #12463, #40770, #69075, #40405, #57771, #64527, #52104, #57021, #63403, #6076, #5334, #12095, #45681, #40032, #29084, #436, #46431, #17756, #14301, #19969, #25987, #24879, #53578, #60335, #13922, #1892, #66371, #70553, #43353, #19231, #31294, #13189, #49012, #2258, #24523, #8285, #64888, #18869, #72022, #65996, #71276, #53209, #8663, #30192, #19595, #53945, #36594, #36227, #59244, #7555, #20336, #31678, #54697, #42975, #42238, #54325, #70918, #37337, #65251, #7186, #36961, #3006, #13556, #71648, #35860, #30562, #59605, #2636, #30923, #42611, #7918, #59967, #25624, #65625, #25252, #47898, #1543, #47528, #48638, #41875, #58875, #48269, #73158, #4138, #50143, #50509, #45232, #3754, #4503, #66749, #44863, #67868, #33561, #21466, #14677, #9037, #72407, #72789, #37716, #55444, #38462, #61465, #44488, #15800, #60716, #27496, #55820, #16161, #67128, #56565, #4880, #50886, #26366, #67501, #73523, #21830, #20718, #38835, #56191, #43735, #61838, #39202, #32050, #44119, #10157, #33194, #15055, #27128, #55070, #62204, #10529, #26755, #38089, #15423, #27875, #9790, #73900, #49773, #61086, #3379, #22205, #49388, #9415, #32433, #21096, #32812, #35418, #46710, #52387, #58428, #57312, #11276, #18050, #46345, #34308, #24068, #28252, #1091, #51636, #63691, #45599, #6736, #34681, #56936, #40689, #22579, #51260, #29740, #23706, #52015, #11646, #68989, #68614, #16923, #39946, #52755, #64075, #41065, #723, #65876, #12018, #68244, #69735, #5252, #57687, #69362, #62951, #12383, #16536, #353, #17672, #39577, #5623, #23333, #5995, #62572, #10903, #28623, #33937, #22967, #28997, #45974, #35051, #74270, #17298, #40316, #63320, #58063, #6374, #29380, #36145, #7475, #2919, #47451, #64447, #30480, #53129, #60249, #8575, #64807, #14215, #1462, #59889, #71193, #12748, #7104, #37254, #65165, #65544, #48186, #35779, #31214, #19149, #41798, #31591, #58794, #19512, #24443, #65909, #42530, #13476, #25169, #53863, #18421, #54612, #47814, #41435, #53497, #70475, #13836, #30112, #47078, #70115, #36881, #1814, #18793, #13109, #59166, #24800, #19884, #70837, #42152, #2548, #36515, #8202, #59524, #30842, #7837, #2175, #54239, #25539, #48552, #71562, #42890, #3664, #8950, #50423, #21003, #32346, #31962, #10441, #9704 ),
 ( #66284, #21375, #60628, #43269, #73437, #20249, #14965, #61000, #56473, #26280, #14591, #9326, #54987, #39113, #62117, #43647, #67787, #3294, #38753, #50053, #37630, #49301, #16079, #44029, #44399, #27042, #72318, #10071, #72702, #20631, #33471, #66658, #73069, #38002, #44773, #67413, #67038, #4050, #32725, #71937, #25907, #26664, #55359, #49687, #15337, #15711, #38372, #48924, #61377, #61753, #55733, #33106, #56103, #4412, #27407, #21745, #16823, #12295, #34959, #50795, #40599, #28530, #63227, #68521, #51538, #16449, #17957, #74555, #40975, #69270, #57215, #62481, #29286, #22867, #11188, #10811, #63982, #11554, #260, #45881, #68895, #46251, #11927, #33845, #51922, #62852, #5904, #45140, #23243, #39485, #22116, #52296, #73808, #34588, #17205, #5529, #56843, #5164, #28158, #35330, #632, #23613, #57974, #34213, #17581, #69643, #6279, #51169, #40224, #57594, #74178, #46623, #4789, #28904, #63600, #27782, #45503, #68152, #22482, #39851, #29649, #30022, #71470, #47361, #24712, #70387, #19063, #41343, #6646, #58342, #13749, #13386, #65452, #19796, #13019, #7750, #2085, #12656, #70745, #23981, #71103, #42065, #18702, #64353, #59074, #25450, #53409, #42436, #41709, #35687, #52664, #65073, #1000, #46989, #58702, #7013, #30755, #48465, #36792, #59802, #42802, #64723, #1367, #8115, #36424, #24352, #14126, #18328, #65819, #36057, #53776, #53036, #70022, #47724, #7383, #25077, #30390, #1732, #59438, #31120, #48094, #19423, #54148, #2457, #54894, #2827, #67326, #61665, #3578, #31501, #31873, #60537, #3960, #3205, #8863, #20537, #44311, #43551, #8481, #38284, #21288, #72222, #72982, #15623, #66194, #14874, #32636, #32255, #43937, #9233, #61289, #9616, #66946, #66565, #26193, #54522, #25819, #20916, #48838, #67700, #37913, #15250, #26570, #72610, #38663, #37160, #49213, #26949, #14498, #9984, #33015, #56016, #55645, #60162, #71844, #20161, #60910, #43178, #55273, #49594, #49967, #4328, #27317, #37537, #50333, #73355, #21659, #44684, #57881, #34875, #52209, #27694, #22771, #28812, #176, #22031, #68804, #57511, #45056, #17116, #5817, #10355, #62031, #40138, #23152, #51081, #51830, #46164, #68068, #68430, #11472, #11104, #45794, #62761, #63144, #34506, #69182, #22393, #39395, #33379, #56380, #74463, #4701, #46538, #45414, #17493, #5442, #51450, #40512, #15997, #5076, #63516, #16357, #11839, #6188, #29197, #542, #39026, #50703, #73721, #74095, #62394, #56756, #39759, #34127 ) ),
 .UNSPECIFIED., .F., .F., .F. ) 
 B_SPLINE_SURFACE_WITH_KNOTS ( ( 2, 2 ),
 ( 3, 2, 2, 2, 2, 2, 2, 2, 2, 2, 2, 2, 2, 2, 2, 2, 2, 2, 2, 2, 2, 2, 2, 2, 2, 2, 2, 2, 2, 2, 2, 2, 2, 2, 2, 2, 2, 2, 2, 2, 2, 2, 2, 2, 2, 2, 2, 2, 2, 2, 2, 2, 2, 2, 2, 2, 2, 2, 2, 2, 2, 2, 2, 2, 2, 2, 2, 2, 2, 2, 2, 2, 2, 2, 2, 2, 2, 2, 2, 2, 2, 2, 2, 2, 2, 2, 2, 2, 2, 2, 2, 2, 2, 2, 2, 2, 2, 2, 2, 2, 2, 2, 2, 2, 2, 2, 2, 2, 2, 2, 2, 2, 2, 2, 2, 2, 2, 2, 2, 2, 2, 2, 2, 2, 2, 2, 2, 2, 2, 2, 2, 2, 2, 2, 2, 2, 2, 2, 2, 2, 2, 2, 2, 2, 2, 2, 2, 2, 2, 2, 2, 2, 3 ),
 ( 0.000000000000000000, 1.000000000000000000 ),
 ( 0.000000000000000000, 0.006578947368421052266, 0.01315789473684210453, 0.01973684210526315680, 0.02631578947368420907, 0.03289473684210526133, 0.03947368421052631360, 0.04605263157894736586, 0.05263157894736841813, 0.05921052631578947040, 0.06578947368421052266, 0.07236842105263158187, 0.07894736842105262720, 0.08552631578947368640, 0.09210526315789473173, 0.09868421052631579093, 0.1052631578947368363, 0.1118421052631578955, 0.1184210526315789408, 0.1250000000000000000, 0.1315789473684210453, 0.1381578947368421184, 0.1447368421052631637, 0.1513157894736842091, 0.1578947368421052544, 0.1644736842105263275, 0.1710526315789473728, 0.1776315789473684181, 0.1842105263157894635, 0.1907894736842105365, 0.1973684210526315819, 0.2039473684210526272, 0.2105263157894736725, 0.2171052631578947456, 0.2236842105263157909, 0.2302631578947368363, 0.2368421052631578816, 0.2434210526315789547, 0.2500000000000000000, 0.2565789473684210731, 0.2631578947368420907, 0.2697368421052631637, 0.2763157894736842368, 0.2828947368421052544, 0.2894736842105263275, 0.2960526315789473450, 0.3026315789473684181, 0.3092105263157894912, 0.3157894736842105088, 0.3223684210526315819, 0.3289473684210526550, 0.3355263157894736725, 0.3421052631578947456, 0.3486842105263157632, 0.3552631578947368363, 0.3618421052631579093, 0.3684210526315789269, 0.3750000000000000000, 0.3815789473684210731, 0.3881578947368420907, 0.3947368421052631637, 0.4013157894736842368, 0.4078947368421052544, 0.4144736842105263275, 0.4210526315789473450, 0.4276315789473684181, 0.4342105263157894912, 0.4407894736842105088, 0.4473684210526315819, 0.4539473684210526550, 0.4605263157894736725, 0.4671052631578947456, 0.4736842105263157632, 0.4802631578947368363, 0.4868421052631579093, 0.4934210526315789269, 0.5000000000000000000, 0.5065789473684210176, 0.5131578947368421462, 0.5197368421052631637, 0.5263157894736841813, 0.5328947368421053099, 0.5394736842105263275, 0.5460526315789473450, 0.5526315789473684736, 0.5592105263157894912, 0.5657894736842105088, 0.5723684210526315264, 0.5789473684210526550, 0.5855263157894736725, 0.5921052631578946901, 0.5986842105263158187, 0.6052631578947368363, 0.6118421052631578538, 0.6184210526315789824, 0.6250000000000000000, 0.6315789473684210176, 0.6381578947368421462, 0.6447368421052631637, 0.6513157894736841813, 0.6578947368421053099, 0.6644736842105263275, 0.6710526315789473450, 0.6776315789473684736, 0.6842105263157894912, 0.6907894736842105088, 0.6973684210526315264, 0.7039473684210526550, 0.7105263157894736725, 0.7171052631578946901, 0.7236842105263158187, 0.7302631578947368363, 0.7368421052631578538, 0.7434210526315789824, 0.7500000000000000000, 0.7565789473684210176, 0.7631578947368421462, 0.7697368421052631637, 0.7763157894736841813, 0.7828947368421053099, 0.7894736842105263275, 0.7960526315789473450, 0.8026315789473684736, 0.8092105263157894912, 0.8157894736842105088, 0.8223684210526315264, 0.8289473684210526550, 0.8355263157894736725, 0.8421052631578946901, 0.8486842105263158187, 0.8552631578947368363, 0.8618421052631578538, 0.8684210526315789824, 0.8750000000000000000, 0.8815789473684210176, 0.8881578947368421462, 0.8947368421052631637, 0.9013157894736841813, 0.9078947368421053099, 0.9144736842105263275, 0.9210526315789473450, 0.9276315789473684736, 0.9342105263157894912, 0.9407894736842105088, 0.9473684210526315264, 0.9539473684210526550, 0.9605263157894736725, 0.9671052631578946901, 0.9736842105263158187, 0.9802631578947368363, 0.9868421052631578538, 0.9934210526315789824, 0.9940576599040155115 ),
 .UNSPECIFIED. ) 
 GEOMETRIC_REPRESENTATION_ITEM ( )  RATIONAL_B_SPLINE_SURFACE ( (
 ( 1.000000000000000000, 0.9238795325112867385, 1.000000000000000000, 0.9238795325112867385, 1.000000000000000000, 0.9238795325112867385, 1.000000000000000000, 0.9238795325112867385, 1.000000000000000000, 0.9238795325112867385, 1.000000000000000000, 0.9238795325112867385, 1.000000000000000000, 0.9238795325112867385, 1.000000000000000000, 0.9238795325112867385, 1.000000000000000000, 0.9238795325112867385, 1.000000000000000000, 0.9238795325112867385, 1.000000000000000000, 0.9238795325112867385, 1.000000000000000000, 0.9238795325112867385, 1.000000000000000000, 0.9238795325112867385, 1.000000000000000000, 0.9238795325112867385, 1.000000000000000000, 0.9238795325112867385, 1.000000000000000000, 0.9238795325112867385, 1.000000000000000000, 0.9238795325112867385, 1.000000000000000000, 0.9238795325112867385, 1.000000000000000000, 0.9238795325112867385, 1.000000000000000000, 0.9238795325112867385, 1.000000000000000000, 0.9238795325112867385, 1.000000000000000000, 0.9238795325112867385, 1.000000000000000000, 0.9238795325112867385, 1.000000000000000000, 0.9238795325112867385, 1.000000000000000000, 0.9238795325112867385, 1.000000000000000000, 0.9238795325112867385, 1.000000000000000000, 0.9238795325112867385, 1.000000000000000000, 0.9238795325112867385, 1.000000000000000000, 0.9238795325112867385, 1.000000000000000000, 0.9238795325112867385, 1.000000000000000000, 0.9238795325112867385, 1.000000000000000000, 0.9238795325112867385, 1.000000000000000000, 0.9238795325112867385, 1.000000000000000000, 0.9238795325112867385, 1.000000000000000000, 0.9238795325112867385, 1.000000000000000000, 0.9238795325112867385, 1.000000000000000000, 0.9238795325112867385, 1.000000000000000000, 0.9238795325112867385, 1.000000000000000000, 0.9238795325112867385, 1.000000000000000000, 0.9238795325112867385, 1.000000000000000000, 0.9238795325112867385, 1.000000000000000000, 0.9238795325112867385, 1.000000000000000000, 0.9238795325112867385, 1.000000000000000000, 0.9238795325112867385, 1.000000000000000000, 0.9238795325112867385, 1.000000000000000000, 0.9238795325112867385, 1.000000000000000000, 0.9238795325112867385, 1.000000000000000000, 0.9238795325112867385, 1.000000000000000000, 0.9238795325112867385, 1.000000000000000000, 0.9238795325112867385, 1.000000000000000000, 0.9238795325112867385, 1.000000000000000000, 0.9238795325112867385, 1.000000000000000000, 0.9238795325112867385, 1.000000000000000000, 0.9238795325112867385, 1.000000000000000000, 0.9238795325112867385, 1.000000000000000000, 0.9238795325112867385, 1.000000000000000000, 0.9238795325112867385, 1.000000000000000000, 0.9238795325112867385, 1.000000000000000000, 0.9238795325112867385, 1.000000000000000000, 0.9238795325112867385, 1.000000000000000000, 0.9238795325112867385, 1.000000000000000000, 0.9238795325112867385, 1.000000000000000000, 0.9238795325112867385, 1.000000000000000000, 0.9238795325112867385, 1.000000000000000000, 0.9238795325112867385, 1.000000000000000000, 0.9238795325112867385, 1.000000000000000000, 0.9238795325112867385, 1.000000000000000000, 0.9238795325112867385, 1.000000000000000000, 0.9238795325112867385, 1.000000000000000000, 0.9238795325112867385, 1.000000000000000000, 0.9238795325112867385, 1.000000000000000000, 0.9238795325112867385, 1.000000000000000000, 0.9238795325112867385, 1.000000000000000000, 0.9238795325112867385, 1.000000000000000000, 0.9238795325112867385, 1.000000000000000000, 0.9238795325112867385, 1.000000000000000000, 0.9238795325112867385, 1.000000000000000000, 0.9238795325112867385, 1.000000000000000000, 0.9238795325112867385, 1.000000000000000000, 0.9238795325112867385, 1.000000000000000000, 0.9238795325112867385, 1.000000000000000000, 0.9238795325112867385, 1.000000000000000000, 0.9238795325112867385, 1.000000000000000000, 0.9238795325112867385, 1.000000000000000000, 0.9238795325112867385, 1.000000000000000000, 0.9238795325112867385, 1.000000000000000000, 0.9238795325112867385, 1.000000000000000000, 0.9238795325112867385, 1.000000000000000000, 0.9238795325112867385, 1.000000000000000000, 0.9238795325112867385, 1.000000000000000000, 0.9238795325112867385, 1.000000000000000000, 0.9238795325112867385, 1.000000000000000000, 0.9238795325112867385, 1.000000000000000000, 0.9238795325112867385, 1.000000000000000000, 0.9238795325112867385, 1.000000000000000000, 0.9238795325112867385, 1.000000000000000000, 0.9238795325112867385, 1.000000000000000000, 0.9238795325112867385, 1.000000000000000000, 0.9238795325112867385, 1.000000000000000000, 0.9238795325112867385, 1.000000000000000000, 0.9238795325112867385, 1.000000000000000000, 0.9238795325112867385, 1.000000000000000000, 0.9238795325112867385, 1.000000000000000000, 0.9238795325112867385, 1.000000000000000000, 0.9238795325112867385, 1.000000000000000000, 0.9238795325112867385, 1.000000000000000000, 0.9238795325112867385, 1.000000000000000000, 0.9238795325112867385, 1.000000000000000000, 0.9238795325112867385, 1.000000000000000000, 0.9238795325112867385, 1.000000000000000000, 0.9238795325112867385, 1.000000000000000000, 0.9238795325112867385, 1.000000000000000000, 0.9238795325112867385, 1.000000000000000000, 0.9238795325112867385, 1.000000000000000000, 0.9238795325112867385, 1.000000000000000000, 0.9238795325112867385, 1.000000000000000000, 0.9238795325112867385, 1.000000000000000000, 0.9238795325112867385, 1.000000000000000000, 0.9238795325112867385, 1.000000000000000000, 0.9238795325112867385, 1.000000000000000000, 0.9238795325112867385, 1.000000000000000000, 0.9238795325112867385, 1.000000000000000000, 0.9238795325112867385, 1.000000000000000000, 0.9238795325112867385, 1.000000000000000000, 0.9238795325112867385, 1.000000000000000000, 0.9238795325112867385, 1.000000000000000000, 0.9238795325112867385, 1.000000000000000000, 0.9238795325112867385, 1.000000000000000000, 0.9238795325112867385, 1.000000000000000000, 0.9238795325112867385, 1.000000000000000000, 0.9238795325112867385, 1.000000000000000000, 0.9238795325112867385, 1.000000000000000000, 0.9238795325112867385, 1.000000000000000000, 0.9238795325112867385, 1.000000000000000000, 0.9238795325112867385, 1.000000000000000000, 0.9238795325112867385, 1.000000000000000000, 0.9238795325112867385, 1.000000000000000000, 0.9238795325112867385, 1.000000000000000000, 0.9238795325112867385, 1.000000000000000000, 0.9238795325112867385, 1.000000000000000000, 0.9238795325112867385, 1.000000000000000000, 0.9238795325112867385, 1.000000000000000000, 0.9238795325112867385, 1.000000000000000000, 0.9238795325112867385, 1.000000000000000000, 0.9238795325112867385, 1.000000000000000000, 0.9238795325112867385, 1.000000000000000000, 0.9238795325112867385, 1.000000000000000000, 0.9238795325112867385, 1.000000000000000000, 0.9238795325112867385, 1.000000000000000000, 0.9238795325112867385, 1.000000000000000000, 0.9238795325112867385, 1.000000000000000000, 0.9926342558359432244, 0.9866939939076171395),
 ( 1.000000000000000000, 0.9238795325112867385, 1.000000000000000000, 0.9238795325112867385, 1.000000000000000000, 0.9238795325112867385, 1.000000000000000000, 0.9238795325112867385, 1.000000000000000000, 0.9238795325112867385, 1.000000000000000000, 0.9238795325112867385, 1.000000000000000000, 0.9238795325112867385, 1.000000000000000000, 0.9238795325112867385, 1.000000000000000000, 0.9238795325112867385, 1.000000000000000000, 0.9238795325112867385, 1.000000000000000000, 0.9238795325112867385, 1.000000000000000000, 0.9238795325112867385, 1.000000000000000000, 0.9238795325112867385, 1.000000000000000000, 0.9238795325112867385, 1.000000000000000000, 0.9238795325112867385, 1.000000000000000000, 0.9238795325112867385, 1.000000000000000000, 0.9238795325112867385, 1.000000000000000000, 0.9238795325112867385, 1.000000000000000000, 0.9238795325112867385, 1.000000000000000000, 0.9238795325112867385, 1.000000000000000000, 0.9238795325112867385, 1.000000000000000000, 0.9238795325112867385, 1.000000000000000000, 0.9238795325112867385, 1.000000000000000000, 0.9238795325112867385, 1.000000000000000000, 0.9238795325112867385, 1.000000000000000000, 0.9238795325112867385, 1.000000000000000000, 0.9238795325112867385, 1.000000000000000000, 0.9238795325112867385, 1.000000000000000000, 0.9238795325112867385, 1.000000000000000000, 0.9238795325112867385, 1.000000000000000000, 0.9238795325112867385, 1.000000000000000000, 0.9238795325112867385, 1.000000000000000000, 0.9238795325112867385, 1.000000000000000000, 0.9238795325112867385, 1.000000000000000000, 0.9238795325112867385, 1.000000000000000000, 0.9238795325112867385, 1.000000000000000000, 0.9238795325112867385, 1.000000000000000000, 0.9238795325112867385, 1.000000000000000000, 0.9238795325112867385, 1.000000000000000000, 0.9238795325112867385, 1.000000000000000000, 0.9238795325112867385, 1.000000000000000000, 0.9238795325112867385, 1.000000000000000000, 0.9238795325112867385, 1.000000000000000000, 0.9238795325112867385, 1.000000000000000000, 0.9238795325112867385, 1.000000000000000000, 0.9238795325112867385, 1.000000000000000000, 0.9238795325112867385, 1.000000000000000000, 0.9238795325112867385, 1.000000000000000000, 0.9238795325112867385, 1.000000000000000000, 0.9238795325112867385, 1.000000000000000000, 0.9238795325112867385, 1.000000000000000000, 0.9238795325112867385, 1.000000000000000000, 0.9238795325112867385, 1.000000000000000000, 0.9238795325112867385, 1.000000000000000000, 0.9238795325112867385, 1.000000000000000000, 0.9238795325112867385, 1.000000000000000000, 0.9238795325112867385, 1.000000000000000000, 0.9238795325112867385, 1.000000000000000000, 0.9238795325112867385, 1.000000000000000000, 0.9238795325112867385, 1.000000000000000000, 0.9238795325112867385, 1.000000000000000000, 0.9238795325112867385, 1.000000000000000000, 0.9238795325112867385, 1.000000000000000000, 0.9238795325112867385, 1.000000000000000000, 0.9238795325112867385, 1.000000000000000000, 0.9238795325112867385, 1.000000000000000000, 0.9238795325112867385, 1.000000000000000000, 0.9238795325112867385, 1.000000000000000000, 0.9238795325112867385, 1.000000000000000000, 0.9238795325112867385, 1.000000000000000000, 0.9238795325112867385, 1.000000000000000000, 0.9238795325112867385, 1.000000000000000000, 0.9238795325112867385, 1.000000000000000000, 0.9238795325112867385, 1.000000000000000000, 0.9238795325112867385, 1.000000000000000000, 0.9238795325112867385, 1.000000000000000000, 0.9238795325112867385, 1.000000000000000000, 0.9238795325112867385, 1.000000000000000000, 0.9238795325112867385, 1.000000000000000000, 0.9238795325112867385, 1.000000000000000000, 0.9238795325112867385, 1.000000000000000000, 0.9238795325112867385, 1.000000000000000000, 0.9238795325112867385, 1.000000000000000000, 0.9238795325112867385, 1.000000000000000000, 0.9238795325112867385, 1.000000000000000000, 0.9238795325112867385, 1.000000000000000000, 0.9238795325112867385, 1.000000000000000000, 0.9238795325112867385, 1.000000000000000000, 0.9238795325112867385, 1.000000000000000000, 0.9238795325112867385, 1.000000000000000000, 0.9238795325112867385, 1.000000000000000000, 0.9238795325112867385, 1.000000000000000000, 0.9238795325112867385, 1.000000000000000000, 0.9238795325112867385, 1.000000000000000000, 0.9238795325112867385, 1.000000000000000000, 0.9238795325112867385, 1.000000000000000000, 0.9238795325112867385, 1.000000000000000000, 0.9238795325112867385, 1.000000000000000000, 0.9238795325112867385, 1.000000000000000000, 0.9238795325112867385, 1.000000000000000000, 0.9238795325112867385, 1.000000000000000000, 0.9238795325112867385, 1.000000000000000000, 0.9238795325112867385, 1.000000000000000000, 0.9238795325112867385, 1.000000000000000000, 0.9238795325112867385, 1.000000000000000000, 0.9238795325112867385, 1.000000000000000000, 0.9238795325112867385, 1.000000000000000000, 0.9238795325112867385, 1.000000000000000000, 0.9238795325112867385, 1.000000000000000000, 0.9238795325112867385, 1.000000000000000000, 0.9238795325112867385, 1.000000000000000000, 0.9238795325112867385, 1.000000000000000000, 0.9238795325112867385, 1.000000000000000000, 0.9238795325112867385, 1.000000000000000000, 0.9238795325112867385, 1.000000000000000000, 0.9238795325112867385, 1.000000000000000000, 0.9238795325112867385, 1.000000000000000000, 0.9238795325112867385, 1.000000000000000000, 0.9238795325112867385, 1.000000000000000000, 0.9238795325112867385, 1.000000000000000000, 0.9238795325112867385, 1.000000000000000000, 0.9238795325112867385, 1.000000000000000000, 0.9238795325112867385, 1.000000000000000000, 0.9238795325112867385, 1.000000000000000000, 0.9238795325112867385, 1.000000000000000000, 0.9238795325112867385, 1.000000000000000000, 0.9238795325112867385, 1.000000000000000000, 0.9238795325112867385, 1.000000000000000000, 0.9238795325112867385, 1.000000000000000000, 0.9238795325112867385, 1.000000000000000000, 0.9238795325112867385, 1.000000000000000000, 0.9238795325112867385, 1.000000000000000000, 0.9238795325112867385, 1.000000000000000000, 0.9238795325112867385, 1.000000000000000000, 0.9238795325112867385, 1.000000000000000000, 0.9238795325112867385, 1.000000000000000000, 0.9238795325112867385, 1.000000000000000000, 0.9238795325112867385, 1.000000000000000000, 0.9238795325112867385, 1.000000000000000000, 0.9238795325112867385, 1.000000000000000000, 0.9238795325112867385, 1.000000000000000000, 0.9238795325112867385, 1.000000000000000000, 0.9238795325112867385, 1.000000000000000000, 0.9238795325112867385, 1.000000000000000000, 0.9238795325112867385, 1.000000000000000000, 0.9238795325112867385, 1.000000000000000000, 0.9238795325112867385, 1.000000000000000000, 0.9238795325112867385, 1.000000000000000000, 0.9238795325112867385, 1.000000000000000000, 0.9238795325112867385, 1.000000000000000000, 0.9238795325112867385, 1.000000000000000000, 0.9926342558359432244, 0.9866939939076171395) ) ) 
 REPRESENTATION_ITEM ( '' )  SURFACE ( )  );
#51375=CARTESIAN_POINT ( 'NONE',  ( -4.898587196589407898E-16, 7.999999999999991118, 24.51155278432982598 ) ) ;
#51389=ORIENTED_EDGE ( 'NONE', *, *, #43779, .F. ) ;
#51408=CARTESIAN_POINT ( 'NONE',  ( 7.188101187499991163, 2.977408999572648707, 18.83030278187175099 ) ) ;
#51431=CARTESIAN_POINT ( 'NONE',  ( 2.977408999572646486, 7.188101187499992051, 19.39280278187176165 ) ) ;
#51450=CARTESIAN_POINT ( 'NONE',  ( -7.999999999999989342, -3.313708498984762496, 2.424052779823365533 ) ) ;
#51465=CARTESIAN_POINT ( 'NONE',  ( 7.897089018260699866, -1.490448377887923836, -0.000000000000000000 ) ) ;
#51481=CARTESIAN_POINT ( 'NONE',  ( -5.662595241051935346, 5.662595241051935346, 23.32561528394063188 ) ) ;
#51500=CARTESIAN_POINT ( 'NONE',  ( -5.656854249492375253, 5.656854249492375253, 5.330302783920146226 ) ) ;
#51505=LINE ( 'NONE', #40939, #64434 ) ;
#51514=CARTESIAN_POINT ( 'NONE',  ( 5.082755093536318824, 5.082755093536319713, 17.79905278187175810 ) ) ;
#51524=CARTESIAN_POINT ( 'NONE',  ( -5.656854249492375253, 5.656854249492375253, 27.83030278392014978 ) ) ;
#51532=AXIS2_PLACEMENT_3D ( 'NONE', #64162, #12469, #52844 ) ;
#51538=CARTESIAN_POINT ( 'NONE',  ( -7.999999999999991118, 0.000000000000000000, 23.33030277982336642 ) ) ;
#51545=CARTESIAN_POINT ( 'NONE',  ( 3.313708498984762496, -7.999999999999989342, 8.799052779823364645 ) ) ;
#51555=CARTESIAN_POINT ( 'NONE',  ( -4.898587196589407898E-16, 7.999999999999991118, 11.14280278392014800 ) ) ;
#51570=CARTESIAN_POINT ( 'NONE',  ( 7.999999999999988454, -3.313708498984764272, 28.48655277982336997 ) ) ;
#51584=AXIS2_PLACEMENT_3D ( 'NONE', #10996, #61560, #32909 ) ;
#51587=CARTESIAN_POINT ( 'NONE',  ( -8.000000000000010658, -3.313708498984740736, 18.92405277982336642 ) ) ;
#51608=CARTESIAN_POINT ( 'NONE',  ( -2.977408999572647819, 7.188101187499991163, 7.205302781871750994 ) ) ;
#51609=VERTEX_POINT ( 'NONE', #19096 ) ;
#51636=CARTESIAN_POINT ( 'NONE',  ( 2.977408999572646486, 7.188101187499991163, 11.89280278187175810 ) ) ;
#51639=CARTESIAN_POINT ( 'NONE',  ( 5.656854249492374365, 5.656854249492375253, 3.324052784329822430 ) ) ;
#51650=CARTESIAN_POINT ( 'NONE',  ( -5.867873826482948196, -5.445834672501801421, 1.009359820037964095 ) ) ;
#51666=CARTESIAN_POINT ( 'NONE',  ( -7.999999999999991118, 3.313708498984756723, 3.792802784329823318 ) ) ;
#51667=FACE_OUTER_BOUND ( 'NONE', #44901, .T. ) ;
#51683=CARTESIAN_POINT ( 'NONE',  ( -7.999999999999991118, 3.313708498984756723, 21.92405278392015333 ) ) ;
#51688=( BOUNDED_CURVE ( )  B_SPLINE_CURVE ( 2, ( #26808, #51972, #61139, #45930, #63651, #310, #49821, #51587, #62530 ),
 .UNSPECIFIED., .F., .F. ) 
 B_SPLINE_CURVE_WITH_KNOTS ( ( 3, 2, 2, 2, 3 ),
 ( 0.3421052631578947456, 0.3486842105263157632, 0.3552631578947368363, 0.3618421052631579649, 0.3684210526315789824 ),
 .UNSPECIFIED. ) 
 CURVE ( )  GEOMETRIC_REPRESENTATION_ITEM ( )  RATIONAL_B_SPLINE_CURVE ( ( 1.000000000000000000, 0.9238795325112867385, 1.000000000000000000, 0.9238795325112867385, 1.000000000000000000, 0.9238795325112867385, 1.000000000000000000, 0.9238795325112860723, 1.000000000000000666 ) ) 
 REPRESENTATION_ITEM ( '' )  );
#51693=CARTESIAN_POINT ( 'NONE',  ( -4.401442555609577197E-16, 7.188101187499992051, 2.611552781871750994 ) ) ;
#51706=CARTESIAN_POINT ( 'NONE',  ( 5.082755093536318824, 5.082755093536319713, 4.299052781871752771 ) ) ;
#51719=CARTESIAN_POINT ( 'NONE',  ( -2.977408999572647819, 7.188101187499992051, 1.580302781871753659 ) ) ;
#51736=CARTESIAN_POINT ( 'NONE',  ( -5.656854249492375253, 5.656854249492375253, 23.14280277982336642 ) ) ;
#51750=CARTESIAN_POINT ( 'NONE',  ( 5.656854249492376141, -5.656854249492374365, 25.44905278432982954 ) ) ;
#51752=AXIS2_PLACEMENT_3D ( 'NONE', #22595, #57702, #738 ) ;
#51754=EDGE_CURVE ( 'NONE', #33835, #5549, #24563, .T. ) ;
#51761=VERTEX_POINT ( 'NONE', #67733 ) ;
#51784=CARTESIAN_POINT ( 'NONE',  ( -5.082755093536317936, -5.082755093536320601, 21.17405278187175455 ) ) ;
#51809=CARTESIAN_POINT ( 'NONE',  ( -7.188101187499990274, -2.977408999572651815, 18.45530278187175455 ) ) ;
#51815=VERTEX_POINT ( 'NONE', #45087 ) ;
#51830=CARTESIAN_POINT ( 'NONE',  ( 5.656854249492376141, -5.656854249492374365, 4.392802779823363757 ) ) ;
#51833=ORIENTED_EDGE ( 'NONE', *, *, #30709, .F. ) ;
#51859=CARTESIAN_POINT ( 'NONE',  ( -4.903558642999205574E-16, 8.008118988124991233, 14.13811528394063188 ) ) ;
#51869=CARTESIAN_POINT ( 'NONE',  ( 7.188101187499992051, 8.802885111219154394E-16, 14.23655278187175455 ) ) ;
#51882=CARTESIAN_POINT ( 'NONE',  ( 7.999999999999992895, -3.313708498984756279, 10.67405278392014623 ) ) ;
#51896=CARTESIAN_POINT ( 'NONE',  ( 7.188101187499992051, 8.802885111219154394E-16, 17.61155278187175810 ) ) ;
#51907=CARTESIAN_POINT ( 'NONE',  ( -7.999999999999991118, 3.313708498984757167, 27.92405278392015333 ) ) ;
#51914=CARTESIAN_POINT ( 'NONE',  ( 0.000000000000000000, 0.000000000000000000, 29.33030277982336642 ) ) ;
#51922=CARTESIAN_POINT ( 'NONE',  ( -4.898587196589407898E-16, 7.999999999999991118, 21.45530277982336642 ) ) ;
#51923=CARTESIAN_POINT ( 'NONE',  ( 3.472923220124667587, -7.207533209433660382, -2.138143543582478310E-15 ) ) ;
#51926=EDGE_LOOP ( 'NONE', ( #39526, #40514, #57288, #72767 ) ) ;
#51941=CARTESIAN_POINT ( 'NONE',  ( 1.469576158976822172E-15, -7.999999999999991118, 14.89280278392014623 ) ) ;
#51960=CARTESIAN_POINT ( 'NONE',  ( 3.313708498984756279, 7.999999999999991118, 11.04905278392014978 ) ) ;
#51972=CARTESIAN_POINT ( 'NONE',  ( 7.999999999999992895, -3.313708498984756279, 19.48655277982336642 ) ) ;
#51980=CARTESIAN_POINT ( 'NONE',  ( -7.999999999999991118, 3.313708498984757167, 6.736552779823365533 ) ) ;
#51991=CARTESIAN_POINT ( 'NONE',  ( -2.977408999572648707, -7.188101187499990274, 6.267802781871754547 ) ) ;
#52015=CARTESIAN_POINT ( 'NONE',  ( -7.188101187499992051, 0.000000000000000000, 10.86155278187175455 ) ) ;
#52017=CARTESIAN_POINT ( 'NONE',  ( 0.000000000000000000, 0.000000000000000000, 11.00000000000000000 ) ) ;
#52018=CARTESIAN_POINT ( 'NONE',  ( 7.999999999999992895, -3.313708498984756279, 0.04280278432982297099 ) ) ;
#52026=AXIS2_PLACEMENT_3D ( 'NONE', #33644, #49479, #72498 ) ;
#52029=CARTESIAN_POINT ( 'NONE',  ( 7.999999999999992895, -3.313708498984756279, 2.986552779823361981 ) ) ;
#52045=CARTESIAN_POINT ( 'NONE',  ( 7.999999999999991118, 3.313708498984757611, 7.730302784329822430 ) ) ;
#52065=CARTESIAN_POINT ( 'NONE',  ( 7.999999999999992895, -3.313708498984756279, 18.17405278392014623 ) ) ;
#52076=CARTESIAN_POINT ( 'NONE',  ( -2.977408999572648707, -7.188101187499990274, 25.76780278187175810 ) ) ;
#52092=CARTESIAN_POINT ( 'NONE',  ( -7.188101187499990274, -2.977408999572651371, 1.955302781871753881 ) ) ;
#52097=CARTESIAN_POINT ( 'NONE',  ( 5.662595241051936235, -5.662595241051934458, 3.075615283940628331 ) ) ;
#52104=CARTESIAN_POINT ( 'NONE',  ( -2.977408999572648707, -7.188101187499990274, 26.14280278187176165 ) ) ;
#52122=CARTESIAN_POINT ( 'NONE',  ( -7.999999999999989342, -3.313708498984762496, 21.92405277982336642 ) ) ;
#52135=CARTESIAN_POINT ( 'NONE',  ( -5.656854249492375253, 5.656854249492375253, 21.69905278432982243 ) ) ;
#52165=( BOUNDED_CURVE ( )  B_SPLINE_CURVE ( 2, ( #58998, #42358, #36713, #53329, #6568, #1292, #12582, #7672, #25371 ),
 .UNSPECIFIED., .F., .F. ) 
 B_SPLINE_CURVE_WITH_KNOTS ( ( 3, 2, 2, 2, 3 ),
 ( 0.6842105263157894912, 0.6907894736842105088, 0.6973684210526316374, 0.7039473684210527660, 0.7105263157894737835 ),
 .UNSPECIFIED. ) 
 CURVE ( )  GEOMETRIC_REPRESENTATION_ITEM ( )  RATIONAL_B_SPLINE_CURVE ( ( 1.000000000000000000, 0.9238795325112867385, 1.000000000000000000, 0.9238795325112867385, 1.000000000000000000, 0.9238795325112867385, 1.000000000000000000, 0.9238795325112854062, 1.000000000000001332 ) ) 
 REPRESENTATION_ITEM ( '' )  );
#52168=CARTESIAN_POINT ( 'NONE',  ( -5.082755093536319713, 5.082755093536319713, 13.29905278187175277 ) ) ;
#52191=CARTESIAN_POINT ( 'NONE',  ( -5.082755093536317936, -5.082755093536320601, 14.04905278187175455 ) ) ;
#52209=CARTESIAN_POINT ( 'NONE',  ( 5.656854249492376141, -5.656854249492374365, 5.892802779823364645 ) ) ;
#52236=CARTESIAN_POINT ( 'NONE',  ( -8.008118988124991233, 0.000000000000000000, 11.51311528394062833 ) ) ;
#52242=CARTESIAN_POINT ( 'NONE',  ( -4.401442555609577197E-16, 7.188101187499992051, 11.61155278187175632 ) ) ;
#52256=CARTESIAN_POINT ( 'NONE',  ( 3.313708498984762496, -7.999999999999989342, 7.486552783920144449 ) ) ;
#52271=CARTESIAN_POINT ( 'NONE',  ( -7.188101187499992051, 0.000000000000000000, 18.36155278187175455 ) ) ;
#52274=DIRECTION ( 'NONE',  ( -0.000000000000000000, -0.000000000000000000, 1.000000000000000000 ) ) ;
#52287=CARTESIAN_POINT ( 'NONE',  ( -7.999999999999991118, 0.000000000000000000, 24.83030277982336642 ) ) ;
#52296=CARTESIAN_POINT ( 'NONE',  ( 3.313708498984762496, -7.999999999999989342, 20.79905277982336642 ) ) ;
#52314=CARTESIAN_POINT ( 'NONE',  ( 7.999999999999992895, -3.313708498984756279, 9.174052783920144449 ) ) ;
#52362=CARTESIAN_POINT ( 'NONE',  ( -2.977408999572647819, 7.188101187499991163, 4.205302781871751883 ) ) ;
#52372=EDGE_LOOP ( 'NONE', ( #65771, #25348, #24121, #27244 ) ) ;
#52387=CARTESIAN_POINT ( 'NONE',  ( 2.977408999572650927, -7.188101187499990274, 12.83030278187175277 ) ) ;
#52393=CARTESIAN_POINT ( 'NONE',  ( 3.313708498984762496, -7.999999999999989342, 7.486552783920144449 ) ) ;
#52401=CARTESIAN_POINT ( 'NONE',  ( 7.999999999999991118, 9.797174393178815797E-16, 22.76780278392014623 ) ) ;
#52423=CARTESIAN_POINT ( 'NONE',  ( -5.082755093536319713, 5.082755093536319713, 26.79905278187175455 ) ) ;
#52432=CARTESIAN_POINT ( 'NONE',  ( 5.656854249492374365, 5.656854249492375253, 21.45530278392014623 ) ) ;
#52443=CARTESIAN_POINT ( 'NONE',  ( 7.188101187499993827, -2.977408999572645598, 26.14280278187175455 ) ) ;
#52456=CARTESIAN_POINT ( 'NONE',  ( -5.082755093536317936, -5.082755093536320601, 2.049052781871754103 ) ) ;
#52460=CARTESIAN_POINT ( 'NONE',  ( 3.317071493978883456, -8.008118988124989457, 2.981865283940628331 ) ) ;
#52467=CARTESIAN_POINT ( 'NONE',  ( -5.082755093536317936, -5.082755093536320601, 27.54905278187175455 ) ) ;
#52485=CARTESIAN_POINT ( 'NONE',  ( 3.313708498984762496, -7.999999999999989342, 22.29905277982336287 ) ) ;
#52499=CARTESIAN_POINT ( 'NONE',  ( -7.999999999999991118, 3.313708498984756723, 23.29280278432983309 ) ) ;
#52531=CARTESIAN_POINT ( 'NONE',  ( -4.401442555609577197E-16, 7.188101187499992051, 10.11155278187175455 ) ) ;
#52549=CARTESIAN_POINT ( 'NONE',  ( 7.999999999999991118, 1.469576158976822369E-15, 25.76780278392172008 ) ) ;
#52554=CARTESIAN_POINT ( 'NONE',  ( 5.082755093536320601, -5.082755093536318824, 11.42405278187175455 ) ) ;
#52557=CARTESIAN_POINT ( 'NONE',  ( 5.656854249492376141, -5.656854249492374365, 20.89280277982336642 ) ) ;
#52589=DIRECTION ( 'NONE',  ( 1.000000000000000000, 0.000000000000000000, 0.000000000000000000 ) ) ;
#52603=CARTESIAN_POINT ( 'NONE',  ( 3.317071493978877683, 8.008118988124991233, 15.54436528394063188 ) ) ;
#52610=CARTESIAN_POINT ( 'NONE',  ( 5.082755093536320601, -5.082755093536318824, 6.549052781871754547 ) ) ;
#52611=( BOUNDED_CURVE ( )  B_SPLINE_CURVE ( 2, ( #9365, #60289, #42568, #61041, #8616, #61417, #32385, #25947, #66702, #26322, #13876 ),
 .UNSPECIFIED., .F., .F. ) 
 B_SPLINE_CURVE_WITH_KNOTS ( ( 3, 2, 2, 2, 2, 3 ),
 ( 0.3970965164372073364, 0.3970965350674087180, 0.4037148106518655410, 0.4103330862363223086, 0.4169513618207791872, 0.4235696451107979765 ),
 .UNSPECIFIED. ) 
 CURVE ( )  GEOMETRIC_REPRESENTATION_ITEM ( )  RATIONAL_B_SPLINE_CURVE ( ( 0.9999995714485965248, 0.9999997857236950782, 1.000000000000000000, 0.9238795325112867385, 1.000000000000000000, 0.9238795325112867385, 1.000000000000000000, 0.9238795325112867385, 1.000000000000000000, 0.9238795325112867385, 1.000000000000000000 ) ) 
 REPRESENTATION_ITEM ( '' )  );
#52624=CARTESIAN_POINT ( 'NONE',  ( 7.999999999999992895, -3.313708498984756279, 1.674052783920142895 ) ) ;
#52639=CARTESIAN_POINT ( 'NONE',  ( 7.188101187499991163, 2.977408999572648707, 17.70530278187175455 ) ) ;
#52647=CARTESIAN_POINT ( 'NONE',  ( 7.188101187499992051, 8.802885111219154394E-16, 26.61155278187175810 ) ) ;
#52652=AXIS2_PLACEMENT_3D ( 'NONE', #60978, #38347, #2895 ) ;
#52664=CARTESIAN_POINT ( 'NONE',  ( 5.656854249492374365, 5.656854249492375253, 15.26780277982336642 ) ) ;
#52683=CARTESIAN_POINT ( 'NONE',  ( 7.999999999999992895, -3.313708498984756279, 7.674052783920145338 ) ) ;
#52697=CARTESIAN_POINT ( 'NONE',  ( 7.999999999999991118, 9.797174393178815797E-16, 27.08030277982336642 ) ) ;
#52701=DIRECTION ( 'NONE',  ( -1.000000000000000000, 0.000000000000000000, 0.000000000000000000 ) ) ;
#52723=CARTESIAN_POINT ( 'NONE',  ( -7.999999999999991118, 9.797174393178815797E-16, 30.00000000000000000 ) ) ;
#52733=CARTESIAN_POINT ( 'NONE',  ( 7.188101187499992051, 8.802885111219154394E-16, 6.736552781871754547 ) ) ;
#52755=CARTESIAN_POINT ( 'NONE',  ( 5.082755093536318824, 5.082755093536319713, 10.29905278187175455 ) ) ;
#52758=CARTESIAN_POINT ( 'NONE',  ( 3.313708498984756279, 7.999999999999991118, 3.417802784329822430 ) ) ;
#52767=CARTESIAN_POINT ( 'NONE',  ( 3.313708498984756279, 7.999999999999991118, 26.04905278392014623 ) ) ;
#52791=CARTESIAN_POINT ( 'NONE',  ( 5.082755093536318824, 5.082755093536319713, 27.92405278187175455 ) ) ;
#52800=CARTESIAN_POINT ( 'NONE',  ( -4.898587196589407898E-16, 7.999999999999991118, 17.14280278392014978 ) ) ;
#52812=CARTESIAN_POINT ( 'NONE',  ( 1.320432766682872962E-15, -7.188101187499992051, 27.36155278187175455 ) ) ;
#52825=CARTESIAN_POINT ( 'NONE',  ( -4.401442555609577197E-16, 7.188101187499992051, 1.486552781871753437 ) ) ;
#52831=CARTESIAN_POINT ( 'NONE',  ( -5.662595241051935346, 5.662595241051935346, 0.8256152839406295518 ) ) ;
#52837=CARTESIAN_POINT ( 'NONE',  ( -7.188101187499991163, 2.977408999572646930, 28.76780278187175455 ) ) ;
#52844=DIRECTION ( 'NONE',  ( 1.224646799147353207E-16, -1.000000000000000000, 0.000000000000000000 ) ) ;
#52845=DIRECTION ( 'NONE',  ( -0.000000000000000000, -0.000000000000000000, 1.000000000000000000 ) ) ;
#52855=CARTESIAN_POINT ( 'NONE',  ( -3.313708498984758943, -7.999999999999989342, 16.11155277982336642 ) ) ;
#52871=CARTESIAN_POINT ( 'NONE',  ( -4.898587196589407898E-16, 7.999999999999991118, 17.01155278432982954 ) ) ;
#52895=ORIENTED_EDGE ( 'NONE', *, *, #22789, .T. ) ;
#52902=CARTESIAN_POINT ( 'NONE',  ( -2.977408999572648707, -7.188101187499990274, 10.76780278187175632 ) ) ;
#52929=CARTESIAN_POINT ( 'NONE',  ( -7.188101187499990274, -2.977408999572651815, 12.45530278187175277 ) ) ;
#52951=VERTEX_POINT ( 'NONE', #58399 ) ;
#52973=CARTESIAN_POINT ( 'NONE',  ( -5.662595241051935346, 5.662595241051935346, 12.82561528394063011 ) ) ;
#52978=CARTESIAN_POINT ( 'NONE',  ( -7.188101187499992051, 2.977408999572646930, 7.392802781871750994 ) ) ;
#52995=CARTESIAN_POINT ( 'NONE',  ( 5.656854249492376141, -5.656854249492374365, 3.080302783920144005 ) ) ;
#53010=CARTESIAN_POINT ( 'NONE',  ( 2.977408999572650927, -7.188101187499990274, 15.83030278187175277 ) ) ;
#53012=CARTESIAN_POINT ( 'NONE',  ( 7.999999999999991118, 0.000000000000000000, 30.00000000000000000 ) ) ;
#53029=( BOUNDED_CURVE ( )  B_SPLINE_CURVE ( 2, ( #71117, #54535, #25464, #54909, #47735, #59451, #71483, #60551, #42815 ),
 .UNSPECIFIED., .F., .F. ) 
 B_SPLINE_CURVE_WITH_KNOTS ( ( 3, 2, 2, 2, 3 ),
 ( 0.05263157894736845976, 0.05921052631578951897, 0.06578947368421057817, 0.07236842105263163738, 0.07894736842105269659 ),
 .UNSPECIFIED. ) 
 CURVE ( )  GEOMETRIC_REPRESENTATION_ITEM ( )  RATIONAL_B_SPLINE_CURVE ( ( 0.9999999999999995559, 0.9238795325112871826, 1.000000000000000000, 0.9238795325112867385, 1.000000000000000000, 0.9238795325112867385, 1.000000000000000000, 0.9238795325112859613, 1.000000000000000888 ) ) 
 REPRESENTATION_ITEM ( '' )  );
#53036=CARTESIAN_POINT ( 'NONE',  ( 3.313708498984762496, -7.999999999999989342, 13.29905277982336465 ) ) ;
#53054=CARTESIAN_POINT ( 'NONE',  ( 1.469576158976822172E-15, -7.999999999999991118, 7.392802783920144449 ) ) ;
#53095=AXIS2_PLACEMENT_3D ( 'NONE', #42535, #41803, #48192 ) ;
#53104=CARTESIAN_POINT ( 'NONE',  ( -4.401442555609577197E-16, 7.188101187499992051, 4.111552781871752771 ) ) ;
#53115=DIRECTION ( 'NONE',  ( 1.000000000000000000, 0.000000000000000000, 0.000000000000000000 ) ) ;
#53129=CARTESIAN_POINT ( 'NONE',  ( -7.188101187499990274, -2.977408999572651371, 6.455302781871754547 ) ) ;
#53142=CARTESIAN_POINT ( 'NONE',  ( -3.313708498984758943, -7.999999999999989342, 22.29905278392014623 ) ) ;
#53170=CARTESIAN_POINT ( 'NONE',  ( 0.000000000000000000, -7.999999999999991118, 29.33030277982336642 ) ) ;
#53172=CARTESIAN_POINT ( 'NONE',  ( -5.656854249492373476, -5.656854249492376141, 17.70530278392014623 ) ) ;
#53184=CARTESIAN_POINT ( 'NONE',  ( -7.188101187499992051, 0.000000000000000000, 25.48655278187175810 ) ) ;
#53197=CARTESIAN_POINT ( 'NONE',  ( 1.320432766682872962E-15, -7.188101187499992051, 2.236552781871754103 ) ) ;
#53199=CARTESIAN_POINT ( 'NONE',  ( 3.313708498984756279, 7.999999999999991118, 15.36155277982336642 ) ) ;
#53203=CARTESIAN_POINT ( 'NONE',  ( -3.317071493978880348, -8.008118988124989457, 1.294365283940630107 ) ) ;
#53209=CARTESIAN_POINT ( 'NONE',  ( -7.188101187499992051, 0.000000000000000000, 22.86155278187175455 ) ) ;
#53228=CARTESIAN_POINT ( 'NONE',  ( 5.656854249492376141, -5.656854249492374365, 16.39280277982336287 ) ) ;
#53242=CARTESIAN_POINT ( 'NONE',  ( -4.898587196589407898E-16, 7.999999999999991118, 18.51155278432982243 ) ) ;
#53275=( BOUNDED_CURVE ( )  B_SPLINE_CURVE ( 2, ( #52697, #18362, #23274, #70052, #41740, #57625, #5938, #64387, #35361 ),
 .UNSPECIFIED., .F., .F. ) 
 B_SPLINE_CURVE_WITH_KNOTS ( ( 3, 2, 2, 2, 3 ),
 ( 0.07894736842105269659, 0.08552631578947372804, 0.09210526315789474561, 0.09868421052631579093, 0.1052631578947368085 ),
 .UNSPECIFIED. ) 
 CURVE ( )  GEOMETRIC_REPRESENTATION_ITEM ( )  RATIONAL_B_SPLINE_CURVE ( ( 0.9999999999999992228, 0.9238795325112875156, 1.000000000000000000, 0.9238795325112867385, 1.000000000000000000, 0.9238795325112867385, 1.000000000000000000, 0.9238795325112870716, 0.9999999999999996669 ) ) 
 REPRESENTATION_ITEM ( '' )  );
#53277=CARTESIAN_POINT ( 'NONE',  ( -2.977408999572647819, 7.188101187499991163, 11.70530278187175099 ) ) ;
#53302=CARTESIAN_POINT ( 'NONE',  ( 7.188101187499992051, 2.977408999572647819, 11.70530278187175632 ) ) ;
#53316=LINE ( 'NONE', #1640, #46285 ) ;
#53329=CARTESIAN_POINT ( 'NONE',  ( -3.313708498984757611, 7.999999999999991118, 9.549052779823364645 ) ) ;
#53333=ORIENTED_EDGE ( 'NONE', *, *, #46210, .F. ) ;
#53342=CARTESIAN_POINT ( 'NONE',  ( -7.999999999999991118, 0.000000000000000000, 12.83030277982336465 ) ) ;
#53344=CARTESIAN_POINT ( 'NONE',  ( 3.317071493978883456, -8.008118988124989457, 11.98186528394062655 ) ) ;
#53351=CARTESIAN_POINT ( 'NONE',  ( -5.082755093536319713, 5.082755093536319713, 8.799052781871752771 ) ) ;
#53352=ADVANCED_FACE ( 'NONE', ( #71256 ), #7536, .F. ) ;
#53365=CARTESIAN_POINT ( 'NONE',  ( 7.999999999999992895, -3.313708498984756279, 4.674052783920145338 ) ) ;
#53368=EDGE_CURVE ( 'NONE', #4422, #39299, #72649, .T. ) ;
#53382=CARTESIAN_POINT ( 'NONE',  ( -7.188101187499992051, 0.000000000000000000, 10.86155278187175455 ) ) ;
#53391=CARTESIAN_POINT ( 'NONE',  ( -7.188101187499992051, 2.977408999572646930, 27.26780278187175455 ) ) ;
#53409=CARTESIAN_POINT ( 'NONE',  ( -5.656854249492375253, 5.656854249492375253, 15.64280277982336642 ) ) ;
#53414=CARTESIAN_POINT ( 'NONE',  ( 7.999999999988127719, 1.377684776014802281E-05, 21.26780317368888618 ) ) ;
#53418=CARTESIAN_POINT ( 'NONE',  ( -7.999999999999991118, -1.759549274430992710E-05, 5.517803281724177111 ) ) ;
#53473=CARTESIAN_POINT ( 'NONE',  ( -7.188101187499991163, 2.977408999572646930, 2.892802781871751439 ) ) ;
#53497=CARTESIAN_POINT ( 'NONE',  ( -5.082755093536317936, -5.082755093536320601, 3.549052781871751883 ) ) ;
#53511=CARTESIAN_POINT ( 'NONE',  ( -3.313708498984758943, -7.999999999999989342, 25.29905278392014623 ) ) ;
#53513=EDGE_CURVE ( 'NONE', #22871, #25965, #21066, .T. ) ;
#53528=EDGE_CURVE ( 'NONE', #33233, #49310, #31648, .T. ) ;
#53534=CARTESIAN_POINT ( 'NONE',  ( 5.082755093536318824, 5.082755093536319713, 21.92405278187175455 ) ) ;
#53542=CARTESIAN_POINT ( 'NONE',  ( -5.656854249492373476, -5.656854249492376141, 13.20530278392014623 ) ) ;
#53554=CARTESIAN_POINT ( 'NONE',  ( 2.977408999572646486, 7.188101187499991163, 22.01780278187175455 ) ) ;
#53558=CARTESIAN_POINT ( 'NONE',  ( 7.999999999732929190, -6.536825277765295045E-05, 6.267800880277100362 ) ) ;
#53571=CARTESIAN_POINT ( 'NONE',  ( -3.317071493978878571, 8.008118988124991233, 2.231865283940627886 ) ) ;
#53578=CARTESIAN_POINT ( 'NONE',  ( -2.977408999572648707, -7.188101187499990274, 24.64280278187176165 ) ) ;
#53599=CARTESIAN_POINT ( 'NONE',  ( 7.999999999999991118, 9.797174393178815797E-16, 15.08030277982336642 ) ) ;
#53611=CARTESIAN_POINT ( 'NONE',  ( 7.999999999999991118, 9.797174393178815797E-16, 16.63655278432982954 ) ) ;
#53643=( LENGTH_UNIT ( ) NAMED_UNIT ( * ) SI_UNIT ( .MILLI., .METRE. ) );
#53646=CARTESIAN_POINT ( 'NONE',  ( 7.188101187499992051, 8.802885111219154394E-16, 12.73655278187175277 ) ) ;
#53666=CARTESIAN_POINT ( 'NONE',  ( 7.188101187499992051, 8.802885111219154394E-16, 8.611552781871752771 ) ) ;
#53691=CARTESIAN_POINT ( 'NONE',  ( -8.000000000000021316, -3.313708498984730522, 23.42405277982336642 ) ) ;
#53711=CARTESIAN_POINT ( 'NONE',  ( -5.656854249492373476, -5.656854249492376141, 13.01780277982336465 ) ) ;
#53713=CARTESIAN_POINT ( 'NONE',  ( 8.008118988124991233, 3.317071493978879015, 6.356865283940630995 ) ) ;
#53718=CARTESIAN_POINT ( 'NONE',  ( 2.977408999572650927, -7.188101187499990274, 9.455302781871752771 ) ) ;
#53734=CARTESIAN_POINT ( 'NONE',  ( -7.999999999999991118, 0.000000000000000000, 1.017802783920145782 ) ) ;
#53750=CARTESIAN_POINT ( 'NONE',  ( 5.656854249492374365, 5.656854249492375253, 1.955302783920143117 ) ) ;
#53754=CARTESIAN_POINT ( 'NONE',  ( 0.000000000000000000, 0.000000000000000000, 30.00000000000000000 ) ) ;
#53776=CARTESIAN_POINT ( 'NONE',  ( 5.656854249492376141, -5.656854249492374365, 13.39280277982336465 ) ) ;
#53793=CARTESIAN_POINT ( 'NONE',  ( 7.999999999999989342, -3.268493847551538582E-05, 6.267801859212078774 ) ) ;
#53806=CARTESIAN_POINT ( 'NONE',  ( 5.662595241051934458, 5.662595241051935346, 24.45061528394063188 ) ) ;
#53840=CARTESIAN_POINT ( 'NONE',  ( 5.082755093536320601, -5.082755093536318824, 0.5490527818717526598 ) ) ;
#53863=CARTESIAN_POINT ( 'NONE',  ( 7.188101187499993827, -2.977408999572645598, 4.017802781871751883 ) ) ;
#53880=CARTESIAN_POINT ( 'NONE',  ( 3.313708498984756279, 7.999999999999991118, 23.04905278392014623 ) ) ;
#53900=CARTESIAN_POINT ( 'NONE',  ( -5.082755093536319713, 5.082755093536319713, 19.29905278187175455 ) ) ;
#53908=CARTESIAN_POINT ( 'NONE',  ( -3.313708498984757167, 7.999999999999991118, 11.23655278392014445 ) ) ;
#53920=CARTESIAN_POINT ( 'NONE',  ( -4.401442555609577197E-16, 7.188101187499992051, 20.61155278187175455 ) ) ;
#53938=CARTESIAN_POINT ( 'NONE',  ( 5.656854249492376141, -5.656854249492374365, 25.58030278392014978 ) ) ;
#53945=CARTESIAN_POINT ( 'NONE',  ( -4.401442555609577197E-16, 7.188101187499992051, 22.48655278187175455 ) ) ;
#53962=CARTESIAN_POINT ( 'NONE',  ( 3.313708498984756279, 7.999999999999991118, 16.86155277982336642 ) ) ;
#53978=CARTESIAN_POINT ( 'NONE',  ( 7.999999999999991118, 9.797174393178815797E-16, 18.13655278432982243 ) ) ;
#54009=CARTESIAN_POINT ( 'NONE',  ( -7.188101187499991163, 2.977408999572646930, 5.892802781871754547 ) ) ;
#54036=CARTESIAN_POINT ( 'NONE',  ( 2.977408999572650927, -7.188101187499990274, 6.830302781871754547 ) ) ;
#54038=LINE ( 'NONE', #54786, #13009 ) ;
#54082=CARTESIAN_POINT ( 'NONE',  ( 8.008118988124993010, -3.317071493978877239, 7.669365283940628331 ) ) ;
#54088=CARTESIAN_POINT ( 'NONE',  ( -7.188101187499992051, 0.000000000000000000, 1.486552781871753437 ) ) ;
#54102=CARTESIAN_POINT ( 'NONE',  ( 3.313708498984756279, 7.999999999999991118, 2.049052783920143117 ) ) ;
#54121=CARTESIAN_POINT ( 'NONE',  ( -7.999999999999991118, -1.759625989565808730E-05, 2.517803281745877975 ) ) ;
#54127=CARTESIAN_POINT ( 'NONE',  ( 5.082755093536318824, 5.082755093536319713, 28.29905278187175810 ) ) ;
#54147=CARTESIAN_POINT ( 'NONE',  ( -7.999999999999989342, -3.313708498984762496, 13.11155278392014623 ) ) ;
#54148=CARTESIAN_POINT ( 'NONE',  ( 5.656854249492374365, 5.656854249492375253, 12.26780277982336642 ) ) ;
#54150=DIRECTION ( 'NONE',  ( 0.7578158005275104081, 0.6524685528597132800, 0.000000000000000000 ) ) ;
#54182=CARTESIAN_POINT ( 'NONE',  ( -8.008118988124991233, 3.317071493978878127, 24.91936528394063899 ) ) ;
#54214=CARTESIAN_POINT ( 'NONE',  ( 7.188101187499991163, 2.977408999572648707, 26.70530278187175455 ) ) ;
#54239=CARTESIAN_POINT ( 'NONE',  ( -4.401442555609577197E-16, 7.188101187499992051, 1.486552781871753437 ) ) ;
#54255=CARTESIAN_POINT ( 'NONE',  ( 7.999999999999991118, 9.797174393178815797E-16, 16.76780278392014978 ) ) ;
#54257=VECTOR ( 'NONE', #40980, 1000.000000000000000 ) ;
#54266=ORIENTED_EDGE ( 'NONE', *, *, #47309, .T. ) ;
#54275=ORIENTED_EDGE ( 'NONE', *, *, #53368, .F. ) ;
#54277=CARTESIAN_POINT ( 'NONE',  ( -2.977408999572647819, 7.188101187499992051, 22.20530278187175455 ) ) ;
#54288=CARTESIAN_POINT ( 'NONE',  ( 3.313708498984756279, 7.999999999999991118, 11.04905278392014800 ) ) ;
#54299=CARTESIAN_POINT ( 'NONE',  ( 5.082755093536320601, -5.082755093536318824, 17.04905278187175810 ) ) ;
#54318=CARTESIAN_POINT ( 'NONE',  ( 3.313708498984762496, -7.999999999999989342, 23.98655278392014978 ) ) ;
#54325=CARTESIAN_POINT ( 'NONE',  ( -5.082755093536317936, -5.082755093536320601, 21.54905278187175455 ) ) ;
#54340=CARTESIAN_POINT ( 'NONE',  ( 7.999999999999991118, 3.313708498984757611, 18.17405277982336642 ) ) ;
#54355=CARTESIAN_POINT ( 'NONE',  ( 5.656854249492376141, -5.656854249492374365, 16.44905278432982954 ) ) ;
#54383=FACE_OUTER_BOUND ( 'NONE', #51926, .T. ) ;
#54390=CARTESIAN_POINT ( 'NONE',  ( -7.188101187499992051, 0.000000000000000000, 5.986552781871753659 ) ) ;
#54403=APPLICATION_CONTEXT ( 'automotive_design' ) ;
#54413=CARTESIAN_POINT ( 'NONE',  ( -4.401442555609577197E-16, 7.188101187499992051, 4.486552781871752771 ) ) ;
#54415=FACE_OUTER_BOUND ( 'NONE', #52372, .T. ) ;
#54419=CYLINDRICAL_SURFACE ( 'NONE', #43500, 7.999999999999991118 ) ;
#54442=CARTESIAN_POINT ( 'NONE',  ( 7.999999999999991118, 3.313708498984757611, 4.861552783920145338 ) ) ;
#54461=CARTESIAN_POINT ( 'NONE',  ( -5.662595241051935346, 5.662595241051935346, 8.325615283940630107 ) ) ;
#54468=CARTESIAN_POINT ( 'NONE',  ( 7.188101187499993827, -2.977408999572645598, 3.642802781871751883 ) ) ;
#54482=CARTESIAN_POINT ( 'NONE',  ( 5.082755093536318824, 5.082755093536319713, 23.42405278187175455 ) ) ;
#54505=CARTESIAN_POINT ( 'NONE',  ( -7.188101187499990274, -2.977408999572651815, 24.45530278187175810 ) ) ;
#54522=CARTESIAN_POINT ( 'NONE',  ( 7.999999999999991118, 3.313708498984757611, 9.174052779823364645 ) ) ;
#54525=CARTESIAN_POINT ( 'NONE',  ( 5.656854249492374365, 5.656854249492375253, 1.767802779823364423 ) ) ;
#54533=CARTESIAN_POINT ( 'NONE',  ( -5.656854249492375253, 5.656854249492375253, 20.33030278392014623 ) ) ;
#54535=CARTESIAN_POINT ( 'NONE',  ( -7.999999999999974243, 3.313708498984772710, 27.73655277982335932 ) ) ;
#54554=ADVANCED_FACE ( 'NONE', ( #8097 ), #2069, .F. ) ;
#54588=CARTESIAN_POINT ( 'NONE',  ( -5.082755093536319713, 5.082755093536319713, 2.799052781871750994 ) ) ;
#54612=CARTESIAN_POINT ( 'NONE',  ( 2.977408999572650927, -7.188101187499990274, 3.830302781871751883 ) ) ;
#54628=CARTESIAN_POINT ( 'NONE',  ( -4.898587196589407898E-16, 7.999999999999991118, 18.64280278392014623 ) ) ;
#54638=CARTESIAN_POINT ( 'NONE',  ( -3.313708498984759387, -7.999999999999989342, 26.79905278392014623 ) ) ;
#54646=CARTESIAN_POINT ( 'NONE',  ( 7.999999999999991118, 1.076704741343554046E-05, 12.26780308853677148 ) ) ;
#54650=CARTESIAN_POINT ( 'NONE',  ( -2.977408999572647819, -7.188101187499990274, 22.76780278187175455 ) ) ;
#54660=CARTESIAN_POINT ( 'NONE',  ( -7.999999999999991118, 3.313708498984756723, 14.42405278392014800 ) ) ;
#54671=CARTESIAN_POINT ( 'NONE',  ( 1.320432766682872962E-15, -7.188101187499992051, 18.36155278187175455 ) ) ;
#54690=CARTESIAN_POINT ( 'NONE',  ( 7.999999999999991118, 9.797174393178815797E-16, 24.26780278392014978 ) ) ;
#54697=CARTESIAN_POINT ( 'NONE',  ( 2.977408999572650927, -7.188101187499990274, 21.83030278187175810 ) ) ;
#54713=CARTESIAN_POINT ( 'NONE',  ( -5.656854249492375253, 5.656854249492375253, 9.642802779823364645 ) ) ;
#54725=VERTEX_POINT ( 'NONE', #21643 ) ;
#54732=CARTESIAN_POINT ( 'NONE',  ( 3.313708498984756279, 7.999999999999991118, 12.41780278432982421 ) ) ;
#54761=CARTESIAN_POINT ( 'NONE',  ( 7.188101187499991163, 2.977408999572648707, 6.830302781871755435 ) ) ;
#54763=ORIENTED_EDGE ( 'NONE', *, *, #36305, .F. ) ;
#54773=CARTESIAN_POINT ( 'NONE',  ( -2.977408999572648707, -7.188101187499990274, 11.14280278187175810 ) ) ;
#54784=CARTESIAN_POINT ( 'NONE',  ( -7.188101187499992051, 0.000000000000000000, 4.861552781871752771 ) ) ;
#54786=CARTESIAN_POINT ( 'NONE',  ( 7.999999999999991118, 0.000000000000000000, 30.00000000000000000 ) ) ;
#54801=CARTESIAN_POINT ( 'NONE',  ( 3.313708498984762496, -7.999999999999989342, 26.79905277982337353 ) ) ;
#54813=EDGE_CURVE ( 'NONE', #38243, #19453, #33228, .T. ) ;
#54816=CARTESIAN_POINT ( 'NONE',  ( -7.999999999999991118, 0.000000000000000000, 7.017802783920144449 ) ) ;
#54824=STYLED_ITEM('',(#74713),#66162);
#54834=CARTESIAN_POINT ( 'NONE',  ( 1.471067592899761672E-15, -8.008118988124991233, 7.388115283940628331 ) ) ;
#54840=CARTESIAN_POINT ( 'NONE',  ( -2.977408999572647819, 7.188101187499992051, 5.705302781871753659 ) ) ;
#54850=CARTESIAN_POINT ( 'NONE',  ( -5.082755093536317936, -5.082755093536320601, 24.17405278187175455 ) ) ;
#54877=CARTESIAN_POINT ( 'NONE',  ( 7.188101187499992051, 8.802885111219154394E-16, 20.61155278187175455 ) ) ;
#54894=CARTESIAN_POINT ( 'NONE',  ( 7.999999999999991118, 9.797174393178815797E-16, 12.08030277982336642 ) ) ;
#54896=CARTESIAN_POINT ( 'NONE',  ( -7.999987203421805582, -3.313721295562947144, 17.61155329591527519 ) ) ;
#54905=CARTESIAN_POINT ( 'NONE',  ( 7.999999999999991118, 9.797174393178815797E-16, 4.767802783920145338 ) ) ;
#54907=CARTESIAN_POINT ( 'NONE',  ( 7.999999999999991118, 3.313708498984758055, 19.86155278392014978 ) ) ;
#54909=CARTESIAN_POINT ( 'NONE',  ( -3.313708498984757611, 7.999999999999991118, 27.54905277982337353 ) ) ;
#54925=CARTESIAN_POINT ( 'NONE',  ( -4.903558642999205574E-16, 8.008118988124991233, 26.13811528394063188 ) ) ;
#54954=CARTESIAN_POINT ( 'NONE',  ( 0.000000000000000000, 18.31575019322283637, 2.966738217918095000 ) ) ;
#54959=CARTESIAN_POINT ( 'NONE',  ( -2.977408999572647819, 7.188101187499991163, 27.08030278187175810 ) ) ;
#54961=CARTESIAN_POINT ( 'NONE',  ( 7.999999999999991118, 3.313708498984758055, 15.36155278392014623 ) ) ;
#54962=DIRECTION ( 'NONE',  ( 1.000000000000000000, 0.000000000000000000, 0.000000000000000000 ) ) ;
#54987=CARTESIAN_POINT ( 'NONE',  ( 1.469576158976822172E-15, -7.999999999999991118, 28.20530277982336642 ) ) ;
#55006=CARTESIAN_POINT ( 'NONE',  ( -3.313708498984757167, 7.999999999999991118, 21.73655278392014978 ) ) ;
#55025=CARTESIAN_POINT ( 'NONE',  ( 7.188101187499992051, 8.802885111219154394E-16, 12.73655278187175277 ) ) ;
#55034=CARTESIAN_POINT ( 'NONE',  ( 3.313708498984762496, -7.999999999999989342, 14.98655278392014623 ) ) ;
#55035=CARTESIAN_POINT ( 'NONE',  ( -7.999999999835898379, -3.436314075762838161E-05, 19.01908381112063751 ) ) ;
#55040=CARTESIAN_POINT ( 'NONE',  ( -7.999999999999948486, 3.313708498984799355, 12.73655277982336465 ) ) ;
#55046=CARTESIAN_POINT ( 'NONE',  ( 2.977408999572650927, -7.188101187499990274, 19.95530278187175810 ) ) ;
#55051=CARTESIAN_POINT ( 'NONE',  ( -8.000000000000053291, -3.313708498984698547, 17.42405277982336287 ) ) ;
#55063=CARTESIAN_POINT ( 'NONE',  ( -5.873835977744188419, -5.451354504359680497, -0.3078279556938505190 ) ) ;
#55070=CARTESIAN_POINT ( 'NONE',  ( 7.188101187499991163, 2.977408999572648707, 14.70530278187175455 ) ) ;
#55089=CARTESIAN_POINT ( 'NONE',  ( -7.999999999999991118, 3.313708498984756723, 8.236552779823362869 ) ) ;
#55104=CARTESIAN_POINT ( 'NONE',  ( -7.999999999999989342, -3.313708498984762496, 9.980302784329824206 ) ) ;
#55125=( BOUNDED_CURVE ( )  B_SPLINE_CURVE ( 2, ( #8456, #3180, #67301, #72196, #9592, #37513, #25793, #14099, #20509, #31476, #49567 ),
 .UNSPECIFIED., .F., .F. ) 
 B_SPLINE_CURVE_WITH_KNOTS ( ( 3, 2, 2, 2, 2, 3 ),
 ( 0.1058924239672156403, 0.1125106849357718625, 0.1191289605202222601, 0.1257472361046726717, 0.1323655116891230554, 0.1323655657721681533 ),
 .UNSPECIFIED. ) 
 CURVE ( )  GEOMETRIC_REPRESENTATION_ITEM ( )  RATIONAL_B_SPLINE_CURVE ( ( 0.9999996637896906293, 0.9238797006168126824, 1.000000000000000000, 0.9238795325112867385, 1.000000000000000000, 0.9238795325112867385, 1.000000000000000000, 0.9238795325112867385, 1.000000000000000000, 0.9999993779608262745, 0.9999987559318189723 ) ) 
 REPRESENTATION_ITEM ( '' )  );
#55136=CARTESIAN_POINT ( 'NONE',  ( -2.977408999572647819, 7.188101187499991163, 7.205302781871750994 ) ) ;
#55149=CARTESIAN_POINT ( 'NONE',  ( 7.188101187499991163, 2.977408999572648707, 8.705302781871752771 ) ) ;
#55163=CARTESIAN_POINT ( 'NONE',  ( -7.188101187499992051, 0.000000000000000000, 6.361552781871754547 ) ) ;
#55180=CARTESIAN_POINT ( 'NONE',  ( -7.999999999999989342, -3.313708498984762496, 24.92405277982336997 ) ) ;
#55192=CARTESIAN_POINT ( 'NONE',  ( -7.999999999999989342, -3.313708498984762496, 2.611552783920144005 ) ) ;
#55199=ORIENTED_EDGE ( 'NONE', *, *, #29256, .F. ) ;
#55215=CARTESIAN_POINT ( 'NONE',  ( -7.188101187499990274, -2.977408999572651815, 1.580302781871753659 ) ) ;
#55228=CARTESIAN_POINT ( 'NONE',  ( 1.320432766682872962E-15, -7.188101187499992051, 27.36155278187175455 ) ) ;
#55233=CARTESIAN_POINT ( 'NONE',  ( 2.081755106360743568, 7.796932491752575523, -0.000000000000000000 ) ) ;
#55252=CARTESIAN_POINT ( 'NONE',  ( -5.082755093536317936, -5.082755093536320601, 20.04905278187175455 ) ) ;
#55273=CARTESIAN_POINT ( 'NONE',  ( -5.656854249492373476, -5.656854249492376141, 7.017802779823365533 ) ) ;
#55276=ORIENTED_EDGE ( 'NONE', *, *, #36030, .T. ) ;
#55279=CARTESIAN_POINT ( 'NONE',  ( 3.313708498984756279, 7.999999999999991118, 14.04905278392014800 ) ) ;
#55303=CARTESIAN_POINT ( 'NONE',  ( -6.062591786044946751, -5.219672483564715471, -0.3118205092643556720 ) ) ;
#55328=CARTESIAN_POINT ( 'NONE',  ( 7.999999999999991118, 9.797174393178815797E-16, 3.080302779823361981 ) ) ;
#55333=CARTESIAN_POINT ( 'NONE',  ( -7.188101187499991163, 2.977408999572646930, 25.76780278187175810 ) ) ;
#55359=CARTESIAN_POINT ( 'NONE',  ( 5.656854249492376141, -5.656854249492374365, 25.39280277982336642 ) ) ;
#55377=CARTESIAN_POINT ( 'NONE',  ( -3.313708498984758943, -7.999999999999989342, 16.29905278392014623 ) ) ;
#55398=CARTESIAN_POINT ( 'NONE',  ( 1.320432766682872962E-15, -7.188101187499992051, 15.36155278187175277 ) ) ;
#55401=EDGE_LOOP ( 'NONE', ( #27279, #16912, #527, #72929 ) ) ;
#55409=CARTESIAN_POINT ( 'NONE',  ( -5.656854249492373476, -5.656854249492376141, 7.205302783920144449 ) ) ;
#55420=CARTESIAN_POINT ( 'NONE',  ( 5.082755093536318824, 5.082755093536319713, 15.92405278187175632 ) ) ;
#55427=FACE_OUTER_BOUND ( 'NONE', #14187, .T. ) ;
#55437=CARTESIAN_POINT ( 'NONE',  ( 5.656854249492374365, 5.656854249492375253, 25.95530278392014623 ) ) ;
#55444=CARTESIAN_POINT ( 'NONE',  ( 5.082755093536320601, -5.082755093536318824, 17.42405278187175810 ) ) ;
#55450=CARTESIAN_POINT ( 'NONE',  ( 7.999999999999991118, 9.797174393178815797E-16, 9.080302779823364645 ) ) ;
#55459=CARTESIAN_POINT ( 'NONE',  ( -7.999999999999991118, 3.313708498984756723, 6.736552779823365533 ) ) ;
#55475=CARTESIAN_POINT ( 'NONE',  ( -4.898587196589407898E-16, 7.999999999999991118, 12.51155278432982421 ) ) ;
#55488=ORIENTED_EDGE ( 'NONE', *, *, #57616, .T. ) ;
#55503=VERTEX_POINT ( 'NONE', #27644 ) ;
#55507=CARTESIAN_POINT ( 'NONE',  ( -7.999999999999991118, 0.000000000000000000, 17.33030277982336287 ) ) ;
#55511=CARTESIAN_POINT ( 'NONE',  ( 5.082755093536320601, -5.082755093536318824, 8.049052781871752771 ) ) ;
#55512=ORIENTED_EDGE ( 'NONE', *, *, #72199, .F. ) ;
#55525=CARTESIAN_POINT ( 'NONE',  ( 5.082755093536318824, 5.082755093536319713, 13.29905278187175277 ) ) ;
#55539=CARTESIAN_POINT ( 'NONE',  ( -5.082755093536319713, 5.082755093536319713, 3.174052781871751439 ) ) ;
#55554=CARTESIAN_POINT ( 'NONE',  ( -3.313708498984757167, 7.999999999999991118, 26.04905277982336997 ) ) ;
#55565=CARTESIAN_POINT ( 'NONE',  ( 7.999999999999992895, -3.313708498984756279, 3.174052783920144893 ) ) ;
#55586=CARTESIAN_POINT ( 'NONE',  ( 7.188101187499992051, 8.802885111219154394E-16, 2.236552781871750550 ) ) ;
#55600=CARTESIAN_POINT ( 'NONE',  ( -5.082755093536317936, -5.082755093536320601, 27.17405278187175455 ) ) ;
#55625=CARTESIAN_POINT ( 'NONE',  ( -7.188101187499992051, 2.977408999572646930, 24.26780278187175810 ) ) ;
#55636=CARTESIAN_POINT ( 'NONE',  ( -3.313708498984759387, -7.999999999999989342, -0.2009472160798553286 ) ) ;
#55645=CARTESIAN_POINT ( 'NONE',  ( 7.999999999999991118, 9.797174393178815797E-16, 7.580302779823366421 ) ) ;
#55647=CARTESIAN_POINT ( 'NONE',  ( -7.999994982332486515, -3.313713516652264435, 20.61155298467860320 ) ) ;
#55652=CARTESIAN_POINT ( 'NONE',  ( 7.999999999999991118, 9.797174393178815797E-16, 1.580302779823364201 ) ) ;
#55663=CARTESIAN_POINT ( 'NONE',  ( 7.999999999999991118, 9.797174393178815797E-16, 19.58030277982336642 ) ) ;
#55675=CARTESIAN_POINT ( 'NONE',  ( -3.317071493978878571, 8.008118988124991233, 20.23186528394063544 ) ) ;
#55686=EDGE_CURVE ( 'NONE', #70510, #59338, #25470, .T. ) ;
#55709=CARTESIAN_POINT ( 'NONE',  ( -5.082755093536317936, -5.082755093536320601, 21.54905278187175455 ) ) ;
#55733=CARTESIAN_POINT ( 'NONE',  ( -5.656854249492375253, 5.656854249492375253, 24.64280277982336642 ) ) ;
#55751=CARTESIAN_POINT ( 'NONE',  ( -4.898587196589407898E-16, 7.999999999999991118, 20.14280278392014623 ) ) ;
#55772=CARTESIAN_POINT ( 'NONE',  ( 5.082755093536320601, -5.082755093536318824, 15.54905278187175455 ) ) ;
#55783=CARTESIAN_POINT ( 'NONE',  ( 3.313708498984762496, -7.999999999999989342, 10.48655278392014800 ) ) ;
#55788=CARTESIAN_POINT ( 'NONE',  ( 7.999999999999991118, 3.313708498984758055, 12.17405277982336642 ) ) ;
#55794=CARTESIAN_POINT ( 'NONE',  ( 1.320432766682872962E-15, -7.188101187499992051, 15.36155278187175277 ) ) ;
#55806=DIRECTION ( 'NONE',  ( -0.000000000000000000, -0.000000000000000000, 1.000000000000000000 ) ) ;
#55820=CARTESIAN_POINT ( 'NONE',  ( -7.188101187499991163, 2.977408999572646930, 16.76780278187175099 ) ) ;
#55838=CARTESIAN_POINT ( 'NONE',  ( 3.313708498984756279, 7.999999999999991118, 10.86155277982336820 ) ) ;
#55839=CYLINDRICAL_SURFACE ( 'NONE', #74636, 7.999999999999991118 ) ;
#55853=CARTESIAN_POINT ( 'NONE',  ( -3.313708498984757167, 7.999999999999991118, 12.60530278432982421 ) ) ;
#55877=CARTESIAN_POINT ( 'NONE',  ( -3.313708498984757611, 7.999999999999991118, 9.736552783920146226 ) ) ;
#55883=CARTESIAN_POINT ( 'NONE',  ( 7.188101187499991163, 2.977408999572648707, 0.8303027818717529929 ) ) ;
#55896=CARTESIAN_POINT ( 'NONE',  ( 5.082755093536318824, 5.082755093536319713, 10.29905278187175455 ) ) ;
#55941=CARTESIAN_POINT ( 'NONE',  ( -6.062585341144163031, -5.219679969245603957, -0.3118202219565458511 ) ) ;
#55964=AXIS2_PLACEMENT_3D ( 'NONE', #31355, #32112, #2692 ) ;
#55973=CARTESIAN_POINT ( 'NONE',  ( 3.313708498984762496, -7.999999999999989342, 10.29905277982336465 ) ) ;
#55974=CARTESIAN_POINT ( 'NONE',  ( 1.320432766682872962E-15, -7.188101187499992051, 22.86155278187175455 ) ) ;
#55996=CARTESIAN_POINT ( 'NONE',  ( -2.977408999572647819, 7.188101187499992051, 21.08030278187175810 ) ) ;
#56016=CARTESIAN_POINT ( 'NONE',  ( 7.999999999999991118, 3.313708498984757611, 7.674052779823366421 ) ) ;
#56020=( BOUNDED_CURVE ( )  B_SPLINE_CURVE ( 2, ( #33313, #50265, #56311, #68366, #22325, #62695, #5372, #11032, #67994 ),
 .UNSPECIFIED., .F., .F. ) 
 B_SPLINE_CURVE_WITH_KNOTS ( ( 3, 2, 2, 2, 3 ),
 ( 0.1578947368421052821, 0.1644736842105263552, 0.1710526315789474006, 0.1776315789473684459, 0.1842105263157894912 ),
 .UNSPECIFIED. ) 
 CURVE ( )  GEOMETRIC_REPRESENTATION_ITEM ( )  RATIONAL_B_SPLINE_CURVE ( ( 0.9999999999999996669, 0.9238795325112870716, 1.000000000000000000, 0.9238795325112867385, 1.000000000000000000, 0.9238795325112867385, 1.000000000000000000, 0.9238795325112864054, 1.000000000000000222 ) ) 
 REPRESENTATION_ITEM ( '' )  );
#56024=CARTESIAN_POINT ( 'NONE',  ( -4.898587196589407898E-16, 7.999999999999991118, 1.955302779823364645 ) ) ;
#56030=CARTESIAN_POINT ( 'NONE',  ( -7.999999999999991118, 3.313708498984757167, 20.42405278392015333 ) ) ;
#56046=CARTESIAN_POINT ( 'NONE',  ( 3.317071493978877683, 8.008118988124991233, 18.54436528394063188 ) ) ;
#56058=CARTESIAN_POINT ( 'NONE',  ( 7.999999999999991118, 9.797174393178815797E-16, 21.08030277982336642 ) ) ;
#56078=CARTESIAN_POINT ( 'NONE',  ( -7.188101187499990274, -2.977408999572651371, 24.45530278187175455 ) ) ;
#56079=CYLINDRICAL_SURFACE ( 'NONE', #64302, 7.999999999999991118 ) ;
#56103=CARTESIAN_POINT ( 'NONE',  ( -4.898587196589407898E-16, 7.999999999999991118, 24.45530277982336642 ) ) ;
#56122=CARTESIAN_POINT ( 'NONE',  ( -3.313708498984758943, -7.999999999999989342, 10.29905278392014623 ) ) ;
#56124=DIRECTION ( 'NONE',  ( -0.000000000000000000, -0.000000000000000000, 1.000000000000000000 ) ) ;
#56143=CARTESIAN_POINT ( 'NONE',  ( -7.188101187499992051, 2.977408999572646930, 16.39280278187175455 ) ) ;
#56166=CARTESIAN_POINT ( 'NONE',  ( -7.188101187499990274, -2.977408999572651371, 12.08030278187175099 ) ) ;
#56172=CARTESIAN_POINT ( 'NONE',  ( 1.469576158976822172E-15, -7.999999999999991118, 17.70530277982336642 ) ) ;
#56181=VECTOR ( 'NONE', #1012, 1000.000000000000000 ) ;
#56191=CARTESIAN_POINT ( 'NONE',  ( -2.977408999572648707, -7.188101187499990274, 15.64280278187175632 ) ) ;
#56206=CARTESIAN_POINT ( 'NONE',  ( -4.898587196589407898E-16, 7.999999999999991118, 3.455302779823362425 ) ) ;
#56221=CARTESIAN_POINT ( 'NONE',  ( -5.656854249492375253, 5.656854249492375253, 9.699052784329824206 ) ) ;
#56249=CARTESIAN_POINT ( 'NONE',  ( 5.082755093536318824, 5.082755093536319713, 2.424052781871750994 ) ) ;
#56262=CARTESIAN_POINT ( 'NONE',  ( 5.082755093536318824, 5.082755093536319713, 5.799052781871753659 ) ) ;
#56290=CARTESIAN_POINT ( 'NONE',  ( 7.999999999999991118, 3.313708498984757611, 28.67405277982336642 ) ) ;
#56303=CARTESIAN_POINT ( 'NONE',  ( 7.999999999999992895, -3.313708498984756279, 27.04280278432983309 ) ) ;
#56311=CARTESIAN_POINT ( 'NONE',  ( -5.656854249492375253, 5.656854249492375253, 24.64280277982336642 ) ) ;
#56339=CARTESIAN_POINT ( 'NONE',  ( 2.977408999572646486, 7.188101187499991163, 17.51780278187175455 ) ) ;
#56362=CARTESIAN_POINT ( 'NONE',  ( -7.188101187499990274, -2.977408999572651815, 13.95530278187175455 ) ) ;
#56380=CARTESIAN_POINT ( 'NONE',  ( 7.999999999999991118, 9.797174393178815797E-16, 3.080302779823361981 ) ) ;
#56390=CARTESIAN_POINT ( 'NONE',  ( -5.656854249492373476, -5.656854249492376141, 10.20530278392014623 ) ) ;
#56409=CARTESIAN_POINT ( 'NONE',  ( -3.317071493978880348, -8.008118988124989457, 20.79436528394063188 ) ) ;
#56410=CARTESIAN_POINT ( 'NONE',  ( -5.656854249492375253, 5.656854249492375253, 23.33030278392014978 ) ) ;
#56445=CARTESIAN_POINT ( 'NONE',  ( 7.188101187499993827, -2.977408999572645598, 25.01780278187175455 ) ) ;
#56468=EDGE_CURVE ( 'NONE', #74609, #19989, #15, .T. ) ;
#56473=CARTESIAN_POINT ( 'NONE',  ( 7.999999999999991118, 9.797174393178815797E-16, 28.58030277982336642 ) ) ;
#56489=CARTESIAN_POINT ( 'NONE',  ( -3.313708498984757611, 7.999999999999991118, 23.04905277982336287 ) ) ;
#56491=CARTESIAN_POINT ( 'NONE',  ( 3.313708498984756279, 7.999999999999991118, 11.04905278392014800 ) ) ;
#56494=ORIENTED_EDGE ( 'NONE', *, *, #59880, .F. ) ;
#56515=CARTESIAN_POINT ( 'NONE',  ( 5.082755093536318824, 5.082755093536319713, 14.42405278187175455 ) ) ;
#56538=CARTESIAN_POINT ( 'NONE',  ( 7.188101187499993827, -2.977408999572645598, 15.64280278187175277 ) ) ;
#56565=CARTESIAN_POINT ( 'NONE',  ( -4.401442555609577197E-16, 7.188101187499992051, 16.48655278187175810 ) ) ;
#56568=CARTESIAN_POINT ( 'NONE',  ( 1.469576158976822172E-15, -7.999999999999991118, 1.392802783920146004 ) ) ;
#56580=CARTESIAN_POINT ( 'NONE',  ( 7.999999999999992895, -3.313708498984756279, 4.486552779823363757 ) ) ;
#56584=PRODUCT_DEFINITION_SHAPE ( 'NONE', 'NONE',  #25152 ) ;
#56598=CARTESIAN_POINT ( 'NONE',  ( 3.313708498984762496, -7.999999999999989342, 4.355302784329824206 ) ) ;
#56600=CARTESIAN_POINT ( 'NONE',  ( -3.313708498984757611, 7.999999999999991118, 5.049052779823363757 ) ) ;
#56609=DIRECTION ( 'NONE',  ( 1.000000000000000000, 0.000000000000000000, 0.000000000000000000 ) ) ;
#56628=CARTESIAN_POINT ( 'NONE',  ( -5.082755093536317936, -5.082755093536320601, 0.1740527818717522990 ) ) ;
#56630=B_SPLINE_CURVE_WITH_KNOTS ( 'NONE', 3,
 ( #28905, #51923, #23244, #16450 ),
 .UNSPECIFIED., .F., .F.,
 ( 4, 4 ),
 ( 0.000000000000000000, 4.515620356819685806E-05 ),
 .UNSPECIFIED. ) ;
#56641=CARTESIAN_POINT ( 'NONE',  ( 7.188101187499991163, 2.977408999572648707, 7.205302781871754547 ) ) ;
#56669=CARTESIAN_POINT ( 'NONE',  ( -5.656854249492375253, 5.656854249492375253, 21.64280277982336997 ) ) ;
#56682=CARTESIAN_POINT ( 'NONE',  ( 3.313708498984756279, 7.999999999999991118, 3.549052783920144893 ) ) ;
#56688=VECTOR ( 'NONE', #37223, 1000.000000000000000 ) ;
#56715=CARTESIAN_POINT ( 'NONE',  ( -4.401442555609577197E-16, 7.188101187499992051, 16.11155278187175455 ) ) ;
#56737=CARTESIAN_POINT ( 'NONE',  ( 2.977408999572650927, -7.188101187499990274, 17.33030278187175455 ) ) ;
#56756=CARTESIAN_POINT ( 'NONE',  ( -5.656854249492373476, -5.656854249492376141, 1.017802779823363757 ) ) ;
#56757=CARTESIAN_POINT ( 'NONE',  ( 7.999999999999992895, -3.313708498984756279, 21.17405278392015333 ) ) ;
#56770=CARTESIAN_POINT ( 'NONE',  ( 6.366783985983791361, -4.860392236259310828, -0.000000000000000000 ) ) ;
#56784=CARTESIAN_POINT ( 'NONE',  ( 1.471067592899761672E-15, -8.008118988124991233, 20.88811528394063188 ) ) ;
#56796=CARTESIAN_POINT ( 'NONE',  ( 0.000000000000000000, 0.000000000000000000, 30.00000000000000000 ) ) ;
#56817=CARTESIAN_POINT ( 'NONE',  ( 5.082755093536320601, -5.082755093536318824, 23.42405278187175455 ) ) ;
#56828=CARTESIAN_POINT ( 'NONE',  ( 3.313708498984756279, 7.999999999999991118, 27.54905278392014623 ) ) ;
#56843=CARTESIAN_POINT ( 'NONE',  ( -7.999999999999991118, 0.000000000000000000, 20.33030277982336642 ) ) ;
#56863=CARTESIAN_POINT ( 'NONE',  ( 7.999999999999991118, 9.797174393178815797E-16, 12.26780278392014623 ) ) ;
#56869=DIRECTION ( 'NONE',  ( -0.000000000000000000, -0.000000000000000000, 1.000000000000000000 ) ) ;
#56913=CARTESIAN_POINT ( 'NONE',  ( -7.188101187499990274, -2.977408999572651371, 15.08030278187175455 ) ) ;
#56927=ORIENTED_EDGE ( 'NONE', *, *, #44562, .T. ) ;
#56936=CARTESIAN_POINT ( 'NONE',  ( 5.082755093536320601, -5.082755093536318824, 11.42405278187175455 ) ) ;
#56939=CARTESIAN_POINT ( 'NONE',  ( 7.999999999999991118, 3.313708498984757611, 0.2303027843298232069 ) ) ;
#56950=CARTESIAN_POINT ( 'NONE',  ( 7.999999999999991118, 3.313708498984757611, 4.674052779823363757 ) ) ;
#56951=CARTESIAN_POINT ( 'NONE',  ( -7.999999999999991118, 0.000000000000000000, 22.01780278392014623 ) ) ;
#56968=CARTESIAN_POINT ( 'NONE',  ( -4.898587196589407898E-16, 7.999999999999991118, 8.011552784329822430 ) ) ;
#56996=CARTESIAN_POINT ( 'NONE',  ( 7.188101187499992051, 8.802885111219154394E-16, 2.236552781871750550 ) ) ;
#57010=CARTESIAN_POINT ( 'NONE',  ( -7.188101187499991163, 2.977408999572646930, 6.267802781871754547 ) ) ;
#57021=CARTESIAN_POINT ( 'NONE',  ( -5.082755093536317936, -5.082755093536320601, 26.04905278187175810 ) ) ;
#57025=CARTESIAN_POINT ( 'NONE',  ( -4.401442555609577197E-16, 7.188101187499992051, 1.486552781871753437 ) ) ;
#57040=CARTESIAN_POINT ( 'NONE',  ( 3.313708498984756279, 7.999999999999991118, 21.36155277982336997 ) ) ;
#57053=CARTESIAN_POINT ( 'NONE',  ( -7.999999999999991118, 3.313708498984756723, 24.79280278432983664 ) ) ;
#57083=CARTESIAN_POINT ( 'NONE',  ( 5.082755093536318824, 5.082755093536319713, 21.92405278187175455 ) ) ;
#57100=CARTESIAN_POINT ( 'NONE',  ( 7.999999999999991118, 3.313708498984758055, 25.86155278392014267 ) ) ;
#57106=CARTESIAN_POINT ( 'NONE',  ( 7.188101187499992051, 2.977408999572647819, 19.20530278187175455 ) ) ;
#57132=CARTESIAN_POINT ( 'NONE',  ( 1.469576158976822172E-15, -7.999999999999991118, 14.89280278392014623 ) ) ;
#57155=CARTESIAN_POINT ( 'NONE',  ( -8.008118988124991233, 0.000000000000000000, 22.01311528394063188 ) ) ;
#57175=CARTESIAN_POINT ( 'NONE',  ( 5.656854249492376141, -5.656854249492374365, 9.080302783920146226 ) ) ;
#57189=CARTESIAN_POINT ( 'NONE',  ( 1.320432766682872962E-15, -7.188101187499992051, 18.73655278187175455 ) ) ;
#57209=CARTESIAN_POINT ( 'NONE',  ( -0.1292575518527070144, -8.001915877911162767, -0.000000000000000000 ) ) ;
#57215=CARTESIAN_POINT ( 'NONE',  ( 5.656854249492374365, 5.656854249492375253, 22.76780277982336642 ) ) ;
#57219=EDGE_LOOP ( 'NONE', ( #61532, #66771, #69033, #65688 ) ) ;
#57234=CARTESIAN_POINT ( 'NONE',  ( -4.898587196589407898E-16, 7.999999999999991118, 15.64280278392014800 ) ) ;
#57286=CARTESIAN_POINT ( 'NONE',  ( -2.977408999572648707, -7.188101187499990274, 13.76780278187175455 ) ) ;
#57288=ORIENTED_EDGE ( 'NONE', *, *, #4747, .T. ) ;
#57312=CARTESIAN_POINT ( 'NONE',  ( -2.977408999572648707, -7.188101187499990274, 12.64280278187175277 ) ) ;
#57314=CARTESIAN_POINT ( 'NONE',  ( -7.999999999961167951, -1.666173683171983354E-05, 1.018425797410095646 ) ) ;
#57325=CARTESIAN_POINT ( 'NONE',  ( 5.656854249492374365, 5.656854249492375253, 3.267802779823362425 ) ) ;
#57341=CARTESIAN_POINT ( 'NONE',  ( -7.999999999999989342, -3.313708498984762496, 3.980302784329822874 ) ) ;
#57346=CARTESIAN_POINT ( 'NONE',  ( -4.401442555609577197E-16, 7.188101187499992051, 25.11155278187175810 ) ) ;
#57354=AXIS2_PLACEMENT_3D ( 'NONE', #63097, #11422, #34459 ) ;
#57361=CARTESIAN_POINT ( 'NONE',  ( 3.313708498984762496, -7.999999999999989342, 22.48655278392014623 ) ) ;
#57371=CARTESIAN_POINT ( 'NONE',  ( -2.977408999572647819, 7.188101187499991163, 28.20530278187175455 ) ) ;
#57384=CARTESIAN_POINT ( 'NONE',  ( -2.977408999572648707, -7.188101187499990274, 5.142802781871752771 ) ) ;
#57405=ADVANCED_FACE ( 'NONE', ( #34759 ), #42226, .F. ) ;
#57415=CARTESIAN_POINT ( 'NONE',  ( 5.656854249492376141, -5.656854249492374365, 22.39280277982336997 ) ) ;
#57422=CARTESIAN_POINT ( 'NONE',  ( 5.656854249492376141, -5.656854249492374365, 0.08030278392014492117 ) ) ;
#57429=CARTESIAN_POINT ( 'NONE',  ( 7.999999999999992895, -3.313708498984756279, 21.04280278432983309 ) ) ;
#57447=PLANE ( 'NONE',  #237 ) ;
#57451=ADVANCED_FACE ( 'NONE', ( #70182 ), #18492, .F. ) ;
#57465=CARTESIAN_POINT ( 'NONE',  ( 5.082755093536320601, -5.082755093536318824, 17.04905278187175810 ) ) ;
#57491=CARTESIAN_POINT ( 'NONE',  ( -5.082755093536319713, 5.082755093536319713, 15.17405278187175455 ) ) ;
#57511=CARTESIAN_POINT ( 'NONE',  ( -7.999999999999991118, 3.313708498984756723, 5.236552779823363757 ) ) ;
#57538=CARTESIAN_POINT ( 'NONE',  ( 5.662595241051934458, 5.662595241051935346, 12.45061528394063011 ) ) ;
#57556=CARTESIAN_POINT ( 'NONE',  ( 5.656854249492376141, -5.656854249492374365, 6.080302783920147114 ) ) ;
#57570=CARTESIAN_POINT ( 'NONE',  ( 2.977408999572646486, 7.188101187499991163, 17.89280278187175455 ) ) ;
#57594=CARTESIAN_POINT ( 'NONE',  ( -3.313708498984758943, -7.999999999999989342, 19.11155277982336997 ) ) ;
#57612=CARTESIAN_POINT ( 'NONE',  ( 7.999999999999991118, 3.313708498984757611, 13.86155278392014623 ) ) ;
#57616=EDGE_CURVE ( 'NONE', #60098, #14756, #63593, .T. ) ;
#57625=CARTESIAN_POINT ( 'NONE',  ( -3.313708498984759387, -7.999999999999989342, 26.61155277982336997 ) ) ;
#57628=DIRECTION ( 'NONE',  ( 0.000000000000000000, 0.000000000000000000, -1.000000000000000000 ) ) ;
#57651=CARTESIAN_POINT ( 'NONE',  ( 5.656854249492374365, 5.656854249492375253, 6.267802779823364645 ) ) ;
#57660=ORIENTED_EDGE ( 'NONE', *, *, #26521, .T. ) ;
#57662=CARTESIAN_POINT ( 'NONE',  ( -2.977408999572648707, -7.188101187499990274, 9.267802781871756324 ) ) ;
#57687=CARTESIAN_POINT ( 'NONE',  ( -7.188101187499990274, -2.977408999572651371, 9.455302781871754547 ) ) ;
#57690=CARTESIAN_POINT ( 'NONE',  ( -5.656854249492373476, -5.656854249492376141, -0.4259472156701774592 ) ) ;
#57701=CARTESIAN_POINT ( 'NONE',  ( 3.313708498984762496, -7.999999999999989342, 2.799052779823366421 ) ) ;
#57702=DIRECTION ( 'NONE',  ( -0.000000000000000000, -0.9659258262890700886, -0.2588190451025146888 ) ) ;
#57716=CARTESIAN_POINT ( 'NONE',  ( 7.999999999999992895, -3.313708498984756279, 7.542802784329822430 ) ) ;
#57723=CARTESIAN_POINT ( 'NONE',  ( 7.188101187499992051, 8.802885111219154394E-16, 24.73655278187175810 ) ) ;
#57736=CARTESIAN_POINT ( 'NONE',  ( -5.656854249492375253, 5.656854249492375253, 18.83030278392014623 ) ) ;
#57747=CARTESIAN_POINT ( 'NONE',  ( -4.401442555609577197E-16, 7.188101187499992051, 22.11155278187175455 ) ) ;
#57760=CARTESIAN_POINT ( 'NONE',  ( -5.082755093536319713, 5.082755093536319713, 6.174052781871754547 ) ) ;
#57764=CARTESIAN_POINT ( 'NONE',  ( 5.662595241051936235, -5.662595241051934458, 1.575615283940630107 ) ) ;
#57771=CARTESIAN_POINT ( 'NONE',  ( 2.977408999572650927, -7.188101187499990274, 26.33030278187175810 ) ) ;
#57789=CARTESIAN_POINT ( 'NONE',  ( 7.999999999999991118, 9.797174393178815797E-16, 24.08030277982336642 ) ) ;
#57804=CARTESIAN_POINT ( 'NONE',  ( -3.313708498984757167, 7.999999999999991118, 23.10530278432982954 ) ) ;
#57806=CIRCLE ( 'NONE', #51752, 6.000000000000015099 ) ;
#57829=CARTESIAN_POINT ( 'NONE',  ( -3.313708498984757611, 7.999999999999991118, 12.73655278392014623 ) ) ;
#57839=CARTESIAN_POINT ( 'NONE',  ( 7.188101187499993827, -2.977408999572645598, 14.14280278187175455 ) ) ;
#57861=CARTESIAN_POINT ( 'NONE',  ( -4.401442555609577197E-16, 7.188101187499992051, 17.98655278187175810 ) ) ;
#57881=CARTESIAN_POINT ( 'NONE',  ( 7.999999999999991118, 9.797174393178815797E-16, 6.080302779823364645 ) ) ;
#57909=CARTESIAN_POINT ( 'NONE',  ( -3.317071493978880348, -8.008118988124989457, 11.79436528394062833 ) ) ;
#57917=CARTESIAN_POINT ( 'NONE',  ( -2.977408999572647819, -7.188101187499990274, 10.76780278187175632 ) ) ;
#57928=VECTOR ( 'NONE', #13094, 1000.000000000000000 ) ;
#57933=CARTESIAN_POINT ( 'NONE',  ( 5.656854249492376141, -5.656854249492374365, 10.58030278392014800 ) ) ;
#57949=CARTESIAN_POINT ( 'NONE',  ( -7.188101187499992051, 0.000000000000000000, 16.86155278187175810 ) ) ;
#57952=CARTESIAN_POINT ( 'NONE',  ( 5.656854249492376141, -5.656854249492374365, 19.58030278392014978 ) ) ;
#57967=CARTESIAN_POINT ( 'NONE',  ( 7.999999999999991118, 9.797174393178815797E-16, 25.58030277982336997 ) ) ;
#57974=CARTESIAN_POINT ( 'NONE',  ( 5.656854249492374365, 5.656854249492375253, 19.76780277982336642 ) ) ;
#57978=EDGE_LOOP ( 'NONE', ( #41627, #66716, #27737, #20151 ) ) ;
#57994=CARTESIAN_POINT ( 'NONE',  ( 7.999999999999991118, 3.313708498984757611, 6.361552783920146226 ) ) ;
#57996=CARTESIAN_POINT ( 'NONE',  ( -7.188101187499992051, 0.000000000000000000, 28.48655278187175810 ) ) ;
#58020=( BOUNDED_CURVE ( )  B_SPLINE_CURVE ( 2, ( #28254, #44491, #51262, #16540, #56568, #4882, #67504, #45602, #57314 ),
 .UNSPECIFIED., .F., .F. ) 
 B_SPLINE_CURVE_WITH_KNOTS ( ( 3, 2, 2, 2, 3 ),
 ( 0.9265586498208127075, 0.9331768574084092771, 0.9397951329928664332, 0.9464134085773237004, 0.9530316461170064146 ),
 .UNSPECIFIED. ) 
 CURVE ( )  GEOMETRIC_REPRESENTATION_ITEM ( )  RATIONAL_B_SPLINE_CURVE ( ( 0.9999984358766603743, 0.9238803145809916240, 1.000000000000000000, 0.9238795325112867385, 1.000000000000000000, 0.9238795325112867385, 1.000000000000000000, 0.9238799700853922436, 0.9999991248568196323 ) ) 
 REPRESENTATION_ITEM ( '' )  );
#58023=VERTEX_POINT ( 'NONE', #6046 ) ;
#58030=AXIS2_PLACEMENT_3D ( 'NONE', #18140, #52845, #25908 ) ;
#58032=DIRECTION ( 'NONE',  ( -0.000000000000000000, -0.000000000000000000, 1.000000000000000000 ) ) ;
#58039=CARTESIAN_POINT ( 'NONE',  ( -7.188101187499991163, 2.977408999572646930, 5.892802781871754547 ) ) ;
#58063=CARTESIAN_POINT ( 'NONE',  ( 5.082755093536318824, 5.082755093536319713, 7.299052781871751883 ) ) ;
#58074=LINE ( 'NONE', #6385, #22702 ) ;
#58077=CARTESIAN_POINT ( 'NONE',  ( -7.999999999999991118, 3.313708498984756723, 24.92405278392015333 ) ) ;
#58093=CARTESIAN_POINT ( 'NONE',  ( 7.999999999714877852, 6.754118554053788561E-05, 0.2678047518895779744 ) ) ;
#58096=CARTESIAN_POINT ( 'NONE',  ( -5.082755093536317936, -5.082755093536320601, 24.17405278187175455 ) ) ;
#58106=CARTESIAN_POINT ( 'NONE',  ( 7.999999999999991118, 3.313708498984757611, 22.86155278392014623 ) ) ;
#58120=CARTESIAN_POINT ( 'NONE',  ( 2.977408999572646486, 7.188101187499991163, 26.51780278187175455 ) ) ;
#58136=CARTESIAN_POINT ( 'NONE',  ( -7.188101187499991163, 2.977408999572646930, 1.767802781871753881 ) ) ;
#58141=CARTESIAN_POINT ( 'NONE',  ( -8.008118988124991233, 3.317071493978878127, 3.919365283940628775 ) ) ;
#58166=CARTESIAN_POINT ( 'NONE',  ( -5.656854249492373476, -5.656854249492376141, 19.01780277982336642 ) ) ;
#58180=CARTESIAN_POINT ( 'NONE',  ( 7.999999999999991118, 3.313708498984757611, 25.73030278432982598 ) ) ;
#58212=CARTESIAN_POINT ( 'NONE',  ( -7.188101187499992051, 0.000000000000000000, 10.48655278187175455 ) ) ;
#58233=CARTESIAN_POINT ( 'NONE',  ( -3.313708498984757611, 7.999999999999991118, 26.23655278392014623 ) ) ;
#58239=CARTESIAN_POINT ( 'NONE',  ( -4.401442555609577197E-16, 7.188101187499992051, 11.98655278187175632 ) ) ;
#58282=CARTESIAN_POINT ( 'NONE',  ( 5.662595241051934458, 5.662595241051935346, 15.45061528394063011 ) ) ;
#58287=CARTESIAN_POINT ( 'NONE',  ( 5.082755093536318824, 5.082755093536319713, 8.424052781871752771 ) ) ;
#58300=CARTESIAN_POINT ( 'NONE',  ( 7.999999999999991118, 9.797174393178815797E-16, 3.267802783920144449 ) ) ;
#58315=CARTESIAN_POINT ( 'NONE',  ( -2.977408999572648707, -7.188101187499990274, 20.14280278187176165 ) ) ;
#58317=LINE ( 'NONE', #53012, #14231 ) ;
#58319=CARTESIAN_POINT ( 'NONE',  ( -3.313708498984759387, -7.999999999999989342, 19.29905278392014978 ) ) ;
#58323=CARTESIAN_POINT ( 'NONE',  ( -5.082755093536317936, -5.082755093536320601, 26.04905278187175810 ) ) ;
#58334=CARTESIAN_POINT ( 'NONE',  ( 1.181073143174618423, -7.934766031977416922, 0.000000000000000000 ) ) ;
#58342=CARTESIAN_POINT ( 'NONE',  ( -7.999999999999991118, 3.313708498984756723, 17.23655277982336642 ) ) ;
#58359=CARTESIAN_POINT ( 'NONE',  ( -5.656854249492373476, -5.656854249492376141, 4.205302783920145338 ) ) ;
#58380=ORIENTED_EDGE ( 'NONE', *, *, #13294, .F. ) ;
#58389=EDGE_CURVE ( 'NONE', #13756, #26953, #49050, .T. ) ;
#58399=CARTESIAN_POINT ( 'NONE',  ( 7.999999999752645863, -6.290875383172500320E-05, 1.767801038436179750 ) ) ;
#58406=CARTESIAN_POINT ( 'NONE',  ( 7.188101187499991163, 2.977408999572648707, 8.330302781871752771 ) ) ;
#58428=CARTESIAN_POINT ( 'NONE',  ( 1.320432766682872962E-15, -7.188101187499992051, 12.73655278187175277 ) ) ;
#58431=CARTESIAN_POINT ( 'NONE',  ( -3.313708498984758943, -7.999999999999989342, 1.167802784329823984 ) ) ;
#58441=CARTESIAN_POINT ( 'NONE',  ( 5.656854249492376141, -5.656854249492374365, 27.08030278392014978 ) ) ;
#58472=CARTESIAN_POINT ( 'NONE',  ( 7.999999999999991118, 9.797174393178815797E-16, 18.26780278392014623 ) ) ;
#58480=ORIENTED_EDGE ( 'NONE', *, *, #8790, .F. ) ;
#58483=CARTESIAN_POINT ( 'NONE',  ( -5.082755093536317936, -5.082755093536320601, 24.17405278187175455 ) ) ;
#58484=ORIENTED_EDGE ( 'NONE', *, *, #27952, .T. ) ;
#58499=CARTESIAN_POINT ( 'NONE',  ( 8.008118988124991233, 3.317071493978879015, 4.856865283940630107 ) ) ;
#58524=CARTESIAN_POINT ( 'NONE',  ( -3.313708498984758943, -7.999999999999989342, 13.11155277982336465 ) ) ;
#58538=CARTESIAN_POINT ( 'NONE',  ( -3.313708498984758943, -7.999999999999989342, 20.66780278432982598 ) ) ;
#58571=CARTESIAN_POINT ( 'NONE',  ( -7.188101187499991163, 2.977408999572646930, 10.39280278187175810 ) ) ;
#58595=CARTESIAN_POINT ( 'NONE',  ( -5.082755093536317936, -5.082755093536320601, 9.549052781871754547 ) ) ;
#58599=CARTESIAN_POINT ( 'NONE',  ( 8.000000000000014211, -3.313708498984734518, 20.98655277982335932 ) ) ;
#58640=CARTESIAN_POINT ( 'NONE',  ( 8.008118988124991233, 9.807117285998411148E-16, 13.76311528394063011 ) ) ;
#58647=CARTESIAN_POINT ( 'NONE',  ( -7.188101187499990274, -2.977408999572651815, 10.58030278187175455 ) ) ;
#58661=CARTESIAN_POINT ( 'NONE',  ( -7.999999999999989342, -3.313708498984762496, 2.611552783920144005 ) ) ;
#58676=CARTESIAN_POINT ( 'NONE',  ( -5.082755093536317936, -5.082755093536320601, 15.54905278187175632 ) ) ;
#58678=CARTESIAN_POINT ( 'NONE',  ( 7.999999999999991118, 9.797174393178815797E-16, 3.080302779823361981 ) ) ;
#58681=CARTESIAN_POINT ( 'NONE',  ( 7.999999999999992895, -3.313708498984756279, 19.67405278392015333 ) ) ;
#58683=CARTESIAN_POINT ( 'NONE',  ( 7.999999999999950262, -3.313708498984798467, 5.986552779823362869 ) ) ;
#58690=CARTESIAN_POINT ( 'NONE',  ( -5.656854249492375253, 5.656854249492375253, 26.14280277982336997 ) ) ;
#58692=AXIS2_PLACEMENT_3D ( 'NONE', #43622, #61355, #3270 ) ;
#58696=CARTESIAN_POINT ( 'NONE',  ( 3.262048642599709058, -7.308067487734634327, -0.000000000000000000 ) ) ;
#58702=CARTESIAN_POINT ( 'NONE',  ( 5.656854249492376141, -5.656854249492374365, 14.89280277982336642 ) ) ;
#58720=CARTESIAN_POINT ( 'NONE',  ( 5.656854249492376141, -5.656854249492374365, 7.580302783920144449 ) ) ;
#58739=LINE ( 'NONE', #74592, #59131 ) ;
#58771=CARTESIAN_POINT ( 'NONE',  ( 7.188101187499992051, 8.802885111219154394E-16, 5.236552781871753659 ) ) ;
#58794=CARTESIAN_POINT ( 'NONE',  ( -5.082755093536319713, 5.082755093536319713, 4.674052781871752771 ) ) ;
#58807=CARTESIAN_POINT ( 'NONE',  ( 7.999999999999992895, -3.313708498984756279, 25.67405278392015333 ) ) ;
#58824=CARTESIAN_POINT ( 'NONE',  ( 7.999999999971009856, 2.153409470846384379E-05, 12.26780339315719814 ) ) ;
#58830=CARTESIAN_POINT ( 'NONE',  ( 2.977408999572646486, 7.188101187499992051, 25.01780278187175810 ) ) ;
#58839=CARTESIAN_POINT ( 'NONE',  ( 1.469576158976822172E-15, -7.999999999999991118, 19.39280278392014978 ) ) ;
#58848=AXIS2_PLACEMENT_3D ( 'NONE', #49371, #10138, #26350 ) ;
#58850=CARTESIAN_POINT ( 'NONE',  ( 2.977408999572650927, -7.188101187499990274, 25.95530278187175455 ) ) ;
#58861=VECTOR ( 'NONE', #66737, 1000.000000000000000 ) ;
#58865=CARTESIAN_POINT ( 'NONE',  ( 0.000000000000000000, 0.000000000000000000, 30.00000000000000000 ) ) ;
#58868=CARTESIAN_POINT ( 'NONE',  ( -5.662595241051935346, 5.662595241051935346, 3.825615283940628775 ) ) ;
#58875=CARTESIAN_POINT ( 'NONE',  ( 7.188101187499991163, 2.977408999572648707, 19.20530278187175810 ) ) ;
#58878=( BOUNDED_CURVE ( )  B_SPLINE_CURVE ( 2, ( #40981, #28537, #10817, #51545, #39494, #10448, #46630, #5911, #11193 ),
 .UNSPECIFIED., .F., .F. ) 
 B_SPLINE_CURVE_WITH_KNOTS ( ( 3, 2, 2, 2, 3 ),
 ( 0.7105263157894737835, 0.7171052631578948011, 0.7236842105263159297, 0.7302631578947369473, 0.7368421052631579649 ),
 .UNSPECIFIED. ) 
 CURVE ( )  GEOMETRIC_REPRESENTATION_ITEM ( )  RATIONAL_B_SPLINE_CURVE ( ( 0.9999999999999986677, 0.9238795325112880708, 1.000000000000000000, 0.9238795325112867385, 1.000000000000000000, 0.9238795325112867385, 1.000000000000000000, 0.9238795325112854062, 1.000000000000001332 ) ) 
 REPRESENTATION_ITEM ( '' )  );
#58887=CARTESIAN_POINT ( 'NONE',  ( -7.999999999999991118, 0.000000000000000000, 18.83030277982336642 ) ) ;
#58895=CARTESIAN_POINT ( 'NONE',  ( -7.999999999999991118, 3.313708498984756723, 17.23655277982336642 ) ) ;
#58902=ORIENTED_EDGE ( 'NONE', *, *, #13708, .F. ) ;
#58911=CARTESIAN_POINT ( 'NONE',  ( 5.656854249492374365, 5.656854249492375253, 16.82405278432982954 ) ) ;
#58943=CARTESIAN_POINT ( 'NONE',  ( -7.188101187499990274, -2.977408999572651371, 13.58030278187175277 ) ) ;
#58966=CARTESIAN_POINT ( 'NONE',  ( -7.188101187499992051, 2.977408999572646930, 13.76780278187175455 ) ) ;
#58998=CARTESIAN_POINT ( 'NONE',  ( -7.999999999999991118, 0.000000000000000000, 9.830302779823364645 ) ) ;
#59014=CARTESIAN_POINT ( 'NONE',  ( -8.008118988124991233, 3.317071493978878127, 14.41936528394063188 ) ) ;
#59019=CARTESIAN_POINT ( 'NONE',  ( 7.188101187499993827, -2.977408999572645598, 9.642802781871756324 ) ) ;
#59033=CARTESIAN_POINT ( 'NONE',  ( 2.977408999572646486, 7.188101187499991163, 28.01780278187175455 ) ) ;
#59049=CARTESIAN_POINT ( 'NONE',  ( 2.977408999572650927, -7.188101187499990274, 11.33030278187175632 ) ) ;
#59052=CARTESIAN_POINT ( 'NONE',  ( -7.999970022586251339, -3.313738476398500943, 19.11155398332591915 ) ) ;
#59056=CARTESIAN_POINT ( 'NONE',  ( -2.977408999572647819, 7.188101187499992051, 28.58030278187176521 ) ) ;
#59074=CARTESIAN_POINT ( 'NONE',  ( -7.999999999999991118, 0.000000000000000000, 15.83030277982336642 ) ) ;
#59082=ORIENTED_EDGE ( 'NONE', *, *, #67632, .F. ) ;
#59131=VECTOR ( 'NONE', #45917, 1000.000000000000000 ) ;
#59141=CARTESIAN_POINT ( 'NONE',  ( 2.977408999572646486, 7.188101187499991163, 26.89280278187175455 ) ) ;
#59166=CARTESIAN_POINT ( 'NONE',  ( 7.188101187499992051, 8.802885111219154394E-16, 2.611552781871750994 ) ) ;
#59170=VERTEX_POINT ( 'NONE', #24862 ) ;
#59180=CARTESIAN_POINT ( 'NONE',  ( 7.999999999999991118, 9.797174393178815797E-16, 25.76780278392014978 ) ) ;
#59200=CARTESIAN_POINT ( 'NONE',  ( 2.977408999572646486, 7.188101187499992051, 22.01780278187175455 ) ) ;
#59209=CARTESIAN_POINT ( 'NONE',  ( 7.999999999999991118, 9.797174393178815797E-16, 16.76780278392014978 ) ) ;
#59220=CARTESIAN_POINT ( 'NONE',  ( 1.320432766682872962E-15, -7.188101187499992051, 22.86155278187175455 ) ) ;
#59232=CARTESIAN_POINT ( 'NONE',  ( 5.082755093536320601, -5.082755093536318824, 2.424052781871754103 ) ) ;
#59239=CARTESIAN_POINT ( 'NONE',  ( 8.008118988124993010, -3.317071493978877239, 6.169365283940631883 ) ) ;
#59244=CARTESIAN_POINT ( 'NONE',  ( 7.188101187499991163, 2.977408999572648707, 22.20530278187175810 ) ) ;
#59261=CARTESIAN_POINT ( 'NONE',  ( 7.999999999999991118, 9.797174393178815797E-16, 18.08030277982336642 ) ) ;
#59276=CARTESIAN_POINT ( 'NONE',  ( 3.313708498984762496, -7.999999999999989342, 17.85530278432982598 ) ) ;
#59309=CARTESIAN_POINT ( 'NONE',  ( 2.977408999572650927, -7.188101187499990274, 15.45530278187175455 ) ) ;
#59332=CARTESIAN_POINT ( 'NONE',  ( -5.082755093536319713, 5.082755093536319713, 9.174052781871752771 ) ) ;
#59338=VERTEX_POINT ( 'NONE', #32794 ) ;
#59354=CARTESIAN_POINT ( 'NONE',  ( -6.062601303906716588, -5.219661428662635494, 1.000679062340938064 ) ) ;
#59364=ORIENTED_EDGE ( 'NONE', *, *, #36305, .T. ) ;
#59376=CARTESIAN_POINT ( 'NONE',  ( 5.662595241051936235, -5.662595241051934458, 9.075615283940630107 ) ) ;
#59382=CARTESIAN_POINT ( 'NONE',  ( 5.082755093536318824, 5.082755093536319713, 6.924052781871750994 ) ) ;
#59388=ADVANCED_FACE ( 'NONE', ( #55427 ), #44471, .F. ) ;
#59393=CARTESIAN_POINT ( 'NONE',  ( 0.000000000000000000, 0.000000000000000000, 30.00000000000000000 ) ) ;
#59394=CARTESIAN_POINT ( 'NONE',  ( -3.313708498984758943, -7.999999999999989342, 2.799052783920144005 ) ) ;
#59423=FACE_OUTER_BOUND ( 'NONE', #13258, .T. ) ;
#59437=CARTESIAN_POINT ( 'NONE',  ( -7.999999999999861444, -9.580972845112835701E-07, 13.01783880491507261 ) ) ;
#59438=CARTESIAN_POINT ( 'NONE',  ( -5.656854249492375253, 5.656854249492375253, 12.64280277982336287 ) ) ;
#59446=ORIENTED_EDGE ( 'NONE', *, *, #43886, .T. ) ;
#59451=CARTESIAN_POINT ( 'NONE',  ( 3.313708498984756279, 7.999999999999991118, 27.36155277982336642 ) ) ;
#59501=CARTESIAN_POINT ( 'NONE',  ( 5.082755093536318824, 5.082755093536319713, 2.424052781871750994 ) ) ;
#59524=CARTESIAN_POINT ( 'NONE',  ( -7.188101187499992051, 0.000000000000000000, 1.861552781871753881 ) ) ;
#59540=CARTESIAN_POINT ( 'NONE',  ( -3.313708498984757167, 7.999999999999991118, 24.73655278392014978 ) ) ;
#59541=DIRECTION ( 'NONE',  ( 0.000000000000000000, -0.000000000000000000, -1.000000000000000000 ) ) ;
#59560=CARTESIAN_POINT ( 'NONE',  ( -5.082755093536317936, -5.082755093536320601, 19.67405278187175455 ) ) ;
#59570=CARTESIAN_POINT ( 'NONE',  ( 5.656854249492374365, 5.656854249492375253, 12.45530278392014623 ) ) ;
#59582=CARTESIAN_POINT ( 'NONE',  ( -5.082755093536317936, -5.082755093536320601, 18.17405278187175455 ) ) ;
#59593=CARTESIAN_POINT ( 'NONE',  ( 1.320432766682872962E-15, -7.188101187499992051, 0.7365527818717527708 ) ) ;
#59594=DIRECTION ( 'NONE',  ( 1.000000000000000000, 0.000000000000000000, 0.000000000000000000 ) ) ;
#59598=CARTESIAN_POINT ( 'NONE',  ( -7.999999999999991118, 0.000000000000000000, 28.01780278392014978 ) ) ;
#59605=CARTESIAN_POINT ( 'NONE',  ( 7.188101187499993827, -2.977408999572645598, 20.51780278187175455 ) ) ;
#59622=CARTESIAN_POINT ( 'NONE',  ( 1.469576158976822172E-15, -7.999999999999991118, 17.70530277982336642 ) ) ;
#59636=CARTESIAN_POINT ( 'NONE',  ( -3.313708498984758943, -7.999999999999989342, 19.16780278432982954 ) ) ;
#59651=LINE ( 'NONE', #12872, #16718 ) ;
#59672=CARTESIAN_POINT ( 'NONE',  ( 7.188101187499991163, 2.977408999572648707, 9.830302781871752771 ) ) ;
#59696=CARTESIAN_POINT ( 'NONE',  ( -7.188101187499992051, 0.000000000000000000, 7.861552781871751883 ) ) ;
#59739=ORIENTED_EDGE ( 'NONE', *, *, #43713, .T. ) ;
#59740=CARTESIAN_POINT ( 'NONE',  ( 3.313708498984762496, -7.999999999999989342, 13.29905277982336465 ) ) ;
#59742=CARTESIAN_POINT ( 'NONE',  ( 8.008118988124993010, -3.317071493978877239, 9.169365283940628331 ) ) ;
#59747=CARTESIAN_POINT ( 'NONE',  ( 7.188101187499992051, 2.977408999572647819, 0.8303027818717529929 ) ) ;
#59763=CARTESIAN_POINT ( 'NONE',  ( -2.977408999572647819, 7.188101187499991163, 28.20530278187175455 ) ) ;
#59802=CARTESIAN_POINT ( 'NONE',  ( -7.999999999999989342, -3.313708498984762496, 14.42405277982336465 ) ) ;
#59830=LINE ( 'NONE', #7780, #22320 ) ;
#59831=CARTESIAN_POINT ( 'NONE',  ( -8.008118988124991233, 3.317071493978878127, 27.91936528394063544 ) ) ;
#59851=DIRECTION ( 'NONE',  ( 0.000000000000000000, 0.2588190451025143557, -0.9659258262890699775 ) ) ;
#59865=CARTESIAN_POINT ( 'NONE',  ( -7.188101187499990274, -2.977408999572651371, 27.45530278187175810 ) ) ;
#59880=EDGE_CURVE ( 'NONE', #12693, #54725, #42232, .T. ) ;
#59889=CARTESIAN_POINT ( 'NONE',  ( 2.977408999572646486, 7.188101187499991163, 5.892802781871754547 ) ) ;
#59905=CARTESIAN_POINT ( 'NONE',  ( 5.656854249492374365, 5.656854249492375253, 21.45530278392014623 ) ) ;
#59926=CARTESIAN_POINT ( 'NONE',  ( 2.977408999572646486, 7.188101187499992051, 20.51780278187175810 ) ) ;
#59934=CARTESIAN_POINT ( 'NONE',  ( 3.313708498984762496, -7.999999999999989342, 11.98655278392014445 ) ) ;
#59942=CARTESIAN_POINT ( 'NONE',  ( 7.188101187499993827, -2.977408999572645598, 18.64280278187175810 ) ) ;
#59945=VERTEX_POINT ( 'NONE', #60329 ) ;
#59956=CARTESIAN_POINT ( 'NONE',  ( 7.999999999999991118, 9.797174393178815797E-16, 15.08030277982336642 ) ) ;
#59960=CARTESIAN_POINT ( 'NONE',  ( 5.656854249492376141, -5.656854249492374365, 27.08030278392014978 ) ) ;
#59967=CARTESIAN_POINT ( 'NONE',  ( -5.082755093536317936, -5.082755093536320601, 20.04905278187175455 ) ) ;
#59974=EDGE_LOOP ( 'NONE', ( #50765, #37179, #54275, #20566 ) ) ;
#59985=CARTESIAN_POINT ( 'NONE',  ( 3.313708498984762496, -7.999999999999989342, 17.79905277982336642 ) ) ;
#60000=CARTESIAN_POINT ( 'NONE',  ( -3.313708498984757167, 7.999999999999991118, 17.10530278432982598 ) ) ;
#60028=CARTESIAN_POINT ( 'NONE',  ( 5.082755093536318824, 5.082755093536319713, 9.924052781871754547 ) ) ;
#60050=CARTESIAN_POINT ( 'NONE',  ( -2.977408999572647819, -7.188101187499990274, 6.642802781871754547 ) ) ;
#60076=CARTESIAN_POINT ( 'NONE',  ( 3.313708498984762496, -7.999999999999989342, 1.299052779823363979 ) ) ;
#60082=CARTESIAN_POINT ( 'NONE',  ( -3.313708498984757167, 7.999999999999991118, 6.736552783920144449 ) ) ;
#60098=VERTEX_POINT ( 'NONE', #7912 ) ;
#60101=CARTESIAN_POINT ( 'NONE',  ( -8.008118988124991233, 3.317071493978878127, 8.419365283940628331 ) ) ;
#60107=CARTESIAN_POINT ( 'NONE',  ( 7.188101187499992051, 2.977408999572647819, 5.330302781871753659 ) ) ;
#60112=ORIENTED_EDGE ( 'NONE', *, *, #48728, .T. ) ;
#60119=CARTESIAN_POINT ( 'NONE',  ( -5.082755093536319713, 5.082755093536319713, 22.29905278187175455 ) ) ;
#60142=CARTESIAN_POINT ( 'NONE',  ( 7.188101187499992051, 8.802885111219154394E-16, 25.11155278187175810 ) ) ;
#60162=CARTESIAN_POINT ( 'NONE',  ( 7.999999999999992895, -3.313708498984756279, 7.486552779823366421 ) ) ;
#60179=CARTESIAN_POINT ( 'NONE',  ( -5.656854249492375253, 5.656854249492375253, 6.830302783920143561 ) ) ;
#60192=CARTESIAN_POINT ( 'NONE',  ( -8.008118988124991233, 3.317071493978878127, 26.41936528394063188 ) ) ;
#60224=CARTESIAN_POINT ( 'NONE',  ( 7.188101187499993827, -2.977408999572645598, 28.01780278187175455 ) ) ;
#60226=CARTESIAN_POINT ( 'NONE',  ( -7.999999999999991118, 3.313708498984757167, 15.92405278392014445 ) ) ;
#60237=CYLINDRICAL_SURFACE ( 'NONE', #66340, 7.999999999999991118 ) ;
#60238=ORIENTED_EDGE ( 'NONE', *, *, #48601, .T. ) ;
#60249=CARTESIAN_POINT ( 'NONE',  ( -7.188101187499992051, 0.000000000000000000, 6.361552781871754547 ) ) ;
#60265=CARTESIAN_POINT ( 'NONE',  ( 7.999999999999991118, 3.313708498984757611, 21.36155278392014978 ) ) ;
#60288=CARTESIAN_POINT ( 'NONE',  ( -5.082755093536317936, -5.082755093536320601, 22.67405278187175455 ) ) ;
#60289=CARTESIAN_POINT ( 'NONE',  ( 7.999999999999992895, 8.617919685066743914E-06, 16.76780302773458686 ) ) ;
#60297=CARTESIAN_POINT ( 'NONE',  ( 3.313708498984756279, 7.999999999999991118, 15.54905278392014623 ) ) ;
#60307=VERTEX_POINT ( 'NONE', #40684 ) ;
#60309=CARTESIAN_POINT ( 'NONE',  ( -7.188101187499991163, 2.977408999572646930, 20.89280278187176521 ) ) ;
#60328=CARTESIAN_POINT ( 'NONE',  ( -7.999999999999991118, 3.313708498984756723, 24.92405278392015333 ) ) ;
#60329=CARTESIAN_POINT ( 'NONE',  ( -7.999999999999991118, 0.000000000000000000, 23.33030277982336642 ) ) ;
#60335=CARTESIAN_POINT ( 'NONE',  ( -5.082755093536317936, -5.082755093536320601, 24.54905278187175810 ) ) ;
#60351=CARTESIAN_POINT ( 'NONE',  ( 5.656854249492376141, -5.656854249492374365, 10.39280277982336465 ) ) ;
#60369=CARTESIAN_POINT ( 'NONE',  ( 1.469576158976822172E-15, -7.999999999999991118, 11.76155278432982243 ) ) ;
#60401=CARTESIAN_POINT ( 'NONE',  ( 1.320432766682872962E-15, -7.188101187499992051, 9.361552781871752771 ) ) ;
#60416=CARTESIAN_POINT ( 'NONE',  ( 2.977408999572646486, 7.188101187499991163, 11.89280278187175810 ) ) ;
#60422=LINE ( 'NONE', #3843, #63653 ) ;
#60427=CARTESIAN_POINT ( 'NONE',  ( -2.977408999572647819, -7.188101187499990274, 5.142802781871753659 ) ) ;
#60429=CARTESIAN_POINT ( 'NONE',  ( 0.000000000000000000, 0.000000000000000000, 30.00000000000000000 ) ) ;
#60441=CARTESIAN_POINT ( 'NONE',  ( -5.656854249492373476, -5.656854249492376141, 28.01780277982336642 ) ) ;
#60446=CARTESIAN_POINT ( 'NONE',  ( 7.999999999999991118, 1.469576158976822369E-15, 25.76780278392172008 ) ) ;
#60453=CARTESIAN_POINT ( 'NONE',  ( -3.313708498984757167, 7.999999999999991118, 9.736552783920146226 ) ) ;
#60455=DIRECTION ( 'NONE',  ( 0.000000000000000000, -0.2588190451025146332, 0.9659258262890699775 ) ) ;
#60471=CARTESIAN_POINT ( 'NONE',  ( -3.317071493978880348, -8.008118988124989457, 8.794365283940628331 ) ) ;
#60478=CARTESIAN_POINT ( 'NONE',  ( -4.401442555609577197E-16, 7.188101187499992051, 4.111552781871752771 ) ) ;
#60493=CARTESIAN_POINT ( 'NONE',  ( 7.188101187499993827, -2.977408999572645598, 24.64280278187176165 ) ) ;
#60513=CARTESIAN_POINT ( 'NONE',  ( -5.656854249492373476, -5.656854249492376141, 22.01780277982336997 ) ) ;
#60518=CARTESIAN_POINT ( 'NONE',  ( 2.977408999572646486, 7.188101187499992051, 20.89280278187176521 ) ) ;
#60537=CARTESIAN_POINT ( 'NONE',  ( -7.999999999999989342, -3.313708498984762496, 11.42405277982336465 ) ) ;
#60547=CARTESIAN_POINT ( 'NONE',  ( 3.313708498984756279, 7.999999999999991118, 5.049052783920146226 ) ) ;
#60551=CARTESIAN_POINT ( 'NONE',  ( 8.000000000000017764, 3.313708498984730522, 27.17405277982336642 ) ) ;
#60564=VERTEX_POINT ( 'NONE', #14865 ) ;
#60601=CARTESIAN_POINT ( 'NONE',  ( -7.188101187499991163, 2.977408999572646930, 28.76780278187175455 ) ) ;
#60628=CARTESIAN_POINT ( 'NONE',  ( -5.656854249492375253, 5.656854249492375253, 29.14280277982336642 ) ) ;
#60631=VERTEX_POINT ( 'NONE', #9974 ) ;
#60636=CARTESIAN_POINT ( 'NONE',  ( 7.999999999999992895, -3.313708498984756279, 14.98655277982336642 ) ) ;
#60647=CARTESIAN_POINT ( 'NONE',  ( -5.656854249492375253, 5.656854249492375253, 18.83030278392014623 ) ) ;
#60657=CARTESIAN_POINT ( 'NONE',  ( -7.999999999999989342, -3.313708498984762496, 26.61155278392014978 ) ) ;
#60659=CARTESIAN_POINT ( 'NONE',  ( -5.447321192899549303, -4.689935021205116961, 0.1569292013794422458 ) ) ;
#60669=CARTESIAN_POINT ( 'NONE',  ( 7.188101187499992051, 2.977408999572647819, 18.83030278187175455 ) ) ;
#60681=CARTESIAN_POINT ( 'NONE',  ( -7.999999999999991118, 3.313708498984756723, 11.42405278392014623 ) ) ;
#60682=LINE ( 'NONE', #38053, #33063 ) ;
#60692=CARTESIAN_POINT ( 'NONE',  ( -4.401442555609577197E-16, 7.188101187499992051, 19.11155278187175455 ) ) ;
#60697=CARTESIAN_POINT ( 'NONE',  ( 5.656854249492376141, -5.656854249492374365, 6.080302783920147114 ) ) ;
#60710=CARTESIAN_POINT ( 'NONE',  ( -5.662595241051933570, -5.662595241051936235, -0.2993847160593715029 ) ) ;
#60716=CARTESIAN_POINT ( 'NONE',  ( -7.188101187499990274, -2.977408999572651371, 16.95530278187175455 ) ) ;
#60731=CARTESIAN_POINT ( 'NONE',  ( 5.656854249492374365, 5.656854249492375253, 10.76780277982336642 ) ) ;
#60742=ORIENTED_EDGE ( 'NONE', *, *, #73691, .F. ) ;
#60748=DIRECTION ( 'NONE',  ( -0.000000000000000000, -0.000000000000000000, 1.000000000000000000 ) ) ;
#60749=CARTESIAN_POINT ( 'NONE',  ( -4.898587196589407898E-16, 7.999999999999991118, 11.01155278432982598 ) ) ;
#60750=CARTESIAN_POINT ( 'NONE',  ( -7.999999999999991118, 0.000000000000000000, 15.83030277982336642 ) ) ;
#60778=CARTESIAN_POINT ( 'NONE',  ( 2.977408999572646486, 7.188101187499991163, 7.017802781871751883 ) ) ;
#60780=VERTEX_POINT ( 'NONE', #47543 ) ;
#60790=CARTESIAN_POINT ( 'NONE',  ( 7.188101187499991163, 2.977408999572648707, 13.20530278187175277 ) ) ;
#60801=CARTESIAN_POINT ( 'NONE',  ( -5.082755093536317936, -5.082755093536320601, 5.049052781871752771 ) ) ;
#60818=CARTESIAN_POINT ( 'NONE',  ( -7.999999999999989342, -3.313708498984762496, 27.92405277982336642 ) ) ;
#60827=ORIENTED_EDGE ( 'NONE', *, *, #16261, .T. ) ;
#60831=CARTESIAN_POINT ( 'NONE',  ( 3.313708498984762496, -7.999999999999989342, 1.486552783920146448 ) ) ;
#60856=CARTESIAN_POINT ( 'NONE',  ( -2.977408999572647819, 7.188101187499992051, 2.705302781871750994 ) ) ;
#60866=CARTESIAN_POINT ( 'NONE',  ( 7.188101187499991163, 2.977408999572648707, 27.83030278187176165 ) ) ;
#60892=CARTESIAN_POINT ( 'NONE',  ( 2.977408999572646486, 7.188101187499992051, 25.39280278187176165 ) ) ;
#60903=CARTESIAN_POINT ( 'NONE',  ( 1.469576158976822172E-15, -7.999999999999991118, -0.1071972160798552454 ) ) ;
#60910=CARTESIAN_POINT ( 'NONE',  ( 1.469576158976822172E-15, -7.999999999999991118, 7.205302779823365533 ) ) ;
#60916=CARTESIAN_POINT ( 'NONE',  ( -4.898587196589407898E-16, 7.999999999999991118, 14.14280278392014623 ) ) ;
#60941=CARTESIAN_POINT ( 'NONE',  ( -8.008118988124991233, 0.000000000000000000, 23.51311528394063188 ) ) ;
#60942=CARTESIAN_POINT ( 'NONE',  ( 7.999979185126659509, 3.313729313858088776, 22.86155361672978970 ) ) ;
#60976=CARTESIAN_POINT ( 'NONE',  ( 5.082755093536320601, -5.082755093536318824, 26.42405278187175810 ) ) ;
#60978=CARTESIAN_POINT ( 'NONE',  ( 0.000000000000000000, 0.000000000000000000, 30.00000000000000000 ) ) ;
#61000=CARTESIAN_POINT ( 'NONE',  ( 7.999999999999991118, 3.313708498984757611, 28.67405277982336642 ) ) ;
#61015=CARTESIAN_POINT ( 'NONE',  ( 7.999999999999992895, -3.313708498984756279, 11.98655277982336820 ) ) ;
#61018=CARTESIAN_POINT ( 'NONE',  ( 3.313708498984762496, -7.999999999999989342, 17.98655278392014978 ) ) ;
#61040=CARTESIAN_POINT ( 'NONE',  ( -2.977408999572647819, -7.188101187499990274, 12.26780278187175455 ) ) ;
#61041=CARTESIAN_POINT ( 'NONE',  ( 7.999999999999992895, -3.313708498984756279, 16.67405278392014623 ) ) ;
#61052=CARTESIAN_POINT ( 'NONE',  ( -3.313708498984757167, 7.999999999999991118, 9.736552783920146226 ) ) ;
#61061=EDGE_LOOP ( 'NONE', ( #65333, #29142, #14085, #74586 ) ) ;
#61064=CARTESIAN_POINT ( 'NONE',  ( -7.188101187499991163, 2.977408999572646930, 16.39280278187175455 ) ) ;
#61066=( BOUNDED_CURVE ( )  B_SPLINE_CURVE ( 2, ( #8027, #31035, #13301, #18978, #41982, #2369, #36339, #53691, #71384 ),
 .UNSPECIFIED., .F., .F. ) 
 B_SPLINE_CURVE_WITH_KNOTS ( ( 3, 2, 2, 2, 3 ),
 ( 0.1842105263157894912, 0.1907894736842105643, 0.1973684210526316374, 0.2039473684210527105, 0.2105263157894737558 ),
 .UNSPECIFIED. ) 
 CURVE ( )  GEOMETRIC_REPRESENTATION_ITEM ( )  RATIONAL_B_SPLINE_CURVE ( ( 0.9999999999999996669, 0.9238795325112870716, 1.000000000000000000, 0.9238795325112867385, 1.000000000000000000, 0.9238795325112867385, 1.000000000000000000, 0.9238795325112857393, 1.000000000000000888 ) ) 
 REPRESENTATION_ITEM ( '' )  );
#61080=CARTESIAN_POINT ( 'NONE',  ( -7.999999999999991118, 3.313708498984756723, 26.42405278392015333 ) ) ;
#61086=CARTESIAN_POINT ( 'NONE',  ( -7.188101187499991163, 2.977408999572646930, 13.76780278187175455 ) ) ;
#61103=CARTESIAN_POINT ( 'NONE',  ( 5.656854249492374365, 5.656854249492375253, 9.267802779823364645 ) ) ;
#61104=CARTESIAN_POINT ( 'NONE',  ( -7.999999999929542582, -2.214810345207895024E-05, 22.01864141485938831 ) ) ;
#61120=CARTESIAN_POINT ( 'NONE',  ( -5.656854249492375253, 5.656854249492375253, 14.19905278432982598 ) ) ;
#61132=ORIENTED_EDGE ( 'NONE', *, *, #74420, .F. ) ;
#61139=CARTESIAN_POINT ( 'NONE',  ( 5.656854249492376141, -5.656854249492374365, 19.39280277982336642 ) ) ;
#61153=CARTESIAN_POINT ( 'NONE',  ( -2.977408999572647819, 7.188101187499991163, 4.205302781871751883 ) ) ;
#61166=CARTESIAN_POINT ( 'NONE',  ( 7.188101187499991163, 2.977408999572648707, 10.20530278187175455 ) ) ;
#61182=CARTESIAN_POINT ( 'NONE',  ( 2.977408999572646486, 7.188101187499992051, 4.392802781871752771 ) ) ;
#61198=CARTESIAN_POINT ( 'NONE',  ( -7.999999999999991118, -9.344071862984236532, 29.59466119801952644 ) ) ;
#61211=CARTESIAN_POINT ( 'NONE',  ( 3.313708498984756279, 7.999999999999991118, 27.41780278432982954 ) ) ;
#61213=DIRECTION ( 'NONE',  ( 1.000000000000000000, 0.000000000000000000, 0.000000000000000000 ) ) ;
#61234=CARTESIAN_POINT ( 'NONE',  ( -2.977408999572647819, -7.188101187499990274, 4.767802781871752771 ) ) ;
#61243=CARTESIAN_POINT ( 'NONE',  ( 7.999999999999992895, -3.313708498984756279, 10.48655277982336642 ) ) ;
#61244=CARTESIAN_POINT ( 'NONE',  ( -7.188101187499992051, 0.000000000000000000, 26.98655278187175455 ) ) ;
#61269=CARTESIAN_POINT ( 'NONE',  ( 5.082755093536318824, 5.082755093536319713, 25.29905278187175810 ) ) ;
#61289=CARTESIAN_POINT ( 'NONE',  ( -5.656854249492375253, 5.656854249492375253, 9.642802779823364645 ) ) ;
#61320=CARTESIAN_POINT ( 'NONE',  ( -4.903558642999205574E-16, 8.008118988124991233, 23.13811528394063188 ) ) ;
#61338=EDGE_CURVE ( 'NONE', #14923, #71023, #58074, .T. ) ;
#61353=CARTESIAN_POINT ( 'NONE',  ( -4.401442555609577197E-16, 7.188101187499992051, 22.48655278187175455 ) ) ;
#61355=DIRECTION ( 'NONE',  ( -0.000000000000000000, -0.000000000000000000, 1.000000000000000000 ) ) ;
#61377=CARTESIAN_POINT ( 'NONE',  ( -7.999999999999991118, 0.000000000000000000, 24.83030277982336642 ) ) ;
#61379=CARTESIAN_POINT ( 'NONE',  ( -7.999999999999991118, 9.797174393178815797E-16, 30.00000000000000000 ) ) ;
#61395=CARTESIAN_POINT ( 'NONE',  ( -7.999999999999991118, 0.000000000000000000, 16.01780278392014978 ) ) ;
#61416=CARTESIAN_POINT ( 'NONE',  ( 2.977408999572646486, 7.188101187499992051, 13.01780278187175277 ) ) ;
#61417=CARTESIAN_POINT ( 'NONE',  ( 3.313708498984762496, -7.999999999999989342, 16.48655278392014623 ) ) ;
#61429=CARTESIAN_POINT ( 'NONE',  ( 1.469576158976822172E-15, -7.999999999999991118, 7.392802783920144449 ) ) ;
#61434=CARTESIAN_POINT ( 'NONE',  ( -4.898587196589407898E-16, 7.999999999999991118, 12.45530277982336642 ) ) ;
#61441=CARTESIAN_POINT ( 'NONE',  ( 7.188101187499991163, 2.977408999572648707, 12.83030278187175277 ) ) ;
#61446=CARTESIAN_POINT ( 'NONE',  ( -5.656854249492373476, -5.656854249492376141, 17.51780277982336287 ) ) ;
#61452=LINE ( 'NONE', #10517, #32378 ) ;
#61453=ADVANCED_FACE ( 'NONE', ( #20261 ), #24813, .F. ) ;
#61465=CARTESIAN_POINT ( 'NONE',  ( 1.320432766682872962E-15, -7.188101187499992051, 17.23655278187175810 ) ) ;
#61481=CARTESIAN_POINT ( 'NONE',  ( -7.999999999999991118, 0.000000000000000000, 8.330302779823362869 ) ) ;
#61482=CARTESIAN_POINT ( 'NONE',  ( -7.999999999999991118, -2.368985594519444545E-05, 22.01780345414325524 ) ) ;
#61497=CARTESIAN_POINT ( 'NONE',  ( 1.469576158976822172E-15, -7.999999999999991118, 14.76155278432982421 ) ) ;
#61498=CARTESIAN_POINT ( 'NONE',  ( 7.999999999999991118, 9.797174393178815797E-16, 16.58030277982336287 ) ) ;
#61506=( BOUNDED_CURVE ( )  B_SPLINE_CURVE ( 2, ( #60446, #49505, #3119, #38943, #20832, #4246, #73272, #38200, #43089, #43466, #72136 ),
 .UNSPECIFIED., .F., .F. ) 
 B_SPLINE_CURVE_WITH_KNOTS ( ( 3, 2, 2, 2, 2, 3 ),
 ( 0.07941930701348173804, 0.08603758259794166974, 0.09265585818240160143, 0.09927413376686153312, 0.1058924093513214509, 0.1058924239672156403 ),
 .UNSPECIFIED. ) 
 CURVE ( )  GEOMETRIC_REPRESENTATION_ITEM ( )  RATIONAL_B_SPLINE_CURVE ( ( 1.000000000000000000, 0.9238795325112867385, 1.000000000000000000, 0.9238795325112867385, 1.000000000000000000, 0.9238795325112867385, 1.000000000000000000, 0.9238795325112867385, 1.000000000000000000, 0.9999998318944740561, 0.9999996637896906293 ) ) 
 REPRESENTATION_ITEM ( '' )  );
#61532=ORIENTED_EDGE ( 'NONE', *, *, #45453, .F. ) ;
#61534=CARTESIAN_POINT ( 'NONE',  ( -7.999999999999991118, 0.000000000000000000, 20.33030277982336642 ) ) ;
#61543=CARTESIAN_POINT ( 'NONE',  ( -2.977408999572647819, 7.188101187499991163, 13.58030278187175277 ) ) ;
#61558=CARTESIAN_POINT ( 'NONE',  ( -4.401442555609577197E-16, 7.188101187499992051, 7.486552781871751883 ) ) ;
#61560=DIRECTION ( 'NONE',  ( -1.000000000000000000, 0.000000000000000000, 0.000000000000000000 ) ) ;
#61574=CARTESIAN_POINT ( 'NONE',  ( -5.656854249492375253, 5.656854249492375253, 27.64280277982336642 ) ) ;
#61577=EDGE_CURVE ( 'NONE', #26953, #31087, #18858, .T. ) ;
#61585=CARTESIAN_POINT ( 'NONE',  ( 5.656854249492374365, 5.656854249492375253, 3.455302783920144449 ) ) ;
#61620=EDGE_CURVE ( 'NONE', #11426, #39299, #38388, .T. ) ;
#61623=CARTESIAN_POINT ( 'NONE',  ( -7.188101187499990274, -2.977408999572651371, 25.58030278187175810 ) ) ;
#61646=CARTESIAN_POINT ( 'NONE',  ( -2.977408999572647819, -7.188101187499990274, 24.64280278187176165 ) ) ;
#61665=CARTESIAN_POINT ( 'NONE',  ( 3.313708498984762496, -7.999999999999989342, 11.79905277982336465 ) ) ;
#61675=CARTESIAN_POINT ( 'NONE',  ( -7.999999999953861796, 1.809871347124574913E-05, 10.01712378708029938 ) ) ;
#61693=CARTESIAN_POINT ( 'NONE',  ( 5.662595241051934458, 5.662595241051935346, 22.95061528394063188 ) ) ;
#61701=ORIENTED_EDGE ( 'NONE', *, *, #31346, .F. ) ;
#61726=CARTESIAN_POINT ( 'NONE',  ( 5.082755093536320601, -5.082755093536318824, 21.92405278187175455 ) ) ;
#61727=CYLINDRICAL_SURFACE ( 'NONE', #52652, 7.999999999999991118 ) ;
#61731=( BOUNDED_CURVE ( )  B_SPLINE_CURVE ( 2, ( #46350, #22210, #29385, #52393, #69740, #18055, #41070, #6742, #29745, #45237, #51265 ),
 .UNSPECIFIED., .F., .F. ) 
 B_SPLINE_CURVE_WITH_KNOTS ( ( 3, 2, 2, 2, 2, 3 ),
 ( 0.7147737642690134008, 0.7213920387057923822, 0.7280103142902493163, 0.7346285898747061394, 0.7412468654591628514, 0.7412468980011663877 ),
 .UNSPECIFIED. ) 
 CURVE ( )  GEOMETRIC_REPRESENTATION_ITEM ( )  RATIONAL_B_SPLINE_CURVE ( ( 1.000000000000000000, 0.9238795325112867385, 1.000000000000000000, 0.9238795325112867385, 1.000000000000000000, 0.9238795325112867385, 1.000000000000000000, 0.9238795325112867385, 1.000000000000000000, 0.9999996257163232816, 0.9999992514363272855 ) ) 
 REPRESENTATION_ITEM ( '' )  );
#61735=( BOUNDED_CURVE ( )  B_SPLINE_CURVE ( 2, ( #31617, #42556, #3697, #65567, #37659, #54638, #9354, #60657, #42919 ),
 .UNSPECIFIED., .F., .T. ) 
 B_SPLINE_CURVE_WITH_KNOTS ( ( 3, 2, 2, 2, 3 ),
 ( 0.02647310233782740330, 0.03309137792228417779, 0.03970965350674094535, 0.04632792909119771985, 0.05294620388485415940 ),
 .UNSPECIFIED. ) 
 CURVE ( )  GEOMETRIC_REPRESENTATION_ITEM ( )  RATIONAL_B_SPLINE_CURVE ( ( 0.9999999999999981126, 0.9238795325112885148, 1.000000000000000000, 0.9238795325112867385, 1.000000000000000000, 0.9238795325112867385, 1.000000000000000000, 0.9238795325112867385, 1.000000000000000000 ) ) 
 REPRESENTATION_ITEM ( '' )  );
#61753=CARTESIAN_POINT ( 'NONE',  ( -7.999999999999991118, 3.313708498984756723, 24.73655277982336997 ) ) ;
#61771=CARTESIAN_POINT ( 'NONE',  ( 3.313708498984756279, 7.999999999999991118, 12.54905278392014800 ) ) ;
#61792=CARTESIAN_POINT ( 'NONE',  ( -7.188101187499990274, -2.977408999572651815, 13.58030278187175455 ) ) ;
#61813=CARTESIAN_POINT ( 'NONE',  ( -5.082755093536317936, -5.082755093536320601, 12.17405278187175277 ) ) ;
#61818=CARTESIAN_POINT ( 'NONE',  ( -3.313708498984759387, -7.999999999999989342, 23.79905278392014978 ) ) ;
#61838=CARTESIAN_POINT ( 'NONE',  ( -7.188101187499990274, -2.977408999572651371, 15.45530278187175455 ) ) ;
#61854=CARTESIAN_POINT ( 'NONE',  ( -4.898587196589407898E-16, 7.999999999999991118, 9.455302779823364645 ) ) ;
#61855=CARTESIAN_POINT ( 'NONE',  ( -7.999999999961189268, -1.665725685002260109E-05, 4.018425631117963803 ) ) ;
#61869=CARTESIAN_POINT ( 'NONE',  ( -7.999999999999991118, 3.313708498984756723, 12.79280278432982421 ) ) ;
#61910=CARTESIAN_POINT ( 'NONE',  ( 2.977408999572646486, 7.188101187499991163, 7.392802781871750994 ) ) ;
#61950=CARTESIAN_POINT ( 'NONE',  ( 5.656854249492376141, -5.656854249492374365, 26.94905278432982598 ) ) ;
#61961=CARTESIAN_POINT ( 'NONE',  ( -7.999999999999991118, 0.000000000000000000, 1.017802783920145782 ) ) ;
#61989=CARTESIAN_POINT ( 'NONE',  ( 2.977408999572650927, -7.188101187499990274, 21.45530278187175810 ) ) ;
#62011=CARTESIAN_POINT ( 'NONE',  ( -2.977408999572647819, -7.188101187499990274, 15.64280278187175632 ) ) ;
#62027=( GEOMETRIC_REPRESENTATION_CONTEXT ( 3 ) GLOBAL_UNCERTAINTY_ASSIGNED_CONTEXT ( ( #25388 ) ) GLOBAL_UNIT_ASSIGNED_CONTEXT ( ( #34272, #40656, #34646 ) ) REPRESENTATION_CONTEXT ( 'NONE', 'WORKASPACE' ) );
#62031=CARTESIAN_POINT ( 'NONE',  ( 5.656854249492374365, 5.656854249492375253, 4.767802779823363757 ) ) ;
#62036=CARTESIAN_POINT ( 'NONE',  ( -7.999999999999991118, 0.000000000000000000, 14.51780278392014800 ) ) ;
#62058=CARTESIAN_POINT ( 'NONE',  ( -3.317071493978878571, 8.008118988124991233, 21.73186528394063544 ) ) ;
#62093=CARTESIAN_POINT ( 'NONE',  ( -5.082755093536319713, 5.082755093536319713, 22.67405278187175455 ) ) ;
#62110=EDGE_CURVE ( 'NONE', #26401, #6157, #53029, .T. ) ;
#62117=CARTESIAN_POINT ( 'NONE',  ( -5.656854249492373476, -5.656854249492376141, 28.01780277982336642 ) ) ;
#62120=EDGE_LOOP ( 'NONE', ( #18264, #9753, #36571, #44693, #21317, #47535, #1740 ) ) ;
#62136=CARTESIAN_POINT ( 'NONE',  ( 7.999999999999992895, -3.313708498984756279, 15.17405278392014623 ) ) ;
#62156=CARTESIAN_POINT ( 'NONE',  ( -4.401442555609577197E-16, 7.188101187499992051, 16.11155278187175455 ) ) ;
#62179=CARTESIAN_POINT ( 'NONE',  ( -2.977408999572648707, -7.188101187499990274, 10.76780278187175632 ) ) ;
#62189=FACE_OUTER_BOUND ( 'NONE', #55401, .T. ) ;
#62204=CARTESIAN_POINT ( 'NONE',  ( 7.188101187499992051, 8.802885111219154394E-16, 14.61155278187175455 ) ) ;
#62219=CARTESIAN_POINT ( 'NONE',  ( -3.313708498984758943, -7.999999999999989342, 5.611552779823364645 ) ) ;
#62235=CARTESIAN_POINT ( 'NONE',  ( 5.656854249492376141, -5.656854249492374365, 5.949052784329825094 ) ) ;
#62257=EDGE_LOOP ( 'NONE', ( #48886, #8248, #20886, #2980 ) ) ;
#62265=CARTESIAN_POINT ( 'NONE',  ( 7.188101187499993827, -2.977408999572645598, 3.642802781871751883 ) ) ;
#62280=CARTESIAN_POINT ( 'NONE',  ( 1.320432766682872962E-15, -7.188101187499992051, 6.736552781871754547 ) ) ;
#62289=FACE_OUTER_BOUND ( 'NONE', #74622, .T. ) ;
#62293=CARTESIAN_POINT ( 'NONE',  ( -2.977408999572647819, -7.188101187499990274, 0.6428027818717527708 ) ) ;
#62309=CARTESIAN_POINT ( 'NONE',  ( -3.313708498984758943, -7.999999999999989342, 23.61155277982336997 ) ) ;
#62321=CARTESIAN_POINT ( 'NONE',  ( -3.313708498984758943, -7.999999999999989342, 2.799052783920144005 ) ) ;
#62333=ORIENTED_EDGE ( 'NONE', *, *, #8908, .T. ) ;
#62349=CARTESIAN_POINT ( 'NONE',  ( -7.188101187499990274, -2.977408999572651371, 19.58030278187175455 ) ) ;
#62374=CARTESIAN_POINT ( 'NONE',  ( -2.977408999572647819, 7.188101187499992051, 16.58030278187175455 ) ) ;
#62386=CARTESIAN_POINT ( 'NONE',  ( -3.313708498984757611, 7.999999999999991118, 17.23655278392014623 ) ) ;
#62394=CARTESIAN_POINT ( 'NONE',  ( -3.313708498984758943, -7.999999999999989342, 1.111552779823363757 ) ) ;
#62425=CARTESIAN_POINT ( 'NONE',  ( 8.008118988124991233, 3.317071493978879015, 22.85686528394062833 ) ) ;
#62450=CARTESIAN_POINT ( 'NONE',  ( -7.999999999999991118, 0.000000000000000000, 2.330302779823365089 ) ) ;
#62452=CARTESIAN_POINT ( 'NONE',  ( -7.417212451314158628, -3.006759011572777140, -0.000000000000000000 ) ) ;
#62456=CARTESIAN_POINT ( 'NONE',  ( -7.188101187499992051, 0.000000000000000000, 21.36155278187175455 ) ) ;
#62481=CARTESIAN_POINT ( 'NONE',  ( 7.999999999999991118, 3.313708498984757611, 22.67405277982336287 ) ) ;
#62498=CARTESIAN_POINT ( 'NONE',  ( 7.999999999999991118, 9.797174393178815797E-16, 22.58030277982336997 ) ) ;
#62500=CARTESIAN_POINT ( 'NONE',  ( -3.313708498984757167, 7.999999999999991118, 15.73655278392014267 ) ) ;
#62523=VERTEX_POINT ( 'NONE', #23442 ) ;
#62530=CARTESIAN_POINT ( 'NONE',  ( -7.999999999999991118, 0.000000000000000000, 18.83030277982336642 ) ) ;
#62548=CARTESIAN_POINT ( 'NONE',  ( -7.188101187499990274, -2.977408999572651371, 13.58030278187175277 ) ) ;
#62572=CARTESIAN_POINT ( 'NONE',  ( 5.082755093536320601, -5.082755093536318824, 8.424052781871752771 ) ) ;
#62586=CARTESIAN_POINT ( 'NONE',  ( -7.999999999999991118, 3.313708498984756723, 5.236552779823363757 ) ) ;
#62604=CARTESIAN_POINT ( 'NONE',  ( 7.999999999999992895, -3.313708498984756279, 6.042802784329825094 ) ) ;
#62634=CARTESIAN_POINT ( 'NONE',  ( 7.188101187499991163, 2.977408999572648707, 2.330302781871750550 ) ) ;
#62647=CARTESIAN_POINT ( 'NONE',  ( -5.082755093536319713, 5.082755093536319713, 3.174052781871751439 ) ) ;
#62675=CARTESIAN_POINT ( 'NONE',  ( 7.999999999999991118, 9.797174393178815797E-16, 21.08030277982336642 ) ) ;
#62686=CARTESIAN_POINT ( 'NONE',  ( 7.999999999999992895, -3.313708498984756279, 25.54280278432982598 ) ) ;
#62695=CARTESIAN_POINT ( 'NONE',  ( 3.313708498984756279, 7.999999999999991118, 24.36155277982336997 ) ) ;
#62714=AXIS2_PLACEMENT_3D ( 'NONE', #11587, #57628, #52701 ) ;
#62718=( BOUNDED_CURVE ( )  B_SPLINE_CURVE ( 2, ( #39786, #67073, #16761, #39425, #28839, #74122, #62789, #11498, #28472 ),
 .UNSPECIFIED., .F., .F. ) 
 B_SPLINE_CURVE_WITH_KNOTS ( ( 3, 2, 2, 2, 3 ),
 ( 0.6883006607833690449, 0.6949189363678606179, 0.7015372119523523020, 0.7081554875368439861, 0.7147737642690134008 ),
 .UNSPECIFIED. ) 
 CURVE ( )  GEOMETRIC_REPRESENTATION_ITEM ( )  RATIONAL_B_SPLINE_CURVE ( ( 1.000000000001603162, 0.9238795325096835764, 1.000000000000000000, 0.9238795325112867385, 1.000000000000000000, 0.9238795325112867385, 1.000000000000000000, 0.9238795325112867385, 1.000000000000000000 ) ) 
 REPRESENTATION_ITEM ( '' )  );
#62721=CARTESIAN_POINT ( 'NONE',  ( 5.082755093536320601, -5.082755093536318824, 20.04905278187175455 ) ) ;
#62741=CARTESIAN_POINT ( 'NONE',  ( 2.977408999572650927, -7.188101187499990274, 18.83030278187175455 ) ) ;
#62761=CARTESIAN_POINT ( 'NONE',  ( -7.999999999999991118, 3.313708498984756723, 3.736552779823362869 ) ) ;
#62789=CARTESIAN_POINT ( 'NONE',  ( 5.656854249492374365, 5.656854249492375253, 7.955302783920145338 ) ) ;
#62790=CARTESIAN_POINT ( 'NONE',  ( -8.008118988124991233, 0.000000000000000000, 19.01311528394063188 ) ) ;
#62813=CARTESIAN_POINT ( 'NONE',  ( -3.313708498984757167, 7.999999999999991118, 5.236552783920145338 ) ) ;
#62827=CARTESIAN_POINT ( 'NONE',  ( 2.977408999572650927, -7.188101187499990274, 18.83030278187175099 ) ) ;
#62852=CARTESIAN_POINT ( 'NONE',  ( 3.313708498984756279, 7.999999999999991118, 21.36155277982336997 ) ) ;
#62870=CARTESIAN_POINT ( 'NONE',  ( -7.999999999999991118, 0.000000000000000000, 23.33030277982336642 ) ) ;
#62872=CARTESIAN_POINT ( 'NONE',  ( -5.656854249492373476, -5.656854249492376141, 13.20530278392014623 ) ) ;
#62923=PRODUCT_CONTEXT ( 'NONE', #54403, 'mechanical' ) ;
#62928=CARTESIAN_POINT ( 'NONE',  ( -4.401442555609577197E-16, 7.188101187499992051, 13.11155278187175277 ) ) ;
#62951=CARTESIAN_POINT ( 'NONE',  ( -7.188101187499991163, 2.977408999572646930, 9.267802781871756324 ) ) ;
#62955=CARTESIAN_POINT ( 'NONE',  ( -3.313708498984757167, 7.999999999999991118, 0.6053027843298234290 ) ) ;
#62966=CARTESIAN_POINT ( 'NONE',  ( 5.656854249492376141, -5.656854249492374365, 4.392802779823363757 ) ) ;
#62978=ORIENTED_EDGE ( 'NONE', *, *, #2836, .T. ) ;
#62985=CARTESIAN_POINT ( 'NONE',  ( -3.313708498984758943, -7.999999999999989342, 7.167802784329822430 ) ) ;
#63006=CARTESIAN_POINT ( 'NONE',  ( -7.999999999953861796, 1.809871347124574913E-05, 10.01712378708029938 ) ) ;
#63011=CARTESIAN_POINT ( 'NONE',  ( -5.082755093536319713, 5.082755093536319713, 1.299052781871753215 ) ) ;
#63012=VERTEX_POINT ( 'NONE', #68271 ) ;
#63025=CARTESIAN_POINT ( 'NONE',  ( 5.082755093536320601, -5.082755093536318824, 6.924052781871754547 ) ) ;
#63034=CARTESIAN_POINT ( 'NONE',  ( 5.082755093536320601, -5.082755093536318824, 27.92405278187175455 ) ) ;
#63038=CARTESIAN_POINT ( 'NONE',  ( -5.082755093536319713, 5.082755093536319713, 1.674052781871753659 ) ) ;
#63053=CARTESIAN_POINT ( 'NONE',  ( -5.656854249492373476, -5.656854249492376141, 22.01780277982336997 ) ) ;
#63069=CARTESIAN_POINT ( 'NONE',  ( 5.656854249492376141, -5.656854249492374365, 22.44905278432982243 ) ) ;
#63073=ORIENTED_EDGE ( 'NONE', *, *, #28326, .T. ) ;
#63087=DIRECTION ( 'NONE',  ( 0.000000000000000000, 0.000000000000000000, 1.000000000000000000 ) ) ;
#63093=DIRECTION ( 'NONE',  ( -0.000000000000000000, -0.000000000000000000, 1.000000000000000000 ) ) ;
#63097=CARTESIAN_POINT ( 'NONE',  ( 0.000000000000000000, 0.000000000000000000, 0.000000000000000000 ) ) ;
#63100=CARTESIAN_POINT ( 'NONE',  ( -2.977408999572647819, 7.188101187499991163, 17.70530278187175455 ) ) ;
#63114=CARTESIAN_POINT ( 'NONE',  ( 7.999999999999991118, 9.797174393178815797E-16, 7.580302779823366421 ) ) ;
#63122=CARTESIAN_POINT ( 'NONE',  ( -5.082755093536317936, -5.082755093536320601, 15.54905278187175632 ) ) ;
#63144=CARTESIAN_POINT ( 'NONE',  ( -5.656854249492375253, 5.656854249492375253, 3.642802779823362869 ) ) ;
#63149=CARTESIAN_POINT ( 'NONE',  ( 7.999999999999991118, 9.797174393178815797E-16, 10.58030277982336465 ) ) ;
#63158=CARTESIAN_POINT ( 'NONE',  ( 3.499857865026532622, -7.193933550196781823, 0.0006324257780546024528 ) ) ;
#63173=CARTESIAN_POINT ( 'NONE',  ( 8.008118988124991233, 3.317071493978879015, 13.85686528394062833 ) ) ;
#63188=CARTESIAN_POINT ( 'NONE',  ( -4.898587196589407898E-16, 7.999999999999991118, 9.642802783920146226 ) ) ;
#63202=CARTESIAN_POINT ( 'NONE',  ( 7.188101187499992051, 8.802885111219154394E-16, 20.61155278187175455 ) ) ;
#63227=CARTESIAN_POINT ( 'NONE',  ( -5.656854249492373476, -5.656854249492376141, 23.51780277982336642 ) ) ;
#63243=CARTESIAN_POINT ( 'NONE',  ( 7.999999999999968914, 3.313708498984778483, 22.67405277982336287 ) ) ;
#63246=CARTESIAN_POINT ( 'NONE',  ( -3.313708498984758943, -7.999999999999989342, 11.79905278392014800 ) ) ;
#63278=ORIENTED_EDGE ( 'NONE', *, *, #15733, .T. ) ;
#63293=CARTESIAN_POINT ( 'NONE',  ( -5.082755093536317936, -5.082755093536320601, 4.674052781871752771 ) ) ;
#63320=CARTESIAN_POINT ( 'NONE',  ( 2.977408999572646486, 7.188101187499991163, 7.392802781871750994 ) ) ;
#63333=ADVANCED_FACE ( 'NONE', ( #5139 ), #56079, .F. ) ;
#63334=CARTESIAN_POINT ( 'NONE',  ( 1.469576158976822172E-15, -7.999999999999991118, 4.205302779823362869 ) ) ;
#63335=DIRECTION ( 'NONE',  ( -0.000000000000000000, -0.000000000000000000, 1.000000000000000000 ) ) ;
#63348=CARTESIAN_POINT ( 'NONE',  ( -7.999999999999991118, 3.313708498984756723, 5.292802784329825094 ) ) ;
#63355=CARTESIAN_POINT ( 'NONE',  ( -7.188101187499990274, -2.977408999572651815, 27.08030278187175810 ) ) ;
#63367=CARTESIAN_POINT ( 'NONE',  ( -3.313708498984758943, -7.999999999999989342, 19.29905278392014978 ) ) ;
#63378=CARTESIAN_POINT ( 'NONE',  ( -5.082755093536319713, 5.082755093536319713, 22.29905278187175455 ) ) ;
#63391=CARTESIAN_POINT ( 'NONE',  ( 2.977408999572646486, 7.188101187499991163, 2.892802781871751439 ) ) ;
#63396=CARTESIAN_POINT ( 'NONE',  ( 8.008118988124993010, -3.317071493978877239, 3.169365283940628331 ) ) ;
#63403=CARTESIAN_POINT ( 'NONE',  ( -7.188101187499990274, -2.977408999572651371, 25.95530278187175810 ) ) ;
#63420=CARTESIAN_POINT ( 'NONE',  ( 7.999999999999991118, 3.313708498984757611, 22.67405277982336287 ) ) ;
#63435=CARTESIAN_POINT ( 'NONE',  ( -4.898587196589407898E-16, 7.999999999999991118, 26.01155278432982243 ) ) ;
#63470=CARTESIAN_POINT ( 'NONE',  ( 7.188101187499993827, -2.977408999572645598, 21.64280278187176165 ) ) ;
#63496=CARTESIAN_POINT ( 'NONE',  ( -4.401442555609577197E-16, 7.188101187499992051, 14.98655278187175455 ) ) ;
#63516=CARTESIAN_POINT ( 'NONE',  ( -3.313708498984757167, 7.999999999999991118, 2.049052779823364645 ) ) ;
#63529=CARTESIAN_POINT ( 'NONE',  ( 4.787532741003091452, -6.454502166345807979, -0.000000000000000000 ) ) ;
#63542=CARTESIAN_POINT ( 'NONE',  ( 8.008118988124991233, 3.317071493978879015, 16.85686528394063188 ) ) ;
#63548=CARTESIAN_POINT ( 'NONE',  ( 5.082755093536318824, 5.082755093536319713, 12.92405278187175277 ) ) ;
#63561=CARTESIAN_POINT ( 'NONE',  ( 3.313708498984756279, 7.999999999999991118, 6.549052783920143561 ) ) ;
#63576=CARTESIAN_POINT ( 'NONE',  ( 1.320432766682872962E-15, -7.188101187499992051, 15.73655278187175632 ) ) ;
#63591=DIRECTION ( 'NONE',  ( 0.000000000000000000, 0.000000000000000000, -1.000000000000000000 ) ) ;
#63593=( BOUNDED_CURVE ( )  B_SPLINE_CURVE ( 2, ( #30180, #30913, #42599, #25240, #13911, #53199, #36950, #24513, #59956 ),
 .UNSPECIFIED., .F., .F. ) 
 B_SPLINE_CURVE_WITH_KNOTS ( ( 3, 2, 2, 2, 3 ),
 ( 0.4736842105263158187, 0.4802631578947368918, 0.4868421052631579649, 0.4934210526315789269, 0.5000000000000000000 ),
 .UNSPECIFIED. ) 
 CURVE ( )  GEOMETRIC_REPRESENTATION_ITEM ( )  RATIONAL_B_SPLINE_CURVE ( ( 0.9999999999999993339, 0.9238795325112874046, 1.000000000000000000, 0.9238795325112867385, 1.000000000000000000, 0.9238795325112867385, 1.000000000000000000, 0.9238795325112867385, 1.000000000000000000 ) ) 
 REPRESENTATION_ITEM ( '' )  );
#63600=CARTESIAN_POINT ( 'NONE',  ( -5.656854249492375253, 5.656854249492375253, 18.64280277982336642 ) ) ;
#63604=ORIENTED_EDGE ( 'NONE', *, *, #16881, .T. ) ;
#63611=ORIENTED_EDGE ( 'NONE', *, *, #10166, .T. ) ;
#63619=CARTESIAN_POINT ( 'NONE',  ( 7.999999999999991118, 3.313708498984757611, 9.361552783920146226 ) ) ;
#63634=CARTESIAN_POINT ( 'NONE',  ( 7.999999999999706901, -2.135495361439877059E-06, 10.76780272350167245 ) ) ;
#63651=CARTESIAN_POINT ( 'NONE',  ( 1.469576158976822172E-15, -7.999999999999991118, 19.20530277982336642 ) ) ;
#63653=VECTOR ( 'NONE', #72109, 1000.000000000000000 ) ;
#63658=CARTESIAN_POINT ( 'NONE',  ( 8.000000000000035527, 3.313708498984715423, 6.174052779823363757 ) ) ;
#63668=CARTESIAN_POINT ( 'NONE',  ( -4.401442555609577197E-16, 7.188101187499992051, 8.611552781871752771 ) ) ;
#63676=CARTESIAN_POINT ( 'NONE',  ( -6.062591786044946751, -5.219672483564715471, -0.3118205092643556720 ) ) ;
#63680=EDGE_CURVE ( 'NONE', #39327, #43701, #23282, .T. ) ;
#63691=CARTESIAN_POINT ( 'NONE',  ( 5.082755093536318824, 5.082755093536319713, 11.79905278187175632 ) ) ;
#63706=CARTESIAN_POINT ( 'NONE',  ( -7.999999999999991118, 3.313708498984756723, 3.736552779823362869 ) ) ;
#63730=CARTESIAN_POINT ( 'NONE',  ( 5.082755093536320601, -5.082755093536318824, 27.54905278187175455 ) ) ;
#63743=CARTESIAN_POINT ( 'NONE',  ( -3.313708498984758943, -7.999999999999989342, 22.29905278392014623 ) ) ;
#63754=CARTESIAN_POINT ( 'NONE',  ( -7.188101187499992051, 0.000000000000000000, 22.48655278187175455 ) ) ;
#63771=CARTESIAN_POINT ( 'NONE',  ( -4.903558642999205574E-16, 8.008118988124991233, 0.6381152839406293298 ) ) ;
#63775=CARTESIAN_POINT ( 'NONE',  ( -3.313708498984759387, -7.999999999999989342, 7.111552779823365533 ) ) ;
#63778=CARTESIAN_POINT ( 'NONE',  ( 7.188101187499991163, 2.977408999572648707, 28.20530278187175455 ) ) ;
#63794=CARTESIAN_POINT ( 'NONE',  ( -7.999999999999991118, 0.000000000000000000, 23.33030277982336642 ) ) ;
#63810=CARTESIAN_POINT ( 'NONE',  ( 1.469576158976822172E-15, -7.999999999999991118, 25.26155278432982954 ) ) ;
#63847=CARTESIAN_POINT ( 'NONE',  ( 5.082755093536320601, -5.082755093536318824, 11.04905278187175455 ) ) ;
#63870=CARTESIAN_POINT ( 'NONE',  ( -7.188101187499992051, 2.977408999572646930, 10.76780278187175632 ) ) ;
#63883=CARTESIAN_POINT ( 'NONE',  ( 0.000000000000000000, 0.000000000000000000, 30.00000000000000000 ) ) ;
#63904=ADVANCED_FACE ( 'NONE', ( #6231 ), #22814, .F. ) ;
#63919=CARTESIAN_POINT ( 'NONE',  ( -5.662595241051933570, -5.662595241051936235, 11.70061528394062833 ) ) ;
#63927=CARTESIAN_POINT ( 'NONE',  ( 5.082755093536320601, -5.082755093536318824, 9.549052781871754547 ) ) ;
#63943=CARTESIAN_POINT ( 'NONE',  ( -5.656854249492373476, -5.656854249492376141, 1.205302783920146004 ) ) ;
#63958=CARTESIAN_POINT ( 'NONE',  ( 5.082755093536318824, 5.082755093536319713, 14.79905278187175455 ) ) ;
#63965=CARTESIAN_POINT ( 'NONE',  ( 1.320432766682872962E-15, -7.188101187499992051, 26.23655278187175810 ) ) ;
#63975=CARTESIAN_POINT ( 'NONE',  ( 1.469576158976822172E-15, -7.999999999999991118, 25.20530277982336642 ) ) ;
#63982=CARTESIAN_POINT ( 'NONE',  ( 1.469576158976822172E-15, -7.999999999999991118, 22.20530277982336997 ) ) ;
#64000=CARTESIAN_POINT ( 'NONE',  ( -5.656854249492375253, 5.656854249492375253, 6.830302783920143561 ) ) ;
#64029=ORIENTED_EDGE ( 'NONE', *, *, #42354, .F. ) ;
#64034=AXIS2_PLACEMENT_3D ( 'NONE', #39322, #64558, #1572 ) ;
#64050=CARTESIAN_POINT ( 'NONE',  ( -4.401442555609577197E-16, 7.188101187499992051, 5.611552781871753659 ) ) ;
#64060=AXIS2_PLACEMENT_3D ( 'NONE', #74156, #52274, #46968 ) ;
#64061=DIRECTION ( 'NONE',  ( -0.000000000000000000, -0.000000000000000000, 1.000000000000000000 ) ) ;
#64075=CARTESIAN_POINT ( 'NONE',  ( 7.188101187499991163, 2.977408999572648707, 10.20530278187175455 ) ) ;
#64078=CARTESIAN_POINT ( 'NONE',  ( -7.999999999999989342, -3.313708498984762496, 2.480302784329821542 ) ) ;
#64088=CARTESIAN_POINT ( 'NONE',  ( -5.656854249492373476, -5.656854249492376141, 22.20530278392014623 ) ) ;
#64108=CARTESIAN_POINT ( 'NONE',  ( 7.188101187499993827, -2.977408999572645598, 27.64280278187175455 ) ) ;
#64118=CARTESIAN_POINT ( 'NONE',  ( -5.656854249492373476, -5.656854249492376141, 20.70530278392014623 ) ) ;
#64121=DIRECTION ( 'NONE',  ( 1.000000000000000000, 0.000000000000000000, 0.000000000000000000 ) ) ;
#64130=CARTESIAN_POINT ( 'NONE',  ( 1.320432766682872962E-15, -7.188101187499992051, 24.36155278187175810 ) ) ;
#64147=CARTESIAN_POINT ( 'NONE',  ( -3.317071493978878571, 8.008118988124991233, 0.7318652839406294408 ) ) ;
#64154=CARTESIAN_POINT ( 'NONE',  ( 7.188101187499993827, -2.977408999572645598, 28.01780278187175455 ) ) ;
#64158=CARTESIAN_POINT ( 'NONE',  ( -7.999999999929542582, -2.214810345207895024E-05, 22.01864141485938831 ) ) ;
#64162=CARTESIAN_POINT ( 'NONE',  ( 0.000000000000000000, 0.000000000000000000, 11.00000000000000000 ) ) ;
#64176=CARTESIAN_POINT ( 'NONE',  ( 7.999999999999991118, 9.797174393178815797E-16, 13.58030277982336465 ) ) ;
#64191=CARTESIAN_POINT ( 'NONE',  ( -3.313708498984758943, -7.999999999999989342, 26.66780278432982598 ) ) ;
#64220=CARTESIAN_POINT ( 'NONE',  ( 5.082755093536320601, -5.082755093536318824, 12.54905278187175277 ) ) ;
#64243=CARTESIAN_POINT ( 'NONE',  ( 2.977408999572646486, 7.188101187499992051, 10.39280278187175632 ) ) ;
#64258=DIRECTION ( 'NONE',  ( -0.000000000000000000, -0.000000000000000000, 1.000000000000000000 ) ) ;
#64292=CARTESIAN_POINT ( 'NONE',  ( -4.903558642999205574E-16, 8.008118988124991233, 15.63811528394063188 ) ) ;
#64298=CARTESIAN_POINT ( 'NONE',  ( -2.977408999572647819, 7.188101187499992051, 7.205302781871751883 ) ) ;
#64302=AXIS2_PLACEMENT_3D ( 'NONE', #22092, #74154, #5506 ) ;
#64312=CARTESIAN_POINT ( 'NONE',  ( -5.867880820906206552, -5.445827678078542178, -0.3031404557143344003 ) ) ;
#64326=CARTESIAN_POINT ( 'NONE',  ( -5.082755093536319713, 5.082755093536319713, 16.67405278187175810 ) ) ;
#64340=CARTESIAN_POINT ( 'NONE',  ( 5.656854249492374365, 5.656854249492375253, 25.76780277982336997 ) ) ;
#64352=CYLINDRICAL_SURFACE ( 'NONE', #20435, 7.999999999999991118 ) ;
#64353=CARTESIAN_POINT ( 'NONE',  ( -7.999999999999989342, -3.313708498984762496, 15.92405277982336465 ) ) ;
#64371=CARTESIAN_POINT ( 'NONE',  ( 7.999999999999992895, -3.313708498984756279, 4.674052783920145338 ) ) ;
#64387=CARTESIAN_POINT ( 'NONE',  ( -7.999999999999979572, -3.313708498984773154, 26.42405277982336642 ) ) ;
#64422=CARTESIAN_POINT ( 'NONE',  ( -2.977408999572647819, 7.188101187499991163, 8.705302781871752771 ) ) ;
#64434=VECTOR ( 'NONE', #70353, 1000.000000000000000 ) ;
#64447=CARTESIAN_POINT ( 'NONE',  ( -2.977408999572648707, -7.188101187499990274, 6.642802781871754547 ) ) ;
#64462=CARTESIAN_POINT ( 'NONE',  ( -7.999999999999991118, 0.000000000000000000, 26.51780278392014623 ) ) ;
#64483=CARTESIAN_POINT ( 'NONE',  ( -7.188101187499992051, 0.000000000000000000, 25.48655278187175810 ) ) ;
#64492=CARTESIAN_POINT ( 'NONE',  ( -4.898587196589407898E-16, 7.999999999999991118, 21.64280278392014623 ) ) ;
#64504=CARTESIAN_POINT ( 'NONE',  ( 5.082755093536320601, -5.082755093536318824, 24.54905278187175810 ) ) ;
#64520=CARTESIAN_POINT ( 'NONE',  ( 1.471067592899761672E-15, -8.008118988124991233, 4.388115283940629219 ) ) ;
#64527=CARTESIAN_POINT ( 'NONE',  ( 1.320432766682872962E-15, -7.188101187499992051, 26.23655278187175810 ) ) ;
#64535=VERTEX_POINT ( 'NONE', #10669 ) ;
#64544=CARTESIAN_POINT ( 'NONE',  ( -7.999999999999991118, 0.000000000000000000, 17.33030277982336287 ) ) ;
#64558=DIRECTION ( 'NONE',  ( -0.000000000000000000, -0.9659258262890700886, -0.2588190451025146888 ) ) ;
#64559=CARTESIAN_POINT ( 'NONE',  ( -5.656854249492373476, -5.656854249492376141, 19.07405278432982598 ) ) ;
#64592=CARTESIAN_POINT ( 'NONE',  ( -2.977408999572648707, -7.188101187499990274, 15.26780278187175455 ) ) ;
#64617=CARTESIAN_POINT ( 'NONE',  ( -7.188101187499992051, 0.000000000000000000, 10.86155278187175455 ) ) ;
#64637=CARTESIAN_POINT ( 'NONE',  ( -5.656854249492373476, -5.656854249492376141, 1.017802779823363757 ) ) ;
#64659=CARTESIAN_POINT ( 'NONE',  ( -3.317071493978878571, 8.008118988124991233, 14.23186528394062833 ) ) ;
#64664=CARTESIAN_POINT ( 'NONE',  ( -4.401442555609577197E-16, 7.188101187499992051, 8.611552781871752771 ) ) ;
#64679=CARTESIAN_POINT ( 'NONE',  ( 1.469576158976822172E-15, -7.999999999999991118, -0.1071972160798552454 ) ) ;
#64695=CARTESIAN_POINT ( 'NONE',  ( -7.188101187499992051, 0.000000000000000000, 13.86155278187175455 ) ) ;
#64697=CARTESIAN_POINT ( 'NONE',  ( -7.999999999999948486, 3.313708498984799355, 3.736552779823361092 ) ) ;
#64713=PRODUCT_DEFINITION_FORMATION_WITH_SPECIFIED_SOURCE ( 'ANY', '', #11413, .NOT_KNOWN. ) ;
#64723=CARTESIAN_POINT ( 'NONE',  ( -7.999999999999991118, 3.313708498984756723, 14.23655277982336642 ) ) ;
#64740=VERTEX_POINT ( 'NONE', #10592 ) ;
#64749=ORIENTED_EDGE ( 'NONE', *, *, #29256, .T. ) ;
#64783=CARTESIAN_POINT ( 'NONE',  ( 7.188101187499993827, -2.977408999572645598, 9.642802781871756324 ) ) ;
#64807=CARTESIAN_POINT ( 'NONE',  ( -5.082755093536319713, 5.082755093536319713, 6.174052781871754547 ) ) ;
#64821=CARTESIAN_POINT ( 'NONE',  ( -4.898587196589407898E-16, 7.999999999999991118, 24.64280278392014978 ) ) ;
#64838=CARTESIAN_POINT ( 'NONE',  ( 3.313708498984762496, -7.999999999999989342, 11.98655278392014445 ) ) ;
#64843=CARTESIAN_POINT ( 'NONE',  ( -2.977408999572647819, -7.188101187499990274, 21.26780278187175810 ) ) ;
#64851=CARTESIAN_POINT ( 'NONE',  ( 5.656854249492374365, 5.656854249492375253, 16.95530278392014978 ) ) ;
#64864=CARTESIAN_POINT ( 'NONE',  ( -7.188101187499991163, 2.977408999572646930, 23.89280278187176165 ) ) ;
#64881=CARTESIAN_POINT ( 'NONE',  ( 8.008118988124991233, 9.807117285998411148E-16, 1.763115283940626776 ) ) ;
#64888=CARTESIAN_POINT ( 'NONE',  ( 2.977408999572650927, -7.188101187499990274, 23.33030278187175455 ) ) ;
#64903=CARTESIAN_POINT ( 'NONE',  ( -7.999999999999991118, 3.313708498984756723, 15.73655277982336642 ) ) ;
#64916=CARTESIAN_POINT ( 'NONE',  ( 7.999999999999991118, 3.313708498984757611, 15.23030278432982243 ) ) ;
#64947=CARTESIAN_POINT ( 'NONE',  ( -2.977408999572647819, 7.188101187499991163, 13.20530278187175277 ) ) ;
#64968=CARTESIAN_POINT ( 'NONE',  ( 5.082755093536320601, -5.082755093536318824, 12.92405278187175277 ) ) ;
#64974=CARTESIAN_POINT ( 'NONE',  ( -7.999999999999991118, 3.313708498984757167, 3.924052783920144893 ) ) ;
#65003=ORIENTED_EDGE ( 'NONE', *, *, #10935, .F. ) ;
#65015=CARTESIAN_POINT ( 'NONE',  ( -8.008118988124989457, -3.317071493978883900, 7.106865283940628331 ) ) ;
#65019=CARTESIAN_POINT ( 'NONE',  ( -5.082755093536319713, 5.082755093536319713, 11.79905278187175277 ) ) ;
#65033=CARTESIAN_POINT ( 'NONE',  ( -5.656854249492375253, 5.656854249492375253, 0.8303027839201455595 ) ) ;
#65050=CARTESIAN_POINT ( 'NONE',  ( -7.999999999961178609, -1.665943300379353739E-05, 2.518425711869641592 ) ) ;
#65055=CARTESIAN_POINT ( 'NONE',  ( -3.313708498984759387, -7.999999999999989342, 4.111552779823362869 ) ) ;
#65073=CARTESIAN_POINT ( 'NONE',  ( 7.999999999999991118, 3.313708498984757611, 15.17405277982336642 ) ) ;
#65106=CARTESIAN_POINT ( 'NONE',  ( 8.008118988124991233, 3.317071493978879015, 25.85686528394063188 ) ) ;
#65123=( BOUNDED_CURVE ( )  B_SPLINE_CURVE ( 2, ( #63006, #50943, #28672, #55877, #11330, #34363, #45285, #10216, #15854 ),
 .UNSPECIFIED., .F., .F. ) 
 B_SPLINE_CURVE_WITH_KNOTS ( ( 3, 2, 2, 2, 3 ),
 ( 0.6353544975714136012, 0.6419727316923105054, 0.6485910072767669954, 0.6552092828612233744, 0.6618275503331610965 ),
 .UNSPECIFIED. ) 
 CURVE ( )  GEOMETRIC_REPRESENTATION_ITEM ( )  RATIONAL_B_SPLINE_CURVE ( ( 0.9999990462150658566, 0.9238800094067415314, 1.000000000000000000, 0.9238795325112867385, 1.000000000000000000, 0.9238795325112867385, 1.000000000000000000, 0.9238795325112867385, 1.000000000000000000 ) ) 
 REPRESENTATION_ITEM ( '' )  );
#65141=CARTESIAN_POINT ( 'NONE',  ( -2.977408999572647819, 7.188101187499991163, 28.58030278187176165 ) ) ;
#65152=ORIENTED_EDGE ( 'NONE', *, *, #28614, .F. ) ;
#65165=CARTESIAN_POINT ( 'NONE',  ( 5.082755093536320601, -5.082755093536318824, 5.424052781871753659 ) ) ;
#65180=CARTESIAN_POINT ( 'NONE',  ( 3.313708498984762496, -7.999999999999989342, 23.98655278392014978 ) ) ;
#65203=CARTESIAN_POINT ( 'NONE',  ( -7.188101187499992051, 0.000000000000000000, 22.48655278187175455 ) ) ;
#65206=ORIENTED_EDGE ( 'NONE', *, *, #73288, .F. ) ;
#65211=ADVANCED_FACE ( 'NONE', ( #54383 ), #72081, .F. ) ;
#65214=CARTESIAN_POINT ( 'NONE',  ( -7.999999999999991118, 0.000000000000000000, 16.01780278392014978 ) ) ;
#65225=CARTESIAN_POINT ( 'NONE',  ( -5.082755093536319713, 5.082755093536319713, 19.29905278187175455 ) ) ;
#65244=CARTESIAN_POINT ( 'NONE',  ( 1.471067592899761672E-15, -8.008118988124991233, -0.1118847160593713225 ) ) ;
#65251=CARTESIAN_POINT ( 'NONE',  ( -7.188101187499991163, 2.977408999572646930, 21.26780278187175810 ) ) ;
#65261=CARTESIAN_POINT ( 'NONE',  ( -3.313708498984757611, 7.999999999999991118, 18.54905277982336287 ) ) ;
#65269=CARTESIAN_POINT ( 'NONE',  ( 3.313708498984762496, -7.999999999999989342, 14.79905277982336465 ) ) ;
#65286=CARTESIAN_POINT ( 'NONE',  ( -5.656854249492375253, 5.656854249492375253, 20.19905278432982243 ) ) ;
#65319=CARTESIAN_POINT ( 'NONE',  ( -7.188101187499992051, 0.000000000000000000, 14.98655278187175455 ) ) ;
#65333=ORIENTED_EDGE ( 'NONE', *, *, #27003, .F. ) ;
#65345=CARTESIAN_POINT ( 'NONE',  ( -5.082755093536317936, -5.082755093536320601, 8.049052781871752771 ) ) ;
#65352=ORIENTED_EDGE ( 'NONE', *, *, #67745, .T. ) ;
#65370=VERTEX_POINT ( 'NONE', #32872 ) ;
#65390=CARTESIAN_POINT ( 'NONE',  ( 5.662595241051934458, 5.662595241051935346, 9.450615283940630107 ) ) ;
#65397=CARTESIAN_POINT ( 'NONE',  ( -2.977408999572647819, 7.188101187499992051, 8.705302781871752771 ) ) ;
#65409=CARTESIAN_POINT ( 'NONE',  ( -7.999999999999991118, 3.313708498984756723, 3.924052783920144893 ) ) ;
#65422=EDGE_CURVE ( 'NONE', #62523, #71023, #65123, .T. ) ;
#65433=CARTESIAN_POINT ( 'NONE',  ( -4.401442555609577197E-16, 7.188101187499992051, 26.98655278187175455 ) ) ;
#65445=DIRECTION ( 'NONE',  ( -0.000000000000000000, -0.000000000000000000, -1.000000000000000000 ) ) ;
#65452=CARTESIAN_POINT ( 'NONE',  ( -4.898587196589407898E-16, 7.999999999999991118, 16.95530277982336287 ) ) ;
#65456=( BOUNDED_SURFACE ( )  B_SPLINE_SURFACE ( 1, 2, ( 
 ( #3605, #59831, #71875, #36455, #19455, #2487, #13417, #20944, #7781, #49240, #72255, #13777, #65848, #49625, #31150, #48126, #66224, #60192, #37941, #2858, #54925, #14158, #14529, #65106, #37191, #20569, #20189, #25846, #36821, #8513, #48866, #8146, #43208, #54182, #30786, #48496, #71132, #26603, #53806, #25479, #32285, #71500, #43583, #37567, #2116, #66598, #14903, #19824, #60941, #9262, #51481, #73749, #61320, #15277, #61693, #62425, #32666, #73010, #5105, #3991, #45445, #22056, #50734, #38314, #57155, #74492, #9645, #62058, #38691, #4355, #28473, #68461, #74123, #16762, #43965, #4728, #56784, #56409, #27723, #21319, #45083, #66974, #22425, #55675, #28096, #67727, #68098, #33046, #16024, #39787, #16386, #27346, #10383, #33785, #21686, #26980, #62790, #10015, #51111, #5471, #39426, #56046, #10750, #11132, #50362, #34155, #49994, #44342, #67352, #73381, #39057, #15650, #33409, #44712, #12600, #568, #29590, #941, #41649, #63542, #7321, #11867, #5847, #23923, #17897, #70325, #35267, #41282, #23551, #46932, #22800, #46563, #64292, #52603, #58282, #69208, #40910, #6584, #46191, #69957, #23181, #40168, #6217, #28840, #35997, #59014, #40536, #64659, #51859, #35626, #18267, #63173, #58640, #69584, #17520, #12957, #6948, #30326, #29960, #11499, #68831, #34903, #52973, #34532, #203, #1306, #57538, #24288, #47301, #18640, #17143, #53344, #45820, #57909, #63919, #29222, #52236, #12230, #66132, #71783, #43113, #1671, #19734, #25755, #71409, #48404, #30695, #65758, #26127, #20099, #47661, #48776, #8050, #42743, #19361, #31055, #14437, #14061, #65390, #2390, #2768, #59742, #59376, #37470, #48032, #60471, #3144, #37097, #71041, #60101, #54461, #42375, #8800, #31813, #7687, #8419, #13688, #54082, #13323, #31434, #54834, #36729, #24651, #65015, #70683, #36361, #25387, #42006, #25013, #2026, #19000, #53713, #18126, #59239, #23409, #1886, #46788, #429, #35853, #40398, #24872, #69069, #70546, #47154, #29077, #41504, #36221, #58499, #6448, #23784, #70186, #12457, #64520, #12818, #1164, #30556, #69810, #58141, #58868, #46424, #24516, #47521, #13183, #29818, #17374, #63396, #52097, #52460, #11722, #6070, #18495, #798, #34762, #69438, #7179, #53571, #29451, #6805, #41142, #17749, #64881, #24142, #57764, #7548, #30185, #53203, #40764, #1536, #18862, #41868, #52831, #64147, #63771, #12088, #35126, #35487, #2629, #14670, #42968, #31671, #65244, #42231, #60710, #55063, #36587 ),
 ( #59598, #2999, #8656, #26359, #32043, #38083, #36954, #13915, #19225, #9031, #59960, #7911, #37709, #3372, #13549, #43346, #25245, #61080, #14294, #48262, #49381, #37331, #55437, #20712, #30917, #25980, #53938, #25617, #2252, #9408, #19962, #72400, #43728, #60328, #71269, #8278, #19588, #66364, #32426, #42604, #54690, #65619, #31288, #54318, #70911, #3747, #48631, #66742, #15048, #71641, #65989, #49005, #47891, #72015, #20330, #58106, #34360, #6041, #41476, #57361, #35459, #63743, #1134, #29423, #18097, #51683, #28669, #47126, #64492, #23015, #52432, #18466, #46394, #11692, #5672, #41111, #28, #46022, #64118, #69043, #12425, #69780, #12792, #35824, #24490, #23381, #402, #17346, #70159, #69412, #40368, #24112, #58839, #63367, #29790, #34731, #47492, #769, #57736, #7150, #23755, #41842, #30155, #29046, #58472, #52065, #12061, #17718, #70516, #6417, #53172, #1510, #46757, #40733, #35096, #6782, #52800, #18835, #64851, #19929, #59209, #42199, #25217, #36193, #43699, #7519, #48972, #20299, #65214, #65588, #30525, #49352, #8627, #60297, #24844, #14638, #65960, #47862, #31639, #55034, #2599, #48233, #42575, #14264, #31259, #54660, #2968, #42939, #72369, #13887, #2221, #25953, #13519, #43317, #66334, #32015, #48605, #13155, #53542, #70883, #71241, #1858, #19197, #37301, #19561, #36557, #59570, #71986, #20680, #36926, #25589, #59934, #7885, #9000, #37681, #30890, #3341, #60681, #26331, #53908, #8246, #54288, #71608, #28492, #46214, #51882, #57933, #55783, #32775, #38052, #5865, #4099, #26717, #34551, #28861, #61052, #63188, #44080, #6240, #34173, #67092, #222, #57175, #589, #40559, #9374, #22823, #3718, #45463, #21057, #29244, #39809, #23202, #17540, #5491, #32394, #27092, #15389, #11519, #52256, #61429, #74512, #55409, #38425, #50108, #15016, #23572, #49737, #69230, #63561, #9756, #68479, #72753, #66714, #57556, #40185, #73122, #11888, #45839, #22444, #34922, #16782, #51500, #62813, #11149, #68854, #17166, #19020, #42026, #53365, #8073, #24309, #35647, #36379, #23943, #2045, #25032, #65409, #7340, #46581, #40933, #29611, #29977, #69603, #58300, #24670, #52995, #17917, #960, #59394, #31073, #58661, #36015, #6968, #46950, #42393, #1691, #54102, #36750, #47681, #30713, #52624, #70701, #13342, #69979, #70348, #63943, #18288, #53734, #12252, #65033, #1326, #7707, #41669, #30346, #35288, #6605, #48052, #71061, #41303, #64679, #19379, #47321, #64312, #12617 ),
 ( #13706, #18659, #2414, #59763, #12978, #59033, #25409, #60866, #38240, #37870, #9188, #2787, #55228, #32973, #55600, #71426, #61244, #49168, #32209, #14456, #72177, #26908, #3533, #8820, #43507, #15209, #3161, #8437, #49923, #43135, #9575, #61623, #49550, #66152, #72568, #66905, #37492, #32593, #3919, #31457, #20872, #60493, #20490, #37117, #14830, #72938, #54850, #21247, #42761, #43893, #65778, #48794, #48423, #25773, #54482, #38620, #44271, #66519, #15580, #71802, #55974, #26149, #20121, #67282, #19754, #14081, #60119, #9939, #26524, #31831, #57083, #23108, #45017, #63470, #68022, #61989, #5398, #74049, #51784, #16688, #22729, #5033, #28401, #4284, #28030, #45749, #34087, #39720, #50660, #22349, #62721, #27652, #11058, #4657, #21616, #62349, #10311, #17446, #40467, #21990, #46121, #33337, #17073, #51408, #44641, #74423, #51041, #73679, #69139, #68761, #11794, #40095, #67655, #50293, #16316, #63100, #15955, #56339, #11425, #38982, #5770, #34462, #57465, #73314, #34832, #45375, #39352, #27276, #28768, #10680, #132, #33713, #56715, #68390, #1602, #46491, #12161, #18933, #17824, #59309, #35926, #64592, #29150, #70978, #65319, #18199, #41939, #18568, #41212, #42302, #7617, #13257, #30624, #57839, #41578, #70613, #70256, #12890, #35196, #58943, #13623, #36293, #52168, #64947, #6879, #7249, #46863, #29890, #53646, #30259, #64220, #1236, #47590, #35559, #40838, #1956, #869, #24946, #19293, #53277, #23855, #24586, #47963, #69886, #6143, #499, #63847, #23479, #12528, #52902, #69512, #47228, #58212, #58571, #6514, #29521, #52531, #24214, #60028, #59672, #13986, #65686, #49833, #32499, #60401, #26820, #37026, #44180, #14367, #42673, #3442, #7983, #67194, #36662, #26430, #37400, #43417, #14742, #55511, #2697, #21156, #25685, #19661, #37782, #31740, #9484, #49076, #55136, #8728, #60778, #30989, #54761, #49457, #66432, #72089, #8346, #3070, #20403, #31362, #9103, #54390, #54009, #20028, #48703, #72852, #2321, #71711, #3823, #43041, #72476, #32117, #25316, #20783, #43803, #66818, #15120, #66060, #38150, #48332, #61153, #71340, #26054, #39265, #73961, #4566, #62265, #16981, #22265, #73589, #33622, #5309, #67934, #73224, #40008, #33250, #28312, #51693, #39637, #56249, #62634, #56996, #27562, #51321, #22638, #21530, #10966, #50572, #10593, #27187, #4943, #63011, #44927, #45658, #32879, #34002, #55883, #38895, #38528, #67565, #44553, #28679, #11335, #56628, #5680, #15862 ) ),
 .UNSPECIFIED., .F., .F., .F. ) 
 B_SPLINE_SURFACE_WITH_KNOTS ( ( 2, 1, 2 ),
 ( 3, 2, 2, 2, 2, 2, 2, 2, 2, 2, 2, 2, 2, 2, 2, 2, 2, 2, 2, 2, 2, 2, 2, 2, 2, 2, 2, 2, 2, 2, 2, 2, 2, 2, 2, 2, 2, 2, 2, 2, 2, 2, 2, 2, 2, 2, 2, 2, 2, 2, 2, 2, 2, 2, 2, 2, 2, 2, 2, 2, 2, 2, 2, 2, 2, 2, 2, 2, 2, 2, 2, 2, 2, 2, 2, 2, 2, 2, 2, 2, 2, 2, 2, 2, 2, 2, 2, 2, 2, 2, 2, 2, 2, 2, 2, 2, 2, 2, 2, 2, 2, 2, 2, 2, 2, 2, 2, 2, 2, 2, 2, 2, 2, 2, 2, 2, 2, 2, 2, 2, 2, 2, 2, 2, 2, 2, 2, 2, 2, 2, 2, 2, 2, 2, 2, 2, 2, 2, 2, 2, 2, 2, 2, 2, 2, 2, 2, 2, 2, 2, 2, 2, 3 ),
 ( -0.01000000000000000021, 0.000000000000000000, 1.000000000000000000 ),
 ( 0.000000000000000000, 0.006578947368421052266, 0.01315789473684210453, 0.01973684210526315680, 0.02631578947368420907, 0.03289473684210526133, 0.03947368421052631360, 0.04605263157894736586, 0.05263157894736841813, 0.05921052631578947040, 0.06578947368421052266, 0.07236842105263158187, 0.07894736842105262720, 0.08552631578947368640, 0.09210526315789473173, 0.09868421052631579093, 0.1052631578947368363, 0.1118421052631578955, 0.1184210526315789408, 0.1250000000000000000, 0.1315789473684210453, 0.1381578947368421184, 0.1447368421052631637, 0.1513157894736842091, 0.1578947368421052544, 0.1644736842105263275, 0.1710526315789473728, 0.1776315789473684181, 0.1842105263157894635, 0.1907894736842105365, 0.1973684210526315819, 0.2039473684210526272, 0.2105263157894736725, 0.2171052631578947456, 0.2236842105263157909, 0.2302631578947368363, 0.2368421052631578816, 0.2434210526315789547, 0.2500000000000000000, 0.2565789473684210731, 0.2631578947368420907, 0.2697368421052631637, 0.2763157894736842368, 0.2828947368421052544, 0.2894736842105263275, 0.2960526315789473450, 0.3026315789473684181, 0.3092105263157894912, 0.3157894736842105088, 0.3223684210526315819, 0.3289473684210526550, 0.3355263157894736725, 0.3421052631578947456, 0.3486842105263157632, 0.3552631578947368363, 0.3618421052631579093, 0.3684210526315789269, 0.3750000000000000000, 0.3815789473684210731, 0.3881578947368420907, 0.3947368421052631637, 0.4013157894736842368, 0.4078947368421052544, 0.4144736842105263275, 0.4210526315789473450, 0.4276315789473684181, 0.4342105263157894912, 0.4407894736842105088, 0.4473684210526315819, 0.4539473684210526550, 0.4605263157894736725, 0.4671052631578947456, 0.4736842105263157632, 0.4802631578947368363, 0.4868421052631579093, 0.4934210526315789269, 0.5000000000000000000, 0.5065789473684210176, 0.5131578947368421462, 0.5197368421052631637, 0.5263157894736841813, 0.5328947368421053099, 0.5394736842105263275, 0.5460526315789473450, 0.5526315789473684736, 0.5592105263157894912, 0.5657894736842105088, 0.5723684210526315264, 0.5789473684210526550, 0.5855263157894736725, 0.5921052631578946901, 0.5986842105263158187, 0.6052631578947368363, 0.6118421052631578538, 0.6184210526315789824, 0.6250000000000000000, 0.6315789473684210176, 0.6381578947368421462, 0.6447368421052631637, 0.6513157894736841813, 0.6578947368421053099, 0.6644736842105263275, 0.6710526315789473450, 0.6776315789473684736, 0.6842105263157894912, 0.6907894736842105088, 0.6973684210526315264, 0.7039473684210526550, 0.7105263157894736725, 0.7171052631578946901, 0.7236842105263158187, 0.7302631578947368363, 0.7368421052631578538, 0.7434210526315789824, 0.7500000000000000000, 0.7565789473684210176, 0.7631578947368421462, 0.7697368421052631637, 0.7763157894736841813, 0.7828947368421053099, 0.7894736842105263275, 0.7960526315789473450, 0.8026315789473684736, 0.8092105263157894912, 0.8157894736842105088, 0.8223684210526315264, 0.8289473684210526550, 0.8355263157894736725, 0.8421052631578946901, 0.8486842105263158187, 0.8552631578947368363, 0.8618421052631578538, 0.8684210526315789824, 0.8750000000000000000, 0.8815789473684210176, 0.8881578947368421462, 0.8947368421052631637, 0.9013157894736841813, 0.9078947368421053099, 0.9144736842105263275, 0.9210526315789473450, 0.9276315789473684736, 0.9342105263157894912, 0.9407894736842105088, 0.9473684210526315264, 0.9539473684210526550, 0.9605263157894736725, 0.9671052631578946901, 0.9736842105263158187, 0.9802631578947368363, 0.9868421052631578538, 0.9934210526315789824, 0.9940576549107595916 ),
 .UNSPECIFIED. ) 
 GEOMETRIC_REPRESENTATION_ITEM ( )  RATIONAL_B_SPLINE_SURFACE ( (
 ( 1.000000000000000000, 0.9238795325112867385, 1.000000000000000000, 0.9238795325112867385, 1.000000000000000000, 0.9238795325112867385, 1.000000000000000000, 0.9238795325112867385, 1.000000000000000000, 0.9238795325112867385, 1.000000000000000000, 0.9238795325112867385, 1.000000000000000000, 0.9238795325112867385, 1.000000000000000000, 0.9238795325112867385, 1.000000000000000000, 0.9238795325112867385, 1.000000000000000000, 0.9238795325112867385, 1.000000000000000000, 0.9238795325112867385, 1.000000000000000000, 0.9238795325112867385, 1.000000000000000000, 0.9238795325112867385, 1.000000000000000000, 0.9238795325112867385, 1.000000000000000000, 0.9238795325112867385, 1.000000000000000000, 0.9238795325112867385, 1.000000000000000000, 0.9238795325112867385, 1.000000000000000000, 0.9238795325112867385, 1.000000000000000000, 0.9238795325112867385, 1.000000000000000000, 0.9238795325112867385, 1.000000000000000000, 0.9238795325112867385, 1.000000000000000000, 0.9238795325112867385, 1.000000000000000000, 0.9238795325112867385, 1.000000000000000000, 0.9238795325112867385, 1.000000000000000000, 0.9238795325112867385, 1.000000000000000000, 0.9238795325112867385, 1.000000000000000000, 0.9238795325112867385, 1.000000000000000000, 0.9238795325112867385, 1.000000000000000000, 0.9238795325112867385, 1.000000000000000000, 0.9238795325112867385, 1.000000000000000000, 0.9238795325112867385, 1.000000000000000000, 0.9238795325112867385, 1.000000000000000000, 0.9238795325112867385, 1.000000000000000000, 0.9238795325112867385, 1.000000000000000000, 0.9238795325112867385, 1.000000000000000000, 0.9238795325112867385, 1.000000000000000000, 0.9238795325112867385, 1.000000000000000000, 0.9238795325112867385, 1.000000000000000000, 0.9238795325112867385, 1.000000000000000000, 0.9238795325112867385, 1.000000000000000000, 0.9238795325112867385, 1.000000000000000000, 0.9238795325112867385, 1.000000000000000000, 0.9238795325112867385, 1.000000000000000000, 0.9238795325112867385, 1.000000000000000000, 0.9238795325112867385, 1.000000000000000000, 0.9238795325112867385, 1.000000000000000000, 0.9238795325112867385, 1.000000000000000000, 0.9238795325112867385, 1.000000000000000000, 0.9238795325112867385, 1.000000000000000000, 0.9238795325112867385, 1.000000000000000000, 0.9238795325112867385, 1.000000000000000000, 0.9238795325112867385, 1.000000000000000000, 0.9238795325112867385, 1.000000000000000000, 0.9238795325112867385, 1.000000000000000000, 0.9238795325112867385, 1.000000000000000000, 0.9238795325112867385, 1.000000000000000000, 0.9238795325112867385, 1.000000000000000000, 0.9238795325112867385, 1.000000000000000000, 0.9238795325112867385, 1.000000000000000000, 0.9238795325112867385, 1.000000000000000000, 0.9238795325112867385, 1.000000000000000000, 0.9238795325112867385, 1.000000000000000000, 0.9238795325112867385, 1.000000000000000000, 0.9238795325112867385, 1.000000000000000000, 0.9238795325112867385, 1.000000000000000000, 0.9238795325112867385, 1.000000000000000000, 0.9238795325112867385, 1.000000000000000000, 0.9238795325112867385, 1.000000000000000000, 0.9238795325112867385, 1.000000000000000000, 0.9238795325112867385, 1.000000000000000000, 0.9238795325112867385, 1.000000000000000000, 0.9238795325112867385, 1.000000000000000000, 0.9238795325112867385, 1.000000000000000000, 0.9238795325112867385, 1.000000000000000000, 0.9238795325112867385, 1.000000000000000000, 0.9238795325112867385, 1.000000000000000000, 0.9238795325112867385, 1.000000000000000000, 0.9238795325112867385, 1.000000000000000000, 0.9238795325112867385, 1.000000000000000000, 0.9238795325112867385, 1.000000000000000000, 0.9238795325112867385, 1.000000000000000000, 0.9238795325112867385, 1.000000000000000000, 0.9238795325112867385, 1.000000000000000000, 0.9238795325112867385, 1.000000000000000000, 0.9238795325112867385, 1.000000000000000000, 0.9238795325112867385, 1.000000000000000000, 0.9238795325112867385, 1.000000000000000000, 0.9238795325112867385, 1.000000000000000000, 0.9238795325112867385, 1.000000000000000000, 0.9238795325112867385, 1.000000000000000000, 0.9238795325112867385, 1.000000000000000000, 0.9238795325112867385, 1.000000000000000000, 0.9238795325112867385, 1.000000000000000000, 0.9238795325112867385, 1.000000000000000000, 0.9238795325112867385, 1.000000000000000000, 0.9238795325112867385, 1.000000000000000000, 0.9238795325112867385, 1.000000000000000000, 0.9238795325112867385, 1.000000000000000000, 0.9238795325112867385, 1.000000000000000000, 0.9238795325112867385, 1.000000000000000000, 0.9238795325112867385, 1.000000000000000000, 0.9238795325112867385, 1.000000000000000000, 0.9238795325112867385, 1.000000000000000000, 0.9238795325112867385, 1.000000000000000000, 0.9238795325112867385, 1.000000000000000000, 0.9238795325112867385, 1.000000000000000000, 0.9238795325112867385, 1.000000000000000000, 0.9238795325112867385, 1.000000000000000000, 0.9238795325112867385, 1.000000000000000000, 0.9238795325112867385, 1.000000000000000000, 0.9238795325112867385, 1.000000000000000000, 0.9238795325112867385, 1.000000000000000000, 0.9238795325112867385, 1.000000000000000000, 0.9238795325112867385, 1.000000000000000000, 0.9238795325112867385, 1.000000000000000000, 0.9238795325112867385, 1.000000000000000000, 0.9238795325112867385, 1.000000000000000000, 0.9238795325112867385, 1.000000000000000000, 0.9238795325112867385, 1.000000000000000000, 0.9238795325112867385, 1.000000000000000000, 0.9238795325112867385, 1.000000000000000000, 0.9238795325112867385, 1.000000000000000000, 0.9238795325112867385, 1.000000000000000000, 0.9238795325112867385, 1.000000000000000000, 0.9238795325112867385, 1.000000000000000000, 0.9238795325112867385, 1.000000000000000000, 0.9238795325112867385, 1.000000000000000000, 0.9238795325112867385, 1.000000000000000000, 0.9238795325112867385, 1.000000000000000000, 0.9238795325112867385, 1.000000000000000000, 0.9238795325112867385, 1.000000000000000000, 0.9238795325112867385, 1.000000000000000000, 0.9238795325112867385, 1.000000000000000000, 0.9238795325112867385, 1.000000000000000000, 0.9238795325112867385, 1.000000000000000000, 0.9238795325112867385, 1.000000000000000000, 0.9238795325112867385, 1.000000000000000000, 0.9238795325112867385, 1.000000000000000000, 0.9238795325112867385, 1.000000000000000000, 0.9238795325112867385, 1.000000000000000000, 0.9238795325112867385, 1.000000000000000000, 0.9238795325112867385, 1.000000000000000000, 0.9238795325112867385, 1.000000000000000000, 0.9238795325112867385, 1.000000000000000000, 0.9238795325112867385, 1.000000000000000000, 0.9238795325112867385, 1.000000000000000000, 0.9238795325112867385, 1.000000000000000000, 0.9238795325112867385, 1.000000000000000000, 0.9238795325112867385, 1.000000000000000000, 0.9238795325112867385, 1.000000000000000000, 0.9238795325112867385, 1.000000000000000000, 0.9926343136094674113, 0.9866940870930933638),
 ( 1.000000000000000000, 0.9238795325112867385, 1.000000000000000000, 0.9238795325112867385, 1.000000000000000000, 0.9238795325112867385, 1.000000000000000000, 0.9238795325112867385, 1.000000000000000000, 0.9238795325112867385, 1.000000000000000000, 0.9238795325112867385, 1.000000000000000000, 0.9238795325112867385, 1.000000000000000000, 0.9238795325112867385, 1.000000000000000000, 0.9238795325112867385, 1.000000000000000000, 0.9238795325112867385, 1.000000000000000000, 0.9238795325112867385, 1.000000000000000000, 0.9238795325112867385, 1.000000000000000000, 0.9238795325112867385, 1.000000000000000000, 0.9238795325112867385, 1.000000000000000000, 0.9238795325112867385, 1.000000000000000000, 0.9238795325112867385, 1.000000000000000000, 0.9238795325112867385, 1.000000000000000000, 0.9238795325112867385, 1.000000000000000000, 0.9238795325112867385, 1.000000000000000000, 0.9238795325112867385, 1.000000000000000000, 0.9238795325112867385, 1.000000000000000000, 0.9238795325112867385, 1.000000000000000000, 0.9238795325112867385, 1.000000000000000000, 0.9238795325112867385, 1.000000000000000000, 0.9238795325112867385, 1.000000000000000000, 0.9238795325112867385, 1.000000000000000000, 0.9238795325112867385, 1.000000000000000000, 0.9238795325112867385, 1.000000000000000000, 0.9238795325112867385, 1.000000000000000000, 0.9238795325112867385, 1.000000000000000000, 0.9238795325112867385, 1.000000000000000000, 0.9238795325112867385, 1.000000000000000000, 0.9238795325112867385, 1.000000000000000000, 0.9238795325112867385, 1.000000000000000000, 0.9238795325112867385, 1.000000000000000000, 0.9238795325112867385, 1.000000000000000000, 0.9238795325112867385, 1.000000000000000000, 0.9238795325112867385, 1.000000000000000000, 0.9238795325112867385, 1.000000000000000000, 0.9238795325112867385, 1.000000000000000000, 0.9238795325112867385, 1.000000000000000000, 0.9238795325112867385, 1.000000000000000000, 0.9238795325112867385, 1.000000000000000000, 0.9238795325112867385, 1.000000000000000000, 0.9238795325112867385, 1.000000000000000000, 0.9238795325112867385, 1.000000000000000000, 0.9238795325112867385, 1.000000000000000000, 0.9238795325112867385, 1.000000000000000000, 0.9238795325112867385, 1.000000000000000000, 0.9238795325112867385, 1.000000000000000000, 0.9238795325112867385, 1.000000000000000000, 0.9238795325112867385, 1.000000000000000000, 0.9238795325112867385, 1.000000000000000000, 0.9238795325112867385, 1.000000000000000000, 0.9238795325112867385, 1.000000000000000000, 0.9238795325112867385, 1.000000000000000000, 0.9238795325112867385, 1.000000000000000000, 0.9238795325112867385, 1.000000000000000000, 0.9238795325112867385, 1.000000000000000000, 0.9238795325112867385, 1.000000000000000000, 0.9238795325112867385, 1.000000000000000000, 0.9238795325112867385, 1.000000000000000000, 0.9238795325112867385, 1.000000000000000000, 0.9238795325112867385, 1.000000000000000000, 0.9238795325112867385, 1.000000000000000000, 0.9238795325112867385, 1.000000000000000000, 0.9238795325112867385, 1.000000000000000000, 0.9238795325112867385, 1.000000000000000000, 0.9238795325112867385, 1.000000000000000000, 0.9238795325112867385, 1.000000000000000000, 0.9238795325112867385, 1.000000000000000000, 0.9238795325112867385, 1.000000000000000000, 0.9238795325112867385, 1.000000000000000000, 0.9238795325112867385, 1.000000000000000000, 0.9238795325112867385, 1.000000000000000000, 0.9238795325112867385, 1.000000000000000000, 0.9238795325112867385, 1.000000000000000000, 0.9238795325112867385, 1.000000000000000000, 0.9238795325112867385, 1.000000000000000000, 0.9238795325112867385, 1.000000000000000000, 0.9238795325112867385, 1.000000000000000000, 0.9238795325112867385, 1.000000000000000000, 0.9238795325112867385, 1.000000000000000000, 0.9238795325112867385, 1.000000000000000000, 0.9238795325112867385, 1.000000000000000000, 0.9238795325112867385, 1.000000000000000000, 0.9238795325112867385, 1.000000000000000000, 0.9238795325112867385, 1.000000000000000000, 0.9238795325112867385, 1.000000000000000000, 0.9238795325112867385, 1.000000000000000000, 0.9238795325112867385, 1.000000000000000000, 0.9238795325112867385, 1.000000000000000000, 0.9238795325112867385, 1.000000000000000000, 0.9238795325112867385, 1.000000000000000000, 0.9238795325112867385, 1.000000000000000000, 0.9238795325112867385, 1.000000000000000000, 0.9238795325112867385, 1.000000000000000000, 0.9238795325112867385, 1.000000000000000000, 0.9238795325112867385, 1.000000000000000000, 0.9238795325112867385, 1.000000000000000000, 0.9238795325112867385, 1.000000000000000000, 0.9238795325112867385, 1.000000000000000000, 0.9238795325112867385, 1.000000000000000000, 0.9238795325112867385, 1.000000000000000000, 0.9238795325112867385, 1.000000000000000000, 0.9238795325112867385, 1.000000000000000000, 0.9238795325112867385, 1.000000000000000000, 0.9238795325112867385, 1.000000000000000000, 0.9238795325112867385, 1.000000000000000000, 0.9238795325112867385, 1.000000000000000000, 0.9238795325112867385, 1.000000000000000000, 0.9238795325112867385, 1.000000000000000000, 0.9238795325112867385, 1.000000000000000000, 0.9238795325112867385, 1.000000000000000000, 0.9238795325112867385, 1.000000000000000000, 0.9238795325112867385, 1.000000000000000000, 0.9238795325112867385, 1.000000000000000000, 0.9238795325112867385, 1.000000000000000000, 0.9238795325112867385, 1.000000000000000000, 0.9238795325112867385, 1.000000000000000000, 0.9238795325112867385, 1.000000000000000000, 0.9238795325112867385, 1.000000000000000000, 0.9238795325112867385, 1.000000000000000000, 0.9238795325112867385, 1.000000000000000000, 0.9238795325112867385, 1.000000000000000000, 0.9238795325112867385, 1.000000000000000000, 0.9238795325112867385, 1.000000000000000000, 0.9238795325112867385, 1.000000000000000000, 0.9238795325112867385, 1.000000000000000000, 0.9238795325112867385, 1.000000000000000000, 0.9238795325112867385, 1.000000000000000000, 0.9238795325112867385, 1.000000000000000000, 0.9238795325112867385, 1.000000000000000000, 0.9238795325112867385, 1.000000000000000000, 0.9238795325112867385, 1.000000000000000000, 0.9238795325112867385, 1.000000000000000000, 0.9238795325112867385, 1.000000000000000000, 0.9238795325112867385, 1.000000000000000000, 0.9238795325112867385, 1.000000000000000000, 0.9238795325112867385, 1.000000000000000000, 0.9238795325112867385, 1.000000000000000000, 0.9238795325112867385, 1.000000000000000000, 0.9238795325112867385, 1.000000000000000000, 0.9238795325112867385, 1.000000000000000000, 0.9238795325112867385, 1.000000000000000000, 0.9238795325112867385, 1.000000000000000000, 0.9238795325112867385, 1.000000000000000000, 0.9238795325112867385, 1.000000000000000000, 0.9238795325112867385, 1.000000000000000000, 0.9238795325112867385, 1.000000000000000000, 0.9238795325112867385, 1.000000000000000000, 0.9926343136094674113, 0.9866940870930933638),
 ( 1.000000000000000000, 0.9238795325112867385, 1.000000000000000000, 0.9238795325112867385, 1.000000000000000000, 0.9238795325112867385, 1.000000000000000000, 0.9238795325112867385, 1.000000000000000000, 0.9238795325112867385, 1.000000000000000000, 0.9238795325112867385, 1.000000000000000000, 0.9238795325112867385, 1.000000000000000000, 0.9238795325112867385, 1.000000000000000000, 0.9238795325112867385, 1.000000000000000000, 0.9238795325112867385, 1.000000000000000000, 0.9238795325112867385, 1.000000000000000000, 0.9238795325112867385, 1.000000000000000000, 0.9238795325112867385, 1.000000000000000000, 0.9238795325112867385, 1.000000000000000000, 0.9238795325112867385, 1.000000000000000000, 0.9238795325112867385, 1.000000000000000000, 0.9238795325112867385, 1.000000000000000000, 0.9238795325112867385, 1.000000000000000000, 0.9238795325112867385, 1.000000000000000000, 0.9238795325112867385, 1.000000000000000000, 0.9238795325112867385, 1.000000000000000000, 0.9238795325112867385, 1.000000000000000000, 0.9238795325112867385, 1.000000000000000000, 0.9238795325112867385, 1.000000000000000000, 0.9238795325112867385, 1.000000000000000000, 0.9238795325112867385, 1.000000000000000000, 0.9238795325112867385, 1.000000000000000000, 0.9238795325112867385, 1.000000000000000000, 0.9238795325112867385, 1.000000000000000000, 0.9238795325112867385, 1.000000000000000000, 0.9238795325112867385, 1.000000000000000000, 0.9238795325112867385, 1.000000000000000000, 0.9238795325112867385, 1.000000000000000000, 0.9238795325112867385, 1.000000000000000000, 0.9238795325112867385, 1.000000000000000000, 0.9238795325112867385, 1.000000000000000000, 0.9238795325112867385, 1.000000000000000000, 0.9238795325112867385, 1.000000000000000000, 0.9238795325112867385, 1.000000000000000000, 0.9238795325112867385, 1.000000000000000000, 0.9238795325112867385, 1.000000000000000000, 0.9238795325112867385, 1.000000000000000000, 0.9238795325112867385, 1.000000000000000000, 0.9238795325112867385, 1.000000000000000000, 0.9238795325112867385, 1.000000000000000000, 0.9238795325112867385, 1.000000000000000000, 0.9238795325112867385, 1.000000000000000000, 0.9238795325112867385, 1.000000000000000000, 0.9238795325112867385, 1.000000000000000000, 0.9238795325112867385, 1.000000000000000000, 0.9238795325112867385, 1.000000000000000000, 0.9238795325112867385, 1.000000000000000000, 0.9238795325112867385, 1.000000000000000000, 0.9238795325112867385, 1.000000000000000000, 0.9238795325112867385, 1.000000000000000000, 0.9238795325112867385, 1.000000000000000000, 0.9238795325112867385, 1.000000000000000000, 0.9238795325112867385, 1.000000000000000000, 0.9238795325112867385, 1.000000000000000000, 0.9238795325112867385, 1.000000000000000000, 0.9238795325112867385, 1.000000000000000000, 0.9238795325112867385, 1.000000000000000000, 0.9238795325112867385, 1.000000000000000000, 0.9238795325112867385, 1.000000000000000000, 0.9238795325112867385, 1.000000000000000000, 0.9238795325112867385, 1.000000000000000000, 0.9238795325112867385, 1.000000000000000000, 0.9238795325112867385, 1.000000000000000000, 0.9238795325112867385, 1.000000000000000000, 0.9238795325112867385, 1.000000000000000000, 0.9238795325112867385, 1.000000000000000000, 0.9238795325112867385, 1.000000000000000000, 0.9238795325112867385, 1.000000000000000000, 0.9238795325112867385, 1.000000000000000000, 0.9238795325112867385, 1.000000000000000000, 0.9238795325112867385, 1.000000000000000000, 0.9238795325112867385, 1.000000000000000000, 0.9238795325112867385, 1.000000000000000000, 0.9238795325112867385, 1.000000000000000000, 0.9238795325112867385, 1.000000000000000000, 0.9238795325112867385, 1.000000000000000000, 0.9238795325112867385, 1.000000000000000000, 0.9238795325112867385, 1.000000000000000000, 0.9238795325112867385, 1.000000000000000000, 0.9238795325112867385, 1.000000000000000000, 0.9238795325112867385, 1.000000000000000000, 0.9238795325112867385, 1.000000000000000000, 0.9238795325112867385, 1.000000000000000000, 0.9238795325112867385, 1.000000000000000000, 0.9238795325112867385, 1.000000000000000000, 0.9238795325112867385, 1.000000000000000000, 0.9238795325112867385, 1.000000000000000000, 0.9238795325112867385, 1.000000000000000000, 0.9238795325112867385, 1.000000000000000000, 0.9238795325112867385, 1.000000000000000000, 0.9238795325112867385, 1.000000000000000000, 0.9238795325112867385, 1.000000000000000000, 0.9238795325112867385, 1.000000000000000000, 0.9238795325112867385, 1.000000000000000000, 0.9238795325112867385, 1.000000000000000000, 0.9238795325112867385, 1.000000000000000000, 0.9238795325112867385, 1.000000000000000000, 0.9238795325112867385, 1.000000000000000000, 0.9238795325112867385, 1.000000000000000000, 0.9238795325112867385, 1.000000000000000000, 0.9238795325112867385, 1.000000000000000000, 0.9238795325112867385, 1.000000000000000000, 0.9238795325112867385, 1.000000000000000000, 0.9238795325112867385, 1.000000000000000000, 0.9238795325112867385, 1.000000000000000000, 0.9238795325112867385, 1.000000000000000000, 0.9238795325112867385, 1.000000000000000000, 0.9238795325112867385, 1.000000000000000000, 0.9238795325112867385, 1.000000000000000000, 0.9238795325112867385, 1.000000000000000000, 0.9238795325112867385, 1.000000000000000000, 0.9238795325112867385, 1.000000000000000000, 0.9238795325112867385, 1.000000000000000000, 0.9238795325112867385, 1.000000000000000000, 0.9238795325112867385, 1.000000000000000000, 0.9238795325112867385, 1.000000000000000000, 0.9238795325112867385, 1.000000000000000000, 0.9238795325112867385, 1.000000000000000000, 0.9238795325112867385, 1.000000000000000000, 0.9238795325112867385, 1.000000000000000000, 0.9238795325112867385, 1.000000000000000000, 0.9238795325112867385, 1.000000000000000000, 0.9238795325112867385, 1.000000000000000000, 0.9238795325112867385, 1.000000000000000000, 0.9238795325112867385, 1.000000000000000000, 0.9238795325112867385, 1.000000000000000000, 0.9238795325112867385, 1.000000000000000000, 0.9238795325112867385, 1.000000000000000000, 0.9238795325112867385, 1.000000000000000000, 0.9238795325112867385, 1.000000000000000000, 0.9238795325112867385, 1.000000000000000000, 0.9238795325112867385, 1.000000000000000000, 0.9238795325112867385, 1.000000000000000000, 0.9238795325112867385, 1.000000000000000000, 0.9238795325112867385, 1.000000000000000000, 0.9238795325112867385, 1.000000000000000000, 0.9238795325112867385, 1.000000000000000000, 0.9238795325112867385, 1.000000000000000000, 0.9238795325112867385, 1.000000000000000000, 0.9238795325112867385, 1.000000000000000000, 0.9238795325112867385, 1.000000000000000000, 0.9238795325112867385, 1.000000000000000000, 0.9238795325112867385, 1.000000000000000000, 0.9238795325112867385, 1.000000000000000000, 0.9238795325112867385, 1.000000000000000000, 0.9238795325112867385, 1.000000000000000000, 0.9926343136094674113, 0.9866940870930933638) ) ) 
 REPRESENTATION_ITEM ( '' )  SURFACE ( )  );
#65486=CARTESIAN_POINT ( 'NONE',  ( -7.999999999999989342, -6.533544264681542033E-06, 23.51780296876433596 ) ) ;
#65515=APPLICATION_CONTEXT ( 'automotive_design' ) ;
#65519=CARTESIAN_POINT ( 'NONE',  ( 7.188101187499991163, 2.977408999572648707, 28.20530278187175455 ) ) ;
#65531=FACE_OUTER_BOUND ( 'NONE', #65532, .T. ) ;
#65532=EDGE_LOOP ( 'NONE', ( #10033, #33068, #50890, #58380 ) ) ;
#65544=CARTESIAN_POINT ( 'NONE',  ( 2.977408999572650927, -7.188101187499990274, 5.330302781871753659 ) ) ;
#65558=CARTESIAN_POINT ( 'NONE',  ( -3.313708498984757167, 7.999999999999991118, 26.23655278392014623 ) ) ;
#65559=DIRECTION ( 'NONE',  ( 1.000000000000000000, 0.000000000000000000, 0.000000000000000000 ) ) ;
#65567=CARTESIAN_POINT ( 'NONE',  ( 3.313708498984762496, -7.999999999999989342, 26.98655278392014623 ) ) ;
#65579=CARTESIAN_POINT ( 'NONE',  ( 5.082755093536318824, 5.082755093536319713, 20.42405278187175455 ) ) ;
#65582=ADVANCED_FACE ( 'NONE', ( #12795 ), #18100, .F. ) ;
#65588=CARTESIAN_POINT ( 'NONE',  ( -7.999999999999991118, 3.313708498984756723, 15.92405278392014623 ) ) ;
#65590=CARTESIAN_POINT ( 'NONE',  ( 7.999999999999991118, 9.797174393178815797E-16, 18.26780278392014623 ) ) ;
#65592=EDGE_CURVE ( 'NONE', #60307, #38243, #1138, .T. ) ;
#65601=CARTESIAN_POINT ( 'NONE',  ( -7.188101187499992051, 0.000000000000000000, 16.48655278187175810 ) ) ;
#65619=CARTESIAN_POINT ( 'NONE',  ( 7.999999999999992895, -3.313708498984756279, 24.17405278392015333 ) ) ;
#65625=CARTESIAN_POINT ( 'NONE',  ( -7.188101187499992051, 0.000000000000000000, 19.86155278187175455 ) ) ;
#65642=CARTESIAN_POINT ( 'NONE',  ( -7.999999999999989342, -3.313708498984762496, 17.42405277982336997 ) ) ;
#65656=CARTESIAN_POINT ( 'NONE',  ( 7.999999999999992895, -3.313708498984756279, 19.54280278432982954 ) ) ;
#65657=CARTESIAN_POINT ( 'NONE',  ( -8.000000000000010658, -3.313708498984740736, 15.92405277982336287 ) ) ;
#65686=CARTESIAN_POINT ( 'NONE',  ( 7.188101187499993827, -2.977408999572645598, 9.642802781871756324 ) ) ;
#65688=ORIENTED_EDGE ( 'NONE', *, *, #19188, .F. ) ;
#65709=CARTESIAN_POINT ( 'NONE',  ( 2.977408999572650927, -7.188101187499990274, 5.330302781871753659 ) ) ;
#65715=CARTESIAN_POINT ( 'NONE',  ( 7.999999999836578723, -5.113295603412193572E-05, 3.267801294049292871 ) ) ;
#65741=CARTESIAN_POINT ( 'NONE',  ( 5.656854249492376141, -5.656854249492374365, 6.080302783920147114 ) ) ;
#65758=CARTESIAN_POINT ( 'NONE',  ( 3.317071493978883456, -8.008118988124989457, 10.48186528394063188 ) ) ;
#65765=CARTESIAN_POINT ( 'NONE',  ( 5.082755093536320601, -5.082755093536318824, 2.049052781871754103 ) ) ;
#65771=ORIENTED_EDGE ( 'NONE', *, *, #8039, .F. ) ;
#65778=CARTESIAN_POINT ( 'NONE',  ( -5.082755093536319713, 5.082755093536319713, 23.79905278187175455 ) ) ;
#65783=CARTESIAN_POINT ( 'NONE',  ( -6.406773156053975349, 4.907047822329288600, -0.000000000000000000 ) ) ;
#65790=CARTESIAN_POINT ( 'NONE',  ( -6.373372650972353171, -4.860592676736378515, -0.000000000000000000 ) ) ;
#65797=CARTESIAN_POINT ( 'NONE',  ( -7.999999999999991118, 0.000000000000000000, 2.517802783920143561 ) ) ;
#65801=CARTESIAN_POINT ( 'NONE',  ( 7.188101187499992051, 2.977408999572647819, 20.70530278187175810 ) ) ;
#65819=CARTESIAN_POINT ( 'NONE',  ( 7.999999999999991118, 9.797174393178815797E-16, 13.58030277982336465 ) ) ;
#65824=CARTESIAN_POINT ( 'NONE',  ( -3.313708498984757611, 7.999999999999991118, 14.23655278392014623 ) ) ;
#65846=EDGE_LOOP ( 'NONE', ( #63278, #66375, #73954, #64029 ) ) ;
#65848=CARTESIAN_POINT ( 'NONE',  ( 1.471067592899761672E-15, -8.008118988124991233, 26.88811528394063188 ) ) ;
#65876=CARTESIAN_POINT ( 'NONE',  ( 5.082755093536320601, -5.082755093536318824, 9.924052781871754547 ) ) ;
#65883=CARTESIAN_POINT ( 'NONE',  ( 2.977408999572650927, -7.188101187499990274, 0.4553027818717525488 ) ) ;
#65909=CARTESIAN_POINT ( 'NONE',  ( 2.977408999572646486, 7.188101187499991163, 4.392802781871752771 ) ) ;
#65916=PLANE ( 'NONE',  #53095 ) ;
#65926=CARTESIAN_POINT ( 'NONE',  ( 7.999999999999992895, -3.313708498984756279, 19.67405278392014978 ) ) ;
#65952=CARTESIAN_POINT ( 'NONE',  ( -7.188101187499990274, -2.977408999572651815, 24.08030278187175099 ) ) ;
#65953=EDGE_LOOP ( 'NONE', ( #54266, #74448, #5785, #12979, #11301 ) ) ;
#65960=CARTESIAN_POINT ( 'NONE',  ( 7.999999999999991118, 9.797174393178815797E-16, 15.26780278392014623 ) ) ;
#65969=CARTESIAN_POINT ( 'NONE',  ( 0.000000000000000000, 0.000000000000000000, 0.000000000000000000 ) ) ;
#65970=CARTESIAN_POINT ( 'NONE',  ( -7.188101187499992051, 0.000000000000000000, 19.48655278187175455 ) ) ;
#65989=CARTESIAN_POINT ( 'NONE',  ( -5.656854249492375253, 5.656854249492375253, 23.33030278392014978 ) ) ;
#65996=CARTESIAN_POINT ( 'NONE',  ( -5.082755093536317936, -5.082755093536320601, 23.04905278187175455 ) ) ;
#66011=CARTESIAN_POINT ( 'NONE',  ( -3.313708498984758943, -7.999999999999989342, 11.61155277982336820 ) ) ;
#66028=CARTESIAN_POINT ( 'NONE',  ( -5.656854249492373476, -5.656854249492376141, 17.57405278432982243 ) ) ;
#66060=CARTESIAN_POINT ( 'NONE',  ( -7.188101187499992051, 0.000000000000000000, 4.486552781871752771 ) ) ;
#66072=CARTESIAN_POINT ( 'NONE',  ( 7.188101187499993827, -2.977408999572645598, 11.51780278187175810 ) ) ;
#66083=CARTESIAN_POINT ( 'NONE',  ( 5.082755093536318824, 5.082755093536319713, 2.799052781871750994 ) ) ;
#66091=EDGE_CURVE ( 'NONE', #30893, #3504, #70081, .T. ) ;
#66100=CARTESIAN_POINT ( 'NONE',  ( -7.999999999999989342, -3.313708498984762496, 26.42405277982336642 ) ) ;
#66113=CARTESIAN_POINT ( 'NONE',  ( 7.999999999999991118, 9.797174393178815797E-16, 7.767802783920144449 ) ) ;
#66132=CARTESIAN_POINT ( 'NONE',  ( -5.662595241051935346, 5.662595241051935346, 11.32561528394062833 ) ) ;
#66133=ORIENTED_EDGE ( 'NONE', *, *, #47876, .T. ) ;
#66139=CARTESIAN_POINT ( 'NONE',  ( -5.082755093536317936, -5.082755093536320601, 0.1740527818717522990 ) ) ;
#66152=CARTESIAN_POINT ( 'NONE',  ( -7.188101187499991163, 2.977408999572646930, 25.39280278187176165 ) ) ;
#66156=CARTESIAN_POINT ( 'NONE',  ( 1.060465953394919891, 7.999920465055806673, 0.000000000000000000 ) ) ;
#66160=AXIS2_PLACEMENT_3D ( 'NONE', #10092, #56124, #67435 ) ;
#66162=MANIFOLD_SOLID_BREP ( 'Thread1', #4523 ) ;
#66176=CARTESIAN_POINT ( 'NONE',  ( -5.082755093536317936, -5.082755093536320601, 21.54905278187175455 ) ) ;
#66178=CARTESIAN_POINT ( 'NONE',  ( 3.313708498984762496, -7.999999999999989342, 22.48655278392014623 ) ) ;
#66194=CARTESIAN_POINT ( 'NONE',  ( 1.469576158976822172E-15, -7.999999999999991118, 10.20530277982336465 ) ) ;
#66199=DIRECTION ( 'NONE',  ( -0.000000000000000000, -0.000000000000000000, 1.000000000000000000 ) ) ;
#66215=FACE_OUTER_BOUND ( 'NONE', #19080, .T. ) ;
#66224=CARTESIAN_POINT ( 'NONE',  ( -8.008118988124991233, 0.000000000000000000, 26.51311528394063188 ) ) ;
#66260=CARTESIAN_POINT ( 'NONE',  ( 1.320432766682872962E-15, -7.188101187499992051, 27.73655278187175455 ) ) ;
#66281=CARTESIAN_POINT ( 'NONE',  ( -7.999999999999991118, 0.000000000000000000, 11.33030277982336642 ) ) ;
#66284=CARTESIAN_POINT ( 'NONE',  ( -7.999999999999991118, 0.000000000000000000, 29.33030277982336642 ) ) ;
#66303=CARTESIAN_POINT ( 'NONE',  ( 3.313708498984762496, -7.999999999999989342, 20.98655278392014978 ) ) ;
#66325=CARTESIAN_POINT ( 'NONE',  ( -7.188101187499990274, -2.977408999572651815, 22.58030278187175455 ) ) ;
#66328=AXIS2_PLACEMENT_3D ( 'NONE', #15179, #38210, #61213 ) ;
#66334=CARTESIAN_POINT ( 'NONE',  ( 5.656854249492376141, -5.656854249492374365, 13.58030278392014623 ) ) ;
#66340=AXIS2_PLACEMENT_3D ( 'NONE', #19871, #31949, #48172 ) ;
#66346=CARTESIAN_POINT ( 'NONE',  ( -5.082755093536319713, 5.082755093536319713, 20.79905278187175455 ) ) ;
#66364=CARTESIAN_POINT ( 'NONE',  ( 3.313708498984756279, 7.999999999999991118, 24.54905278392014978 ) ) ;
#66371=CARTESIAN_POINT ( 'NONE',  ( -7.188101187499991163, 2.977408999572646930, 24.26780278187175455 ) ) ;
#66375=ORIENTED_EDGE ( 'NONE', *, *, #70622, .T. ) ;
#66386=CARTESIAN_POINT ( 'NONE',  ( -3.313708498984757167, 7.999999999999991118, 6.549052779823365533 ) ) ;
#66391=CIRCLE ( 'NONE', #64034, 6.000000000000015099 ) ;
#66403=CARTESIAN_POINT ( 'NONE',  ( 7.999999999999992895, -3.313708498984756279, 9.042802784329825982 ) ) ;
#66412=ORIENTED_EDGE ( 'NONE', *, *, #28114, .T. ) ;
#66428=CARTESIAN_POINT ( 'NONE',  ( -5.656854249492375253, 5.656854249492375253, 17.14280277982336287 ) ) ;
#66432=CARTESIAN_POINT ( 'NONE',  ( 7.188101187499993827, -2.977408999572645598, 6.642802781871754547 ) ) ;
#66437=VECTOR ( 'NONE', #36882, 1000.000000000000000 ) ;
#66447=CARTESIAN_POINT ( 'NONE',  ( -7.188101187499991163, 2.977408999572646930, 9.267802781871756324 ) ) ;
#66458=CARTESIAN_POINT ( 'NONE',  ( 2.977408999572650927, -7.188101187499990274, 3.830302781871751883 ) ) ;
#66460=DIRECTION ( 'NONE',  ( -0.000000000000000000, -0.000000000000000000, 1.000000000000000000 ) ) ;
#66475=CARTESIAN_POINT ( 'NONE',  ( 7.999999999999992895, -3.313708498984756279, 25.48655277982336642 ) ) ;
#66485=CARTESIAN_POINT ( 'NONE',  ( 5.656854249492374365, 5.656854249492375253, 27.32405278432982598 ) ) ;
#66506=CARTESIAN_POINT ( 'NONE',  ( 2.977408999572650927, -7.188101187499990274, 4.955302781871752771 ) ) ;
#66519=CARTESIAN_POINT ( 'NONE',  ( 7.188101187499993827, -2.977408999572645598, 23.14280278187176165 ) ) ;
#66524=CARTESIAN_POINT ( 'NONE',  ( 4.907047822332399001, 6.406773156051627893, -0.000000000000000000 ) ) ;
#66545=CARTESIAN_POINT ( 'NONE',  ( -2.977408999572647819, -7.188101187499990274, 23.14280278187175810 ) ) ;
#66547=CARTESIAN_POINT ( 'NONE',  ( -5.656854249492373476, -5.656854249492376141, 22.20530278392014623 ) ) ;
#66565=CARTESIAN_POINT ( 'NONE',  ( 3.313708498984756279, 7.999999999999991118, 9.361552779823366421 ) ) ;
#66598=CARTESIAN_POINT ( 'NONE',  ( -3.317071493978880348, -8.008118988124989457, 23.79436528394063188 ) ) ;
#66629=ADVANCED_FACE ( 'NONE', ( #50407 ), #25864, .T. ) ;
#66631=CARTESIAN_POINT ( 'NONE',  ( 7.188101187499993827, -2.977408999572645598, 2.142802781871750550 ) ) ;
#66650=ADVANCED_FACE ( 'NONE', ( #21357 ), #67392, .F. ) ;
#66658=CARTESIAN_POINT ( 'NONE',  ( -7.999999999999989342, -3.313708498984762496, 26.42405277982336642 ) ) ;
#66669=ORIENTED_EDGE ( 'NONE', *, *, #37181, .T. ) ;
#66677=CARTESIAN_POINT ( 'NONE',  ( 5.656854249492376141, -5.656854249492374365, 16.58030278392014978 ) ) ;
#66692=CARTESIAN_POINT ( 'NONE',  ( -7.999999999999991118, 9.797174393178815797E-16, 30.00000000000000000 ) ) ;
#66701=CARTESIAN_POINT ( 'NONE',  ( -5.082755093536319713, 5.082755093536319713, 16.29905278187175455 ) ) ;
#66702=CARTESIAN_POINT ( 'NONE',  ( -5.656854249492373476, -5.656854249492376141, 16.20530278392014978 ) ) ;
#66714=CARTESIAN_POINT ( 'NONE',  ( 7.999999999999992895, -3.313708498984756279, 6.174052783920146226 ) ) ;
#66716=ORIENTED_EDGE ( 'NONE', *, *, #37413, .T. ) ;
#66725=CARTESIAN_POINT ( 'NONE',  ( 7.188101187499993827, -2.977408999572645598, 21.64280278187176165 ) ) ;
#66737=DIRECTION ( 'NONE',  ( -0.000000000000000000, -0.000000000000000000, 1.000000000000000000 ) ) ;
#66742=CARTESIAN_POINT ( 'NONE',  ( -7.999999999999989342, -3.313708498984762496, 23.61155278392014978 ) ) ;
#66749=CARTESIAN_POINT ( 'NONE',  ( -7.188101187499992051, 0.000000000000000000, 18.36155278187175455 ) ) ;
#66758=CARTESIAN_POINT ( 'NONE',  ( -5.656854249492375253, 5.656854249492375253, 18.64280277982336642 ) ) ;
#66766=CARTESIAN_POINT ( 'NONE',  ( -7.999999999999991118, 3.313708498984756723, 11.23655277982336820 ) ) ;
#66767=DIRECTION ( 'NONE',  ( -0.000000000000000000, -0.000000000000000000, 1.000000000000000000 ) ) ;
#66771=ORIENTED_EDGE ( 'NONE', *, *, #18681, .T. ) ;
#66782=CARTESIAN_POINT ( 'NONE',  ( 5.656854249492376141, -5.656854249492374365, 10.44905278432982598 ) ) ;
#66811=ORIENTED_EDGE ( 'NONE', *, *, #38481, .T. ) ;
#66818=CARTESIAN_POINT ( 'NONE',  ( -5.082755093536317936, -5.082755093536320601, 4.674052781871752771 ) ) ;
#66819=EDGE_LOOP ( 'NONE', ( #19410, #19153, #39414, #29402 ) ) ;
#66830=CARTESIAN_POINT ( 'NONE',  ( -7.188101187499991163, 2.977408999572646930, 13.76780278187175455 ) ) ;
#66833=CARTESIAN_POINT ( 'NONE',  ( -3.313708498984759387, -7.999999999999989342, 5.611552779823364645 ) ) ;
#66843=CARTESIAN_POINT ( 'NONE',  ( 5.082755093536318824, 5.082755093536319713, 4.299052781871752771 ) ) ;
#66850=ORIENTED_EDGE ( 'NONE', *, *, #30125, .T. ) ;
#66855=CARTESIAN_POINT ( 'NONE',  ( -7.999999999999991118, 9.797174393178815797E-16, 30.00000000000000000 ) ) ;
#66857=CARTESIAN_POINT ( 'NONE',  ( 3.313708498984756279, 7.999999999999991118, 24.36155277982336997 ) ) ;
#66862=CARTESIAN_POINT ( 'NONE',  ( 7.999999999999991118, 0.000000000000000000, 30.00000000000000000 ) ) ;
#66868=CARTESIAN_POINT ( 'NONE',  ( -5.656854249492373476, -5.656854249492376141, -0.2946972160798554397 ) ) ;
#66893=CARTESIAN_POINT ( 'NONE',  ( -5.082755093536317936, -5.082755093536320601, 4.674052781871752771 ) ) ;
#66905=CARTESIAN_POINT ( 'NONE',  ( -2.977408999572647819, 7.188101187499991163, 25.20530278187175810 ) ) ;
#66910=CARTESIAN_POINT ( 'NONE',  ( -2.081694232949524270, 7.796785530330302194, 0.000000000000000000 ) ) ;
#66928=CARTESIAN_POINT ( 'NONE',  ( 0.000000000000000000, 0.000000000000000000, 29.33030277982336642 ) ) ;
#66929=CARTESIAN_POINT ( 'NONE',  ( -7.188101187499992051, 2.977408999572646930, 25.76780278187175810 ) ) ;
#66934=CARTESIAN_POINT ( 'NONE',  ( 7.999999999999991118, 9.797174393178815797E-16, 16.58030277982336287 ) ) ;
#66938=CARTESIAN_POINT ( 'NONE',  ( 7.999999999981424637, 1.723583929636134980E-05, 16.76780327155163874 ) ) ;
#66946=CARTESIAN_POINT ( 'NONE',  ( -4.898587196589407898E-16, 7.999999999999991118, 9.455302779823364645 ) ) ;
#66959=CARTESIAN_POINT ( 'NONE',  ( 3.313708498984756279, 7.999999999999991118, 20.04905278392014978 ) ) ;
#66974=CARTESIAN_POINT ( 'NONE',  ( -8.008118988124991233, 3.317071493978878127, 20.41936528394063544 ) ) ;
#66975=CARTESIAN_POINT ( 'NONE',  ( 5.656854249492374365, 5.656854249492375253, 22.95530278392014623 ) ) ;
#66989=CARTESIAN_POINT ( 'NONE',  ( -7.999999999999991118, 0.000000000000000000, 21.83030277982336997 ) ) ;
#67010=CARTESIAN_POINT ( 'NONE',  ( -7.188101187499990274, -2.977408999572651371, 25.95530278187175810 ) ) ;
#67012=FACE_OUTER_BOUND ( 'NONE', #2856, .T. ) ;
#67038=CARTESIAN_POINT ( 'NONE',  ( -4.898587196589407898E-16, 7.999999999999991118, 25.95530277982336997 ) ) ;
#67057=CARTESIAN_POINT ( 'NONE',  ( 3.313708498984756279, 7.999999999999991118, 21.54905278392014623 ) ) ;
#67060=CIRCLE ( 'NONE', #70765, 15.99999999999998579 ) ;
#67068=CARTESIAN_POINT ( 'NONE',  ( 5.656854249492376141, -5.656854249492374365, 28.39280277982336642 ) ) ;
#67073=CARTESIAN_POINT ( 'NONE',  ( -8.000000000053406168, 3.313708498931343893, 8.424052783922283183 ) ) ;
#67079=CARTESIAN_POINT ( 'NONE',  ( -4.401442555609577197E-16, 7.188101187499992051, 14.61155278187175455 ) ) ;
#67083=ORIENTED_EDGE ( 'NONE', *, *, #68544, .F. ) ;
#67092=CARTESIAN_POINT ( 'NONE',  ( 7.999999999999991118, 9.797174393178815797E-16, 9.267802783920146226 ) ) ;
#67103=CARTESIAN_POINT ( 'NONE',  ( -2.977408999572647819, 7.188101187499991163, 13.20530278187175277 ) ) ;
#67108=CARTESIAN_POINT ( 'NONE',  ( -7.999999999994639843, -6.164467849698474977E-06, 23.51803407853789807 ) ) ;
#67128=CARTESIAN_POINT ( 'NONE',  ( -2.977408999572647819, 7.188101187499991163, 16.58030278187175455 ) ) ;
#67143=CYLINDRICAL_SURFACE ( 'NONE', #5806, 7.999999999999991118 ) ;
#67146=CARTESIAN_POINT ( 'NONE',  ( 7.999999999999991118, 9.797174393178815797E-16, 10.58030277982336465 ) ) ;
#67163=CARTESIAN_POINT ( 'NONE',  ( 5.656854249492374365, 5.656854249492375253, 12.32405278432982421 ) ) ;
#67194=CARTESIAN_POINT ( 'NONE',  ( -4.401442555609577197E-16, 7.188101187499992051, 8.611552781871752771 ) ) ;
#67206=CARTESIAN_POINT ( 'NONE',  ( -2.977408999572648707, -7.188101187499990274, 9.642802781871756324 ) ) ;
#67221=CARTESIAN_POINT ( 'NONE',  ( -7.188101187499990274, -2.977408999572651815, 3.455302781871751883 ) ) ;
#67237=CARTESIAN_POINT ( 'NONE',  ( 5.656854249492374365, 5.656854249492375253, 25.76780277982336997 ) ) ;
#67251=CARTESIAN_POINT ( 'NONE',  ( -7.999999999999991118, 0.000000000000000000, 2.517802783920143561 ) ) ;
#67272=SPHERICAL_SURFACE ( 'NONE', #70075, 20.00000000000000355 ) ;
#67282=CARTESIAN_POINT ( 'NONE',  ( -7.188101187499990274, -2.977408999572651371, 22.58030278187175099 ) ) ;
#67301=CARTESIAN_POINT ( 'NONE',  ( -5.656854249492375253, 5.656854249492375253, 24.83030278392014978 ) ) ;
#67307=CARTESIAN_POINT ( 'NONE',  ( 5.082755093536320601, -5.082755093536318824, 21.92405278187175455 ) ) ;
#67326=CARTESIAN_POINT ( 'NONE',  ( 5.656854249492376141, -5.656854249492374365, 11.89280277982336642 ) ) ;
#67331=CARTESIAN_POINT ( 'NONE',  ( 7.999999999999304556, -3.314968910423997278E-06, 15.26780269013280034 ) ) ;
#67336=CARTESIAN_POINT ( 'NONE',  ( -7.999999999999991118, 0.000000000000000000, 10.01780278392014623 ) ) ;
#67352=CARTESIAN_POINT ( 'NONE',  ( 1.471067592899761672E-15, -8.008118988124991233, 17.88811528394063188 ) ) ;
#67353=CARTESIAN_POINT ( 'NONE',  ( -7.999999999999991118, 0.000000000000000000, 23.51780278392014978 ) ) ;
#67373=CARTESIAN_POINT ( 'NONE',  ( 5.656854249492374365, 5.656854249492375253, 13.76780277982336465 ) ) ;
#67380=CARTESIAN_POINT ( 'NONE',  ( 1.469576158976822172E-15, -7.999999999999991118, 2.705302779823365533 ) ) ;
#67385=CARTESIAN_POINT ( 'NONE',  ( -2.977408999572648707, -7.188101187499990274, 24.64280278187176165 ) ) ;
#67392=CYLINDRICAL_SURFACE ( 'NONE', #34329, 7.999999999999991118 ) ;
#67403=CARTESIAN_POINT ( 'NONE',  ( 7.999999999999991118, 1.469576158976822369E-15, 25.76780278392172008 ) ) ;
#67405=EDGE_CURVE ( 'NONE', #6758, #27289, #34369, .T. ) ;
#67413=CARTESIAN_POINT ( 'NONE',  ( -3.313708498984757167, 7.999999999999991118, 26.04905277982336997 ) ) ;
#67416=ORIENTED_EDGE ( 'NONE', *, *, #61338, .F. ) ;
#67433=CARTESIAN_POINT ( 'NONE',  ( -5.656854249492375253, 5.656854249492375253, 12.83030278392014623 ) ) ;
#67435=DIRECTION ( 'NONE',  ( 1.000000000000000000, 0.000000000000000000, 0.000000000000000000 ) ) ;
#67452=CARTESIAN_POINT ( 'NONE',  ( -2.977408999572647819, 7.188101187499992051, 14.70530278187175455 ) ) ;
#67477=CARTESIAN_POINT ( 'NONE',  ( -2.977408999572647819, 7.188101187499991163, 10.20530278187175455 ) ) ;
#67479=ORIENTED_EDGE ( 'NONE', *, *, #31951, .F. ) ;
#67488=CARTESIAN_POINT ( 'NONE',  ( -7.188101187499992051, 0.000000000000000000, 28.86155278187175810 ) ) ;
#67501=CARTESIAN_POINT ( 'NONE',  ( 7.188101187499992051, 8.802885111219154394E-16, 16.11155278187175455 ) ) ;
#67504=CARTESIAN_POINT ( 'NONE',  ( -5.656854249492373476, -5.656854249492376141, 1.205302783920146004 ) ) ;
#67517=CARTESIAN_POINT ( 'NONE',  ( 7.999999999999991118, 9.797174393178815797E-16, 7.580302779823366421 ) ) ;
#67531=CARTESIAN_POINT ( 'NONE',  ( 3.313708498984756279, 7.999999999999991118, 10.91780278432982776 ) ) ;
#67534=CYLINDRICAL_SURFACE ( 'NONE', #71885, 7.999999999999991118 ) ;
#67541=CARTESIAN_POINT ( 'NONE',  ( 0.000000000000000000, 145.8547997696495599, 50.08167581047971595 ) ) ;
#67565=CARTESIAN_POINT ( 'NONE',  ( 5.082755093536320601, -5.082755093536318824, 0.5490527818717526598 ) ) ;
#67570=CARTESIAN_POINT ( 'NONE',  ( 3.313708498984756279, 7.999999999999991118, 19.86155277982337353 ) ) ;
#67579=CARTESIAN_POINT ( 'NONE',  ( 2.977408999572650927, -7.188101187499990274, 5.330302781871753659 ) ) ;
#67609=CARTESIAN_POINT ( 'NONE',  ( -7.999999999999991118, -4.672035931492118266, 29.46248198892144643 ) ) ;
#67622=CARTESIAN_POINT ( 'NONE',  ( 7.999999999999991118, 9.797174393178815797E-16, 27.13655278432982598 ) ) ;
#67632=EDGE_CURVE ( 'NONE', #29130, #27473, #51688, .T. ) ;
#67655=CARTESIAN_POINT ( 'NONE',  ( -7.188101187499992051, 0.000000000000000000, 17.98655278187175455 ) ) ;
#67665=VECTOR ( 'NONE', #9330, 1000.000000000000000 ) ;
#67681=CARTESIAN_POINT ( 'NONE',  ( 7.188101187499992051, 8.802885111219154394E-16, 16.11155278187175455 ) ) ;
#67700=CARTESIAN_POINT ( 'NONE',  ( 3.313708498984762496, -7.999999999999989342, 8.799052779823364645 ) ) ;
#67716=CARTESIAN_POINT ( 'NONE',  ( 7.999999999999991118, 9.797174393178815797E-16, 4.580302779823363757 ) ) ;
#67727=CARTESIAN_POINT ( 'NONE',  ( 3.317071493978877683, 8.008118988124991233, 20.04436528394063188 ) ) ;
#67733=CARTESIAN_POINT ( 'NONE',  ( -7.999999999999991118, 0.000000000000000000, 29.33030277982336642 ) ) ;
#67745=EDGE_CURVE ( 'NONE', #49450, #47940, #44439, .T. ) ;
#67762=CARTESIAN_POINT ( 'NONE',  ( -2.977408999572648707, -7.188101187499990274, 21.64280278187176165 ) ) ;
#67787=CARTESIAN_POINT ( 'NONE',  ( -7.999999999999991118, 0.000000000000000000, 27.83030277982336642 ) ) ;
#67794=CARTESIAN_POINT ( 'NONE',  ( -5.656854249492373476, -5.656854249492376141, 14.51780277982336465 ) ) ;
#67802=CARTESIAN_POINT ( 'NONE',  ( 5.656854249492376141, -5.656854249492374365, 11.89280277982336642 ) ) ;
#67805=CARTESIAN_POINT ( 'NONE',  ( -5.656854249492375253, 5.656854249492375253, 14.33030278392014800 ) ) ;
#67823=CARTESIAN_POINT ( 'NONE',  ( -7.188101187499990274, -2.977408999572651815, 16.58030278187175455 ) ) ;
#67845=CARTESIAN_POINT ( 'NONE',  ( -7.188101187499991163, 2.977408999572646930, 14.89280278187175455 ) ) ;
#67868=CARTESIAN_POINT ( 'NONE',  ( -5.082755093536319713, 5.082755093536319713, 18.17405278187175455 ) ) ;
#67885=CARTESIAN_POINT ( 'NONE',  ( 7.999999999999991118, 3.313708498984757611, 3.174052779823361981 ) ) ;
#67902=CARTESIAN_POINT ( 'NONE',  ( 7.999999999999991118, 3.313708498984757611, 12.23030278432982243 ) ) ;
#67934=CARTESIAN_POINT ( 'NONE',  ( -7.188101187499990274, -2.977408999572651371, 3.080302781871750994 ) ) ;
#67947=CARTESIAN_POINT ( 'NONE',  ( 1.320432766682872962E-15, -7.188101187499992051, 3.736552781871751883 ) ) ;
#67975=CARTESIAN_POINT ( 'NONE',  ( -3.313708498984758943, -7.999999999999989342, 19.11155277982336997 ) ) ;
#67986=CARTESIAN_POINT ( 'NONE',  ( 5.656854249492374365, 5.656854249492375253, 1.955302783920143117 ) ) ;
#67991=ORIENTED_EDGE ( 'NONE', *, *, #39191, .F. ) ;
#67994=CARTESIAN_POINT ( 'NONE',  ( 7.999999999999991118, 9.797174393178815797E-16, 24.08030277982336642 ) ) ;
#68022=CARTESIAN_POINT ( 'NONE',  ( 5.082755093536320601, -5.082755093536318824, 21.54905278187175455 ) ) ;
#68028=CARTESIAN_POINT ( 'NONE',  ( 3.459103461385761413, -7.213501455148458419, -0.0001169852011744028255 ) ) ;
#68040=CARTESIAN_POINT ( 'NONE',  ( 5.656854249492374365, 5.656854249492375253, 7.767802779823362869 ) ) ;
#68049=CARTESIAN_POINT ( 'NONE',  ( 7.188101187499992051, 8.802885111219154394E-16, 19.11155278187175455 ) ) ;
#68059=CARTESIAN_POINT ( 'NONE',  ( -7.999999999970034636, -1.442163225726577833E-05, 17.51834960462420909 ) ) ;
#68067=CARTESIAN_POINT ( 'NONE',  ( -7.999999999999991118, 0.000000000000000000, 20.33030277982336642 ) ) ;
#68068=CARTESIAN_POINT ( 'NONE',  ( 1.469576158976822172E-15, -7.999999999999991118, 4.205302779823362869 ) ) ;
#68073=CARTESIAN_POINT ( 'NONE',  ( -5.656854249492373476, -5.656854249492376141, 14.70530278392014800 ) ) ;
#68098=CARTESIAN_POINT ( 'NONE',  ( 5.662595241051934458, 5.662595241051935346, 19.95061528394062833 ) ) ;
#68123=CARTESIAN_POINT ( 'NONE',  ( 5.656854249492376141, -5.656854249492374365, 2.892802779823365533 ) ) ;
#68125=CARTESIAN_POINT ( 'NONE',  ( -7.999999999999992895, 4.898587196589407898E-16, 0.000000000000000000 ) ) ;
#68128=CARTESIAN_POINT ( 'NONE',  ( 7.188101187499992051, 8.802885111219154394E-16, 23.61155278187175455 ) ) ;
#68152=CARTESIAN_POINT ( 'NONE',  ( 3.313708498984756279, 7.999999999999991118, 18.36155277982337353 ) ) ;
#68170=CARTESIAN_POINT ( 'NONE',  ( -7.999999999999991118, 0.000000000000000000, 14.51780278392014800 ) ) ;
#68216=VECTOR ( 'NONE', #30652, 1000.000000000000000 ) ;
#68217=CARTESIAN_POINT ( 'NONE',  ( 2.977408999572650927, -7.188101187499990274, 12.45530278187175277 ) ) ;
#68244=CARTESIAN_POINT ( 'NONE',  ( 1.320432766682872962E-15, -7.188101187499992051, 9.736552781871754547 ) ) ;
#68258=CARTESIAN_POINT ( 'NONE',  ( 7.999999999999991118, 9.797174393178815797E-16, 6.080302779823364645 ) ) ;
#68259=CARTESIAN_POINT ( 'NONE',  ( 3.313708498984762496, -7.999999999999989342, 4.486552783920144449 ) ) ;
#68271=CARTESIAN_POINT ( 'NONE',  ( 7.999999999999991118, -2.975320552349488356E-08, 19.76780278304987348 ) ) ;
#68274=CARTESIAN_POINT ( 'NONE',  ( -3.313708498984757167, 7.999999999999991118, 5.105302784329824206 ) ) ;
#68283=DIRECTION ( 'NONE',  ( -0.000000000000000000, -0.000000000000000000, 1.000000000000000000 ) ) ;
#68285=ORIENTED_EDGE ( 'NONE', *, *, #37413, .F. ) ;
#68302=FACE_OUTER_BOUND ( 'NONE', #57219, .T. ) ;
#68317=CARTESIAN_POINT ( 'NONE',  ( 7.188101187499993827, -2.977408999572645598, 4.017802781871751883 ) ) ;
#68330=CARTESIAN_POINT ( 'NONE',  ( 5.082755093536320601, -5.082755093536318824, 0.9240527818717529929 ) ) ;
#68338=ADVANCED_FACE ( 'NONE', ( #6967 ), #36378, .F. ) ;
#68346=CARTESIAN_POINT ( 'NONE',  ( -4.898587196589407898E-16, 7.999999999999991118, 22.95530277982336642 ) ) ;
#68349=VECTOR ( 'NONE', #23022, 1000.000000000000000 ) ;
#68360=CARTESIAN_POINT ( 'NONE',  ( 5.656854249492374365, 5.656854249492375253, 21.32405278432982243 ) ) ;
#68366=CARTESIAN_POINT ( 'NONE',  ( -3.313708498984757611, 7.999999999999991118, 24.54905277982336287 ) ) ;
#68372=ORIENTED_EDGE ( 'NONE', *, *, #22674, .T. ) ;
#68378=CARTESIAN_POINT ( 'NONE',  ( -5.272365137108047328, -4.893145049964592097, 0.1656095422372733383 ) ) ;
#68390=CARTESIAN_POINT ( 'NONE',  ( 2.977408999572646486, 7.188101187499991163, 16.01780278187175455 ) ) ;
#68411=CARTESIAN_POINT ( 'NONE',  ( -4.401442555609577197E-16, 7.188101187499992051, 19.48655278187175455 ) ) ;
#68430=CARTESIAN_POINT ( 'NONE',  ( -3.313708498984758943, -7.999999999999989342, 4.111552779823362869 ) ) ;
#68461=CARTESIAN_POINT ( 'NONE',  ( 8.008118988124991233, 3.317071493978879015, 21.35686528394063544 ) ) ;
#68472=DIRECTION ( 'NONE',  ( 1.000000000000000000, 0.000000000000000000, 0.000000000000000000 ) ) ;
#68479=CARTESIAN_POINT ( 'NONE',  ( 7.999999999999991118, 3.313708498984757611, 6.361552783920146226 ) ) ;
#68495=CARTESIAN_POINT ( 'NONE',  ( 2.977408999572650927, -7.188101187499990274, 26.33030278187175810 ) ) ;
#68521=CARTESIAN_POINT ( 'NONE',  ( -7.999999999999989342, -3.313708498984762496, 23.42405277982336642 ) ) ;
#68531=EDGE_LOOP ( 'NONE', ( #44283, #19127 ) ) ;
#68539=CARTESIAN_POINT ( 'NONE',  ( -7.999999999999989342, -3.313708498984762496, 11.61155278392014445 ) ) ;
#68544=EDGE_CURVE ( 'NONE', #21048, #8103, #38253, .T. ) ;
#68555=CARTESIAN_POINT ( 'NONE',  ( -7.999999999971585396, 1.424435121157765920E-05, 7.017269882810325932 ) ) ;
#68574=ORIENTED_EDGE ( 'NONE', *, *, #72166, .T. ) ;
#68589=CARTESIAN_POINT ( 'NONE',  ( 1.320432766682872962E-15, -7.188101187499992051, 12.36155278187175277 ) ) ;
#68614=CARTESIAN_POINT ( 'NONE',  ( -2.977408999572647819, 7.188101187499991163, 10.58030278187175455 ) ) ;
#68617=CARTESIAN_POINT ( 'NONE',  ( -3.313708498984758943, -7.999999999999989342, -0.3321972156701773482 ) ) ;
#68628=CARTESIAN_POINT ( 'NONE',  ( 3.313708498984756279, 7.999999999999991118, 3.361552779823362425 ) ) ;
#68645=CARTESIAN_POINT ( 'NONE',  ( -7.999999999999991118, 0.000000000000000000, 8.386552784329824206 ) ) ;
#68651=CARTESIAN_POINT ( 'NONE',  ( -7.188101187499992051, 2.977408999572646930, 25.39280278187176165 ) ) ;
#68673=CARTESIAN_POINT ( 'NONE',  ( -7.188101187499991163, 2.977408999572646930, 28.39280278187175810 ) ) ;
#68686=CARTESIAN_POINT ( 'NONE',  ( -2.977408999572647819, 7.188101187499991163, 3.080302781871750994 ) ) ;
#68696=CARTESIAN_POINT ( 'NONE',  ( 5.082755093536318824, 5.082755093536319713, 28.29905278187175810 ) ) ;
#68704=CARTESIAN_POINT ( 'NONE',  ( 7.999999999999998224, 3.313708498984749617, 28.67405277982336642 ) ) ;
#68714=CARTESIAN_POINT ( 'NONE',  ( 7.999999999999991118, 3.313708498984757611, 19.67405277982336642 ) ) ;
#68726=CARTESIAN_POINT ( 'NONE',  ( -7.999999999999989342, -3.313708498984762496, 21.98030278432982598 ) ) ;
#68761=CARTESIAN_POINT ( 'NONE',  ( -2.977408999572648707, -7.188101187499990274, 18.26780278187175455 ) ) ;
#68784=( BOUNDED_CURVE ( )  B_SPLINE_CURVE ( 2, ( #13021, #41711, #7385, #36794, #25079, #8483, #36059, #54896, #31503 ),
 .UNSPECIFIED., .F., .F. ) 
 B_SPLINE_CURVE_WITH_KNOTS ( ( 3, 2, 2, 2, 3 ),
 ( 0.3441504249343935173, 0.3507686059762091801, 0.3573868815606666138, 0.3640051571451240475, 0.3706233993366209178 ),
 .UNSPECIFIED. ) 
 CURVE ( )  GEOMETRIC_REPRESENTATION_ITEM ( )  RATIONAL_B_SPLINE_CURVE ( ( 0.9999978252560842718, 0.9238806198987780105, 1.000000000000000000, 0.9238795325112867385, 1.000000000000000000, 0.9238795325112867385, 1.000000000000000000, 0.9238799165822936255, 0.9999992318618620146 ) ) 
 REPRESENTATION_ITEM ( '' )  );
#68785=CARTESIAN_POINT ( 'NONE',  ( 7.188101187499992051, 2.977408999572647819, 16.20530278187175099 ) ) ;
#68804=CARTESIAN_POINT ( 'NONE',  ( -7.999999999999991118, 0.000000000000000000, 5.330302779823363757 ) ) ;
#68831=CARTESIAN_POINT ( 'NONE',  ( -8.008118988124991233, 0.000000000000000000, 13.01311528394063011 ) ) ;
#68854=CARTESIAN_POINT ( 'NONE',  ( 3.313708498984756279, 7.999999999999991118, 5.049052783920146226 ) ) ;
#68868=CARTESIAN_POINT ( 'NONE',  ( 7.188101187499992051, 8.802885111219154394E-16, 19.11155278187175455 ) ) ;
#68872=FACE_OUTER_BOUND ( 'NONE', #73995, .T. ) ;
#68887=CARTESIAN_POINT ( 'NONE',  ( 0.5297946994982605240, -7.985892691108496422, 0.000000000000000000 ) ) ;
#68895=CARTESIAN_POINT ( 'NONE',  ( -7.999999999999991118, 0.000000000000000000, 21.83030277982336997 ) ) ;
#68913=CARTESIAN_POINT ( 'NONE',  ( -7.999999999999989342, -3.313708498984762496, 10.11155278392014623 ) ) ;
#68926=CYLINDRICAL_SURFACE ( 'NONE', #6724, 7.999999999999991118 ) ;
#68965=CARTESIAN_POINT ( 'NONE',  ( 5.082755093536318824, 5.082755093536319713, 5.424052781871753659 ) ) ;
#68989=CARTESIAN_POINT ( 'NONE',  ( -5.082755093536319713, 5.082755093536319713, 10.67405278187175455 ) ) ;
#69003=CARTESIAN_POINT ( 'NONE',  ( 5.656854249492376141, -5.656854249492374365, 2.892802779823365533 ) ) ;
#69021=CARTESIAN_POINT ( 'NONE',  ( 5.656854249492374365, 5.656854249492375253, 7.824052784329823318 ) ) ;
#69029=CARTESIAN_POINT ( 'NONE',  ( 5.082755093536318824, 5.082755093536319713, 24.92405278187175810 ) ) ;
#69033=ORIENTED_EDGE ( 'NONE', *, *, #13304, .F. ) ;
#69043=CARTESIAN_POINT ( 'NONE',  ( -7.999999999999989342, -3.313708498984762496, 20.61155278392014623 ) ) ;
#69052=CARTESIAN_POINT ( 'NONE',  ( -2.977408999572647819, 7.188101187499991163, 22.20530278187175455 ) ) ;
#69065=CARTESIAN_POINT ( 'NONE',  ( -5.082755093536317936, -5.082755093536320601, 8.049052781871752771 ) ) ;
#69069=CARTESIAN_POINT ( 'NONE',  ( -8.008118988124991233, 3.317071493978878127, 5.419365283940630107 ) ) ;
#69075=CARTESIAN_POINT ( 'NONE',  ( 7.188101187499993827, -2.977408999572645598, 26.51780278187175455 ) ) ;
#69092=CARTESIAN_POINT ( 'NONE',  ( -7.999999999999989342, -3.313708498984762496, 23.42405277982336642 ) ) ;
#69106=CARTESIAN_POINT ( 'NONE',  ( -3.313708498984758943, -7.999999999999989342, 22.16780278432982598 ) ) ;
#69119=ORIENTED_EDGE ( 'NONE', *, *, #47876, .F. ) ;
#69127=( BOUNDED_CURVE ( )  B_SPLINE_CURVE ( 2, ( #50325, #37905, #60903, #55636, #49204, #33744, #9608 ),
 .UNSPECIFIED., .F., .F. ) 
 B_SPLINE_CURVE_WITH_KNOTS ( ( 3, 2, 2, 3 ),
 ( 0.9889792491610456260, 0.9927413376685174651, 0.9993596132529668497, 1.000000000000000000 ),
 .UNSPECIFIED. ) 
 CURVE ( )  GEOMETRIC_REPRESENTATION_ITEM ( )  RATIONAL_B_SPLINE_CURVE ( ( 0.9626528551087341068, 0.9567301282231954751, 1.000000000000000000, 0.9238795325112867385, 1.000000000000000000, 0.9926345559450140410, 0.9866944779687418787 ) ) 
 REPRESENTATION_ITEM ( '' )  );
#69139=CARTESIAN_POINT ( 'NONE',  ( 1.320432766682872962E-15, -7.188101187499992051, 18.36155278187175455 ) ) ;
#69156=CARTESIAN_POINT ( 'NONE',  ( -7.999999999994261479, 6.398094505892175214E-06, 25.01756343669228499 ) ) ;
#69161=CARTESIAN_POINT ( 'NONE',  ( 2.977408999572650927, -7.188101187499990274, 15.83030278187175277 ) ) ;
#69182=CARTESIAN_POINT ( 'NONE',  ( -4.898587196589407898E-16, 7.999999999999991118, 3.455302779823362425 ) ) ;
#69208=CARTESIAN_POINT ( 'NONE',  ( 8.008118988124991233, 3.317071493978879015, 15.35686528394063188 ) ) ;
#69212=EDGE_CURVE ( 'NONE', #27089, #73165, #48706, .T. ) ;
#69215=CARTESIAN_POINT ( 'NONE',  ( -7.188101187499992051, 0.000000000000000000, 14.98655278187175455 ) ) ;
#69230=CARTESIAN_POINT ( 'NONE',  ( -4.898587196589407898E-16, 7.999999999999991118, 6.642802783920143561 ) ) ;
#69233=( BOUNDED_CURVE ( )  B_SPLINE_CURVE ( 2, ( #21223, #38958, #61961, #72543, #44249, #44990, #14666, #13180, #72012, #37328, #7545 ),
 .UNSPECIFIED., .F., .F. ) 
 B_SPLINE_CURVE_WITH_KNOTS ( ( 3, 2, 2, 2, 2, 3 ),
 ( 0.9530316461170064146, 0.9530316841617808565, 0.9596499597462393449, 0.9662682353306976113, 0.9728865109151558777, 0.9795047134926050392 ),
 .UNSPECIFIED. ) 
 CURVE ( )  GEOMETRIC_REPRESENTATION_ITEM ( )  RATIONAL_B_SPLINE_CURVE ( ( 0.9999991248568196323, 0.9999995624258944948, 1.000000000000000000, 0.9238795325112867385, 1.000000000000000000, 0.9238795325112867385, 1.000000000000000000, 0.9238795325112867385, 1.000000000000000000, 0.9238803722054950152, 0.9999983206301090721 ) ) 
 REPRESENTATION_ITEM ( '' )  );
#69245=CARTESIAN_POINT ( 'NONE',  ( 7.188101187499993827, -2.977408999572645598, 16.01780278187175455 ) ) ;
#69256=CARTESIAN_POINT ( 'NONE',  ( -7.999999999999991118, 0.000000000000000000, 28.01780278392014978 ) ) ;
#69264=CARTESIAN_POINT ( 'NONE',  ( -5.461505570201114601, -5.862018349920268712, -0.000000000000000000 ) ) ;
#69270=CARTESIAN_POINT ( 'NONE',  ( 3.313708498984756279, 7.999999999999991118, 22.86155277982337353 ) ) ;
#69289=CARTESIAN_POINT ( 'NONE',  ( -5.656854249492373476, -5.656854249492376141, 5.705302783920146226 ) ) ;
#69336=CARTESIAN_POINT ( 'NONE',  ( 5.082755093536320601, -5.082755093536318824, 9.549052781871754547 ) ) ;
#69362=CARTESIAN_POINT ( 'NONE',  ( -7.188101187499992051, 0.000000000000000000, 9.361552781871752771 ) ) ;
#69365=CARTESIAN_POINT ( 'NONE',  ( -7.999999999999991118, 3.313708498984756723, 0.7928027843298236510 ) ) ;
#69375=CARTESIAN_POINT ( 'NONE',  ( 3.313708498984762496, -7.999999999999989342, 1.299052779823363979 ) ) ;
#69380=CARTESIAN_POINT ( 'NONE',  ( 0.000000000000000000, 0.000000000000000000, 11.00000000000000000 ) ) ;
#69388=CARTESIAN_POINT ( 'NONE',  ( -6.062687379811042554, -5.219768740853823807, 2.519839246067225784E-12 ) ) ;
#69391=CARTESIAN_POINT ( 'NONE',  ( -5.656854249492375253, 5.656854249492375253, 6.699052784329822430 ) ) ;
#69400=CARTESIAN_POINT ( 'NONE',  ( -7.188101187499992051, 0.000000000000000000, 26.98655278187175455 ) ) ;
#69403=EDGE_LOOP ( 'NONE', ( #22033, #1722, #36707 ) ) ;
#69412=CARTESIAN_POINT ( 'NONE',  ( 7.999999999999992895, -3.313708498984756279, 19.67405278392014978 ) ) ;
#69420=CARTESIAN_POINT ( 'NONE',  ( 7.188101187499991163, 2.977408999572648707, 23.33030278187175455 ) ) ;
#69433=CARTESIAN_POINT ( 'NONE',  ( -2.977408999572648707, -7.188101187499990274, 2.142802781871754103 ) ) ;
#69438=CARTESIAN_POINT ( 'NONE',  ( -8.008118988124991233, 3.317071493978878127, 2.419365283940627442 ) ) ;
#69445=CARTESIAN_POINT ( 'NONE',  ( 2.977408999572646486, 7.188101187499991163, 26.89280278187175455 ) ) ;
#69465=CARTESIAN_POINT ( 'NONE',  ( 3.313708498984762496, -7.999999999999989342, 23.79905277982336642 ) ) ;
#69479=CARTESIAN_POINT ( 'NONE',  ( -7.999999999999991118, 0.000000000000000000, 23.38655278432982598 ) ) ;
#69512=CARTESIAN_POINT ( 'NONE',  ( -5.082755093536317936, -5.082755093536320601, 10.67405278187175455 ) ) ;
#69536=CARTESIAN_POINT ( 'NONE',  ( 7.188101187499992051, 2.977408999572647819, 10.20530278187175455 ) ) ;
#69540=CARTESIAN_POINT ( 'NONE',  ( -7.999999999999991118, 0.000000000000000000, 20.33030277982336642 ) ) ;
#69560=CARTESIAN_POINT ( 'NONE',  ( 5.656854249492374365, 5.656854249492375253, 10.76780277982336642 ) ) ;
#69584=CARTESIAN_POINT ( 'NONE',  ( 8.008118988124993010, -3.317071493978877239, 13.66936528394063011 ) ) ;
#69590=CARTESIAN_POINT ( 'NONE',  ( -5.082755093536317936, -5.082755093536320601, 6.174052781871754547 ) ) ;
#69603=CARTESIAN_POINT ( 'NONE',  ( 7.999999999999991118, 3.313708498984757611, 3.361552783920145338 ) ) ;
#69617=VERTEX_POINT ( 'NONE', #67488 ) ;
#69619=CARTESIAN_POINT ( 'NONE',  ( -7.188101187499990274, -2.977408999572651371, 18.45530278187175455 ) ) ;
#69621=CARTESIAN_POINT ( 'NONE',  ( -4.898587196589407898E-16, 7.999999999999991118, 3.455302779823362425 ) ) ;
#69632=DIRECTION ( 'NONE',  ( -0.000000000000000000, -0.000000000000000000, 1.000000000000000000 ) ) ;
#69634=ORIENTED_EDGE ( 'NONE', *, *, #8039, .T. ) ;
#69643=CARTESIAN_POINT ( 'NONE',  ( 7.999999999999992895, -3.313708498984756279, 19.48655277982336642 ) ) ;
#69649=LINE ( 'NONE', #17962, #54257 ) ;
#69661=CARTESIAN_POINT ( 'NONE',  ( -5.656854249492375253, 5.656854249492375253, 9.830302783920146226 ) ) ;
#69675=DIRECTION ( 'NONE',  ( -0.000000000000000000, -0.000000000000000000, 1.000000000000000000 ) ) ;
#69712=CARTESIAN_POINT ( 'NONE',  ( 2.977408999572650927, -7.188101187499990274, 9.455302781871754547 ) ) ;
#69735=CARTESIAN_POINT ( 'NONE',  ( -2.977408999572648707, -7.188101187499990274, 9.642802781871756324 ) ) ;
#69740=CARTESIAN_POINT ( 'NONE',  ( 1.469576158976822172E-15, -7.999999999999991118, 7.392802783920144449 ) ) ;
#69749=CARTESIAN_POINT ( 'NONE',  ( 1.469576158976822172E-15, -7.999999999999991118, 25.39280278392014978 ) ) ;
#69780=CARTESIAN_POINT ( 'NONE',  ( -7.999999999999991118, 3.313708498984756723, 20.42405278392014978 ) ) ;
#69792=CARTESIAN_POINT ( 'NONE',  ( -7.188101187499990274, -2.977408999572651371, 22.58030278187175099 ) ) ;
#69805=CARTESIAN_POINT ( 'NONE',  ( 7.188101187499993827, -2.977408999572645598, 2.517802781871750550 ) ) ;
#69810=CARTESIAN_POINT ( 'NONE',  ( -8.008118988124991233, 0.000000000000000000, 4.013115283940629219 ) ) ;
#69817=CARTESIAN_POINT ( 'NONE',  ( 7.188101187499992051, 8.802885111219154394E-16, 28.11155278187175455 ) ) ;
#69824=FACE_OUTER_BOUND ( 'NONE', #871, .T. ) ;
#69836=CARTESIAN_POINT ( 'NONE',  ( -5.656854249492373476, -5.656854249492376141, 14.51780277982336465 ) ) ;
#69853=CARTESIAN_POINT ( 'NONE',  ( -5.656854249492373476, -5.656854249492376141, 25.07405278432982598 ) ) ;
#69881=( NAMED_UNIT ( * ) PLANE_ANGLE_UNIT ( ) SI_UNIT ( $, .RADIAN. ) );
#69886=CARTESIAN_POINT ( 'NONE',  ( 7.188101187499991163, 2.977408999572648707, 11.33030278187175632 ) ) ;
#69911=ADVANCED_FACE ( 'NONE', ( #62189 ), #43534, .F. ) ;
#69912=CARTESIAN_POINT ( 'NONE',  ( 1.320432766682872962E-15, -7.188101187499992051, 9.736552781871754547 ) ) ;
#69957=CARTESIAN_POINT ( 'NONE',  ( 3.317071493978883456, -8.008118988124989457, 14.98186528394062833 ) ) ;
#69965=CARTESIAN_POINT ( 'NONE',  ( 5.082755093536318824, 5.082755093536319713, 11.42405278187175455 ) ) ;
#69979=CARTESIAN_POINT ( 'NONE',  ( 1.469576158976822172E-15, -7.999999999999991118, 1.392802783920146004 ) ) ;
#69995=CARTESIAN_POINT ( 'NONE',  ( -7.188101187499991163, 2.977408999572646930, 18.26780278187175455 ) ) ;
#70003=CARTESIAN_POINT ( 'NONE',  ( 5.082755093536320601, -5.082755093536318824, 26.42405278187175810 ) ) ;
#70008=CARTESIAN_POINT ( 'NONE',  ( -3.313708498984757611, 7.999999999999991118, 26.04905277982337353 ) ) ;
#70014=CARTESIAN_POINT ( 'NONE',  ( -2.479188868019259750, -7.619273332548305078, 0.000000000000000000 ) ) ;
#70022=CARTESIAN_POINT ( 'NONE',  ( 1.469576158976822172E-15, -7.999999999999991118, 13.20530277982336465 ) ) ;
#70038=CARTESIAN_POINT ( 'NONE',  ( 5.656854249492374365, 5.656854249492375253, 6.455302783920143561 ) ) ;
#70052=CARTESIAN_POINT ( 'NONE',  ( 3.313708498984762496, -7.999999999999989342, 26.79905277982337353 ) ) ;
#70075=AXIS2_PLACEMENT_3D ( 'NONE', #5384, #33698, #45732 ) ;
#70081=LINE ( 'NONE', #52723, #13799 ) ;
#70090=CARTESIAN_POINT ( 'NONE',  ( -5.082755093536319713, 5.082755093536319713, 5.799052781871753659 ) ) ;
#70115=CARTESIAN_POINT ( 'NONE',  ( -2.977408999572647819, 7.188101187499991163, 3.080302781871750994 ) ) ;
#70128=CARTESIAN_POINT ( 'NONE',  ( -3.313708498984757167, 7.999999999999991118, 23.23655278392014623 ) ) ;
#70146=LINE ( 'NONE', #18453, #70960 ) ;
#70149=CARTESIAN_POINT ( 'NONE',  ( 5.082755093536320601, -5.082755093536318824, 26.04905278187175810 ) ) ;
#70159=CARTESIAN_POINT ( 'NONE',  ( 7.999999999999991118, 9.797174393178815797E-16, 19.76780278392014623 ) ) ;
#70170=CARTESIAN_POINT ( 'NONE',  ( 5.082755093536318824, 5.082755093536319713, 21.92405278187175455 ) ) ;
#70182=FACE_OUTER_BOUND ( 'NONE', #44929, .T. ) ;
#70186=CARTESIAN_POINT ( 'NONE',  ( 5.662595241051936235, -5.662595241051934458, 4.575615283940629219 ) ) ;
#70194=CARTESIAN_POINT ( 'NONE',  ( -2.977408999572647819, 7.188101187499991163, 28.58030278187176165 ) ) ;
#70212=CARTESIAN_POINT ( 'NONE',  ( -7.999999999999991118, 3.313708498984756723, 12.73655277982336287 ) ) ;
#70218=VERTEX_POINT ( 'NONE', #4686 ) ;
#70226=CARTESIAN_POINT ( 'NONE',  ( -4.898587196589407898E-16, 7.999999999999991118, 20.01155278432982243 ) ) ;
#70256=CARTESIAN_POINT ( 'NONE',  ( 1.320432766682872962E-15, -7.188101187499992051, 13.86155278187175455 ) ) ;
#70258=ORIENTED_EDGE ( 'NONE', *, *, #49440, .T. ) ;
#70279=CARTESIAN_POINT ( 'NONE',  ( 2.977408999572646486, 7.188101187499992051, 13.39280278187175277 ) ) ;
#70282=LINE ( 'NONE', #8758, #68216 ) ;
#70325=CARTESIAN_POINT ( 'NONE',  ( -3.317071493978880348, -8.008118988124989457, 16.29436528394063188 ) ) ;
#70326=B_SPLINE_CURVE_WITH_KNOTS ( 'NONE', 3,
 ( #72821, #19631, #71680, #48303 ),
 .UNSPECIFIED., .F., .F.,
 ( 4, 4 ),
 ( 0.000000000000000000, 1.000000000000000000 ),
 .UNSPECIFIED. ) ;
#70331=CARTESIAN_POINT ( 'NONE',  ( -2.977408999572647819, -7.188101187499990274, 9.267802781871754547 ) ) ;
#70340=ORIENTED_EDGE ( 'NONE', *, *, #9204, .F. ) ;
#70348=CARTESIAN_POINT ( 'NONE',  ( -3.313708498984758943, -7.999999999999989342, 1.299052783920146448 ) ) ;
#70353=DIRECTION ( 'NONE',  ( -0.000000000000000000, -0.000000000000000000, 1.000000000000000000 ) ) ;
#70362=CARTESIAN_POINT ( 'NONE',  ( 2.977408999572646486, 7.188101187499991163, 8.892802781871754547 ) ) ;
#70379=CARTESIAN_POINT ( 'NONE',  ( -8.000000000000000000, -3.313708498984752282, 24.92405277982337353 ) ) ;
#70387=CARTESIAN_POINT ( 'NONE',  ( -3.313708498984758943, -7.999999999999989342, 17.61155277982336997 ) ) ;
#70405=EDGE_LOOP ( 'NONE', ( #16494, #63611, #44815, #41941, #7164, #8011 ) ) ;
#70450=CARTESIAN_POINT ( 'NONE',  ( -7.188101187499991163, 2.977408999572646930, 8.892802781871754547 ) ) ;
#70475=CARTESIAN_POINT ( 'NONE',  ( -7.188101187499990274, -2.977408999572651371, 3.455302781871751439 ) ) ;
#70489=CARTESIAN_POINT ( 'NONE',  ( -5.656854249492373476, -5.656854249492376141, 25.20530278392014978 ) ) ;
#70500=CARTESIAN_POINT ( 'NONE',  ( -6.062583391206407768, -5.219682234019338729, -0.1039400739145942276 ) ) ;
#70508=CARTESIAN_POINT ( 'NONE',  ( 7.188101187499993827, -2.977408999572645598, 18.64280278187176521 ) ) ;
#70510=VERTEX_POINT ( 'NONE', #8008 ) ;
#70516=CARTESIAN_POINT ( 'NONE',  ( 1.469576158976822172E-15, -7.999999999999991118, 17.89280278392014623 ) ) ;
#70530=CARTESIAN_POINT ( 'NONE',  ( 7.188101187499991163, 2.977408999572648707, 26.33030278187175810 ) ) ;
#70542=CARTESIAN_POINT ( 'NONE',  ( 5.082755093536320601, -5.082755093536318824, 0.9240527818717529929 ) ) ;
#70543=CARTESIAN_POINT ( 'NONE',  ( 0.000000000000000000, 0.000000000000000000, 30.00000000000000000 ) ) ;
#70546=CARTESIAN_POINT ( 'NONE',  ( -5.662595241051935346, 5.662595241051935346, 5.325615283940630107 ) ) ;
#70553=CARTESIAN_POINT ( 'NONE',  ( -5.082755093536319713, 5.082755093536319713, 24.17405278187175455 ) ) ;
#70560=EDGE_LOOP ( 'NONE', ( #71195, #13448, #771, #19974 ) ) ;
#70571=CARTESIAN_POINT ( 'NONE',  ( 1.469576158976822172E-15, -7.999999999999991118, 16.20530277982336287 ) ) ;
#70584=CARTESIAN_POINT ( 'NONE',  ( -4.898587196589407898E-16, 7.999999999999991118, 15.51155278432982598 ) ) ;
#70613=CARTESIAN_POINT ( 'NONE',  ( 2.977408999572650927, -7.188101187499990274, 13.95530278187175277 ) ) ;
#70622=EDGE_CURVE ( 'NONE', #49450, #70218, #70282, .T. ) ;
#70637=CARTESIAN_POINT ( 'NONE',  ( -7.188101187499992051, 2.977408999572646930, 9.267802781871754547 ) ) ;
#70673=FACE_OUTER_BOUND ( 'NONE', #65846, .T. ) ;
#70683=CARTESIAN_POINT ( 'NONE',  ( -8.008118988124991233, 0.000000000000000000, 7.013115283940628331 ) ) ;
#70688=CARTESIAN_POINT ( 'NONE',  ( -5.082755093536317936, -5.082755093536320601, 7.674052781871751883 ) ) ;
#70701=CARTESIAN_POINT ( 'NONE',  ( 5.656854249492376141, -5.656854249492374365, 1.580302783920146226 ) ) ;
#70716=CARTESIAN_POINT ( 'NONE',  ( 2.977408999572646486, 7.188101187499991163, 13.39280278187175455 ) ) ;
#70745=CARTESIAN_POINT ( 'NONE',  ( 5.656854249492376141, -5.656854249492374365, 16.39280277982336287 ) ) ;
#70765=AXIS2_PLACEMENT_3D ( 'NONE', #71976, #36919, #37294 ) ;
#70769=CARTESIAN_POINT ( 'NONE',  ( 0.000000000000000000, 0.000000000000000000, 30.00000000000000000 ) ) ;
#70805=LINE ( 'NONE', #25511, #26537 ) ;
#70812=CARTESIAN_POINT ( 'NONE',  ( -2.977408999572648707, -7.188101187499990274, 1.767802781871753881 ) ) ;
#70837=CARTESIAN_POINT ( 'NONE',  ( 2.977408999572650927, -7.188101187499990274, 2.330302781871754991 ) ) ;
#70852=CARTESIAN_POINT ( 'NONE',  ( -3.313708498984757167, 7.999999999999991118, 27.73655278392014978 ) ) ;
#70874=CARTESIAN_POINT ( 'NONE',  ( 5.082755093536320601, -5.082755093536318824, 20.04905278187175455 ) ) ;
#70883=CARTESIAN_POINT ( 'NONE',  ( -7.999999999999989342, -3.313708498984762496, 13.11155278392014623 ) ) ;
#70894=CARTESIAN_POINT ( 'NONE',  ( 1.320432766682872962E-15, -7.188101187499992051, 19.86155278187175455 ) ) ;
#70911=CARTESIAN_POINT ( 'NONE',  ( 1.469576158976822172E-15, -7.999999999999991118, 23.89280278392014978 ) ) ;
#70918=CARTESIAN_POINT ( 'NONE',  ( -7.188101187499990274, -2.977408999572651371, 21.45530278187175810 ) ) ;
#70934=CARTESIAN_POINT ( 'NONE',  ( -4.898587196589407898E-16, 7.999999999999991118, 15.45530277982336642 ) ) ;
#70946=CARTESIAN_POINT ( 'NONE',  ( 1.469576158976822172E-15, -7.999999999999991118, 20.76155278432982243 ) ) ;
#70960=VECTOR ( 'NONE', #51294, 1000.000000000000000 ) ;
#70978=CARTESIAN_POINT ( 'NONE',  ( -7.188101187499990274, -2.977408999572651371, 15.08030278187175455 ) ) ;
#70999=CARTESIAN_POINT ( 'NONE',  ( -7.188101187499992051, 0.000000000000000000, 9.361552781871752771 ) ) ;
#71007=VECTOR ( 'NONE', #63335, 1000.000000000000000 ) ;
#71023=VERTEX_POINT ( 'NONE', #40038 ) ;
#71029=CARTESIAN_POINT ( 'NONE',  ( 0.000000000000000000, 0.000000000000000000, 30.00000000000000000 ) ) ;
#71041=CARTESIAN_POINT ( 'NONE',  ( -8.008118988124991233, 0.000000000000000000, 8.513115283940630107 ) ) ;
#71047=CARTESIAN_POINT ( 'NONE',  ( -7.188101187499990274, -2.977408999572651815, 12.08030278187175277 ) ) ;
#71061=CARTESIAN_POINT ( 'NONE',  ( 5.656854249492376141, -5.656854249492374365, 0.08030278392014492117 ) ) ;
#71085=CARTESIAN_POINT ( 'NONE',  ( -5.082755093536319713, 5.082755093536319713, 27.17405278187175455 ) ) ;
#71097=CARTESIAN_POINT ( 'NONE',  ( 7.999999999999991118, 9.797174393178815797E-16, 28.58030277982336642 ) ) ;
#71103=CARTESIAN_POINT ( 'NONE',  ( 1.469576158976822172E-15, -7.999999999999991118, 16.20530277982336287 ) ) ;
#71105=DIRECTION ( 'NONE',  ( 0.6524685526581929240, -0.7578158002934526349, 2.485390736430017174E-05 ) ) ;
#71117=CARTESIAN_POINT ( 'NONE',  ( -7.999999999999991118, 0.000000000000000000, 27.83030277982336642 ) ) ;
#71132=CARTESIAN_POINT ( 'NONE',  ( -4.903558642999205574E-16, 8.008118988124991233, 24.63811528394063188 ) ) ;
#71168=CARTESIAN_POINT ( 'NONE',  ( -2.977408999572648707, -7.188101187499990274, 3.267802781871751439 ) ) ;
#71181=CARTESIAN_POINT ( 'NONE',  ( 7.999999999999991118, 0.000000000000000000, 30.00000000000000000 ) ) ;
#71193=CARTESIAN_POINT ( 'NONE',  ( 5.082755093536318824, 5.082755093536319713, 5.799052781871753659 ) ) ;
#71195=ORIENTED_EDGE ( 'NONE', *, *, #69212, .T. ) ;
#71197=( BOUNDED_CURVE ( )  B_SPLINE_CURVE ( 2, ( #11384, #39681, #11018, #34051, #57422, #24146, #23042 ),
 .UNSPECIFIED., .F., .F. ) 
 B_SPLINE_CURVE_WITH_KNOTS ( ( 3, 2, 2, 3 ),
 ( 0.9795047134926050392, 0.9795047864996143661, 0.9861230620840667482, 0.9889322145411023612 ),
 .UNSPECIFIED. ) 
 CURVE ( )  GEOMETRIC_REPRESENTATION_ITEM ( )  RATIONAL_B_SPLINE_CURVE ( ( 0.9999983206301090721, 0.9999991603057917233, 1.000000000000000000, 0.9238795325112867385, 1.000000000000000000, 0.9676903756049457517, 0.9628086392139758587 ) ) 
 REPRESENTATION_ITEM ( '' )  );
#71209=CARTESIAN_POINT ( 'NONE',  ( 7.999999999999991118, 3.313708498984757611, 25.86155278392014623 ) ) ;
#71210=LINE ( 'NONE', #2192, #72187 ) ;
#71230=CARTESIAN_POINT ( 'NONE',  ( -7.188101187499990274, -2.977408999572651815, 19.58030278187175455 ) ) ;
#71241=CARTESIAN_POINT ( 'NONE',  ( -7.999999999999991118, 0.000000000000000000, 13.01780278392014623 ) ) ;
#71251=CARTESIAN_POINT ( 'NONE',  ( 7.188101187499991163, 2.977408999572648707, 20.33030278187175455 ) ) ;
#71256=FACE_OUTER_BOUND ( 'NONE', #11991, .T. ) ;
#71269=CARTESIAN_POINT ( 'NONE',  ( -5.656854249492375253, 5.656854249492375253, 24.83030278392014978 ) ) ;
#71276=CARTESIAN_POINT ( 'NONE',  ( -7.188101187499990274, -2.977408999572651371, 22.95530278187175455 ) ) ;
#71293=CARTESIAN_POINT ( 'NONE',  ( -4.898587196589407898E-16, 7.999999999999991118, 13.95530277982336465 ) ) ;
#71309=CYLINDRICAL_SURFACE ( 'NONE', #73668, 7.999999999999991118 ) ;
#71310=CARTESIAN_POINT ( 'NONE',  ( 5.656854249492376141, -5.656854249492374365, 14.94905278432982421 ) ) ;
#71312=CARTESIAN_POINT ( 'NONE',  ( -3.313708498984759387, -7.999999999999989342, 16.11155277982336642 ) ) ;
#71340=CARTESIAN_POINT ( 'NONE',  ( -4.401442555609577197E-16, 7.188101187499992051, 4.111552781871752771 ) ) ;
#71361=CARTESIAN_POINT ( 'NONE',  ( -7.188101187499990274, -2.977408999572651815, 1.955302781871753881 ) ) ;
#71384=CARTESIAN_POINT ( 'NONE',  ( -7.999999999999991118, 0.000000000000000000, 23.33030277982336642 ) ) ;
#71390=CARTESIAN_POINT ( 'NONE',  ( 3.313708498984756279, 7.999999999999991118, 6.549052783920143561 ) ) ;
#71407=( BOUNDED_CURVE ( )  B_SPLINE_CURVE ( 2, ( #3214, #53418, #42445, #13757, #14508, #37548, #71479, #60547, #8871, #31882, #54905, #38294, #15633 ),
 .UNSPECIFIED., .F., .F. ) 
 B_SPLINE_CURVE_WITH_KNOTS ( ( 3, 2, 2, 2, 2, 2, 3 ),
 ( 0.7941930320969252666, 0.7941930701348174360, 0.8008113457192742590, 0.8074296213037310821, 0.8140478968881879052, 0.8206661724726446172, 0.8206662513146789628 ),
 .UNSPECIFIED. ) 
 CURVE ( )  GEOMETRIC_REPRESENTATION_ITEM ( )  RATIONAL_B_SPLINE_CURVE ( ( 0.9999991250151324396, 0.9999995625050517312, 1.000000000000000000, 0.9238795325112867385, 1.000000000000000000, 0.9238795325112867385, 1.000000000000000000, 0.9238795325112867385, 1.000000000000000000, 0.9238795325112867385, 1.000000000000000000, 0.9999990931939241046, 0.9999981864094533712 ) ) 
 REPRESENTATION_ITEM ( '' )  );
#71409=CARTESIAN_POINT ( 'NONE',  ( 8.008118988124991233, 9.807117285998411148E-16, 10.76311528394063188 ) ) ;
#71416=CARTESIAN_POINT ( 'NONE',  ( -7.188101187499992051, 2.977408999572646930, 1.392802781871753437 ) ) ;
#71426=CARTESIAN_POINT ( 'NONE',  ( -7.188101187499990274, -2.977408999572651371, 27.08030278187175810 ) ) ;
#71430=CARTESIAN_POINT ( 'NONE',  ( 6.985286989847971917, 4.041240684893442570, -0.000000000000000000 ) ) ;
#71444=CARTESIAN_POINT ( 'NONE',  ( 7.999999999999991118, -3.145386390148749531E-05, 1.767801894041102218 ) ) ;
#71449=CARTESIAN_POINT ( 'NONE',  ( 2.977408999572650927, -7.188101187499990274, 26.33030278187176165 ) ) ;
#71470=CARTESIAN_POINT ( 'NONE',  ( 5.656854249492376141, -5.656854249492374365, 17.89280277982336642 ) ) ;
#71479=CARTESIAN_POINT ( 'NONE',  ( -4.898587196589407898E-16, 7.999999999999991118, 5.142802783920146226 ) ) ;
#71483=CARTESIAN_POINT ( 'NONE',  ( 5.656854249492374365, 5.656854249492375253, 27.26780277982336642 ) ) ;
#71500=CARTESIAN_POINT ( 'NONE',  ( 8.008118988124993010, -3.317071493978877239, 24.16936528394063544 ) ) ;
#71534=CARTESIAN_POINT ( 'NONE',  ( -4.401442555609577197E-16, 7.188101187499992051, 1.111552781871753215 ) ) ;
#71548=VERTEX_POINT ( 'NONE', #46303 ) ;
#71562=CARTESIAN_POINT ( 'NONE',  ( 7.188101187499991163, 2.977408999572648707, 1.205302781871753215 ) ) ;
#71579=CARTESIAN_POINT ( 'NONE',  ( -7.999999999999989342, -3.313708498984762496, 20.61155278392014623 ) ) ;
#71583=DIRECTION ( 'NONE',  ( 1.000000000000000000, -0.000000000000000000, 0.000000000000000000 ) ) ;
#71597=VERTEX_POINT ( 'NONE', #47411 ) ;
#71600=CARTESIAN_POINT ( 'NONE',  ( -4.401442555609577197E-16, 7.188101187499992051, 20.61155278187175455 ) ) ;
#71602=ORIENTED_EDGE ( 'NONE', *, *, #13968, .F. ) ;
#71608=CARTESIAN_POINT ( 'NONE',  ( 5.656854249492374365, 5.656854249492375253, 10.95530278392014800 ) ) ;
#71611=ADVANCED_FACE ( 'NONE', ( #24763 ), #74084, .T. ) ;
#71620=CARTESIAN_POINT ( 'NONE',  ( 7.188101187499992051, 8.802885111219154394E-16, 20.23655278187175099 ) ) ;
#71637=ADVANCED_FACE ( 'NONE', ( #2507 ), #71896, .T. ) ;
#71641=CARTESIAN_POINT ( 'NONE',  ( -7.999999999999991118, 3.313708498984756723, 23.42405278392015333 ) ) ;
#71642=DIRECTION ( 'NONE',  ( -0.000000000000000000, -0.000000000000000000, 1.000000000000000000 ) ) ;
#71648=CARTESIAN_POINT ( 'NONE',  ( 5.082755093536318824, 5.082755093536319713, 20.79905278187175455 ) ) ;
#71664=CARTESIAN_POINT ( 'NONE',  ( 3.313708498984762496, -7.999999999999989342, 11.79905277982336465 ) ) ;
#71679=CARTESIAN_POINT ( 'NONE',  ( 7.999999999999991118, 3.313708498984757611, 16.73030278432982243 ) ) ;
#71680=CARTESIAN_POINT ( 'NONE',  ( -5.652416403964814151, -4.866508352364031786, 0.6881790637065305916 ) ) ;
#71711=CARTESIAN_POINT ( 'NONE',  ( 5.082755093536318824, 5.082755093536319713, 5.424052781871753659 ) ) ;
#71735=CARTESIAN_POINT ( 'NONE',  ( 2.977408999572646486, 7.188101187499992051, 5.892802781871753659 ) ) ;
#71737=CYLINDRICAL_SURFACE ( 'NONE', #49322, 7.999999999999991118 ) ;
#71766=CARTESIAN_POINT ( 'NONE',  ( -5.656854249492375253, 5.656854249492375253, 8.330302783920144449 ) ) ;
#71768=DIRECTION ( 'NONE',  ( 0.000000000000000000, 0.9659258262890700886, 0.2588190451025146888 ) ) ;
#71783=CARTESIAN_POINT ( 'NONE',  ( -3.317071493978878571, 8.008118988124991233, 11.23186528394062833 ) ) ;
#71789=CARTESIAN_POINT ( 'NONE',  ( -5.082755093536319713, 5.082755093536319713, 1.299052781871753215 ) ) ;
#71802=CARTESIAN_POINT ( 'NONE',  ( 2.977408999572650927, -7.188101187499990274, 22.95530278187175455 ) ) ;
#71827=CARTESIAN_POINT ( 'NONE',  ( 5.082755093536318824, 5.082755093536319713, 23.79905278187175455 ) ) ;
#71829=CARTESIAN_POINT ( 'NONE',  ( 7.999999999999992895, -3.313708498984756279, 22.67405278392014978 ) ) ;
#71844=CARTESIAN_POINT ( 'NONE',  ( 5.656854249492376141, -5.656854249492374365, 7.392802779823366421 ) ) ;
#71848=( BOUNDED_CURVE ( )  B_SPLINE_CURVE ( 2, ( #14598, #60636, #31969, #9332, #73445, #21752, #67794, #16085, #39120 ),
 .UNSPECIFIED., .F., .F. ) 
 B_SPLINE_CURVE_WITH_KNOTS ( ( 3, 2, 2, 2, 3 ),
 ( 0.5000000000000000000, 0.5065789473684210176, 0.5131578947368422572, 0.5197368421052632748, 0.5263157894736842923 ),
 .UNSPECIFIED. ) 
 CURVE ( )  GEOMETRIC_REPRESENTATION_ITEM ( )  RATIONAL_B_SPLINE_CURVE ( ( 1.000000000000000000, 0.9238795325112867385, 1.000000000000000000, 0.9238795325112867385, 1.000000000000000000, 0.9238795325112867385, 1.000000000000000000, 0.9238795325112854062, 1.000000000000001332 ) ) 
 REPRESENTATION_ITEM ( '' )  );
#71875=CARTESIAN_POINT ( 'NONE',  ( -5.662595241051935346, 5.662595241051935346, 27.82561528394063188 ) ) ;
#71885=AXIS2_PLACEMENT_3D ( 'NONE', #50920, #39980, #39236 ) ;
#71889=CARTESIAN_POINT ( 'NONE',  ( -7.999999999999991118, 3.313708498984757167, 21.73655277982336642 ) ) ;
#71896=SPHERICAL_SURFACE ( 'NONE', #39187, 15.99999999999998579 ) ;
#71899=CARTESIAN_POINT ( 'NONE',  ( 3.313708498984762496, -7.999999999999989342, 8.986552783920146226 ) ) ;
#71912=CARTESIAN_POINT ( 'NONE',  ( 1.320432766682872962E-15, -7.188101187499992051, 3.361552781871751883 ) ) ;
#71914=CARTESIAN_POINT ( 'NONE',  ( 7.999999999999304556, -3.314968910423997278E-06, 15.26780269013280034 ) ) ;
#71937=CARTESIAN_POINT ( 'NONE',  ( 7.999999999999991118, 3.313708498984757611, 25.67405277982336997 ) ) ;
#71951=CARTESIAN_POINT ( 'NONE',  ( -4.898587196589407898E-16, 7.999999999999991118, 21.64280278392014623 ) ) ;
#71962=ORIENTED_EDGE ( 'NONE', *, *, #65592, .T. ) ;
#71975=CARTESIAN_POINT ( 'NONE',  ( 1.320432766682872962E-15, -7.188101187499992051, 19.86155278187175455 ) ) ;
#71976=CARTESIAN_POINT ( 'NONE',  ( 0.000000000000000000, 130.3999865490244190, 45.94057108883949070 ) ) ;
#71986=CARTESIAN_POINT ( 'NONE',  ( 7.999999999999991118, 3.313708498984757611, 12.36155278392014445 ) ) ;
#71996=CARTESIAN_POINT ( 'NONE',  ( -2.977408999572648707, -7.188101187499990274, 19.76780278187175455 ) ) ;
#72001=CARTESIAN_POINT ( 'NONE',  ( 7.999972922956211541, -3.313735576028537189, 6.174051700559090250 ) ) ;
#72012=CARTESIAN_POINT ( 'NONE',  ( 5.656854249492374365, 5.656854249492375253, 0.4553027839201452265 ) ) ;
#72015=CARTESIAN_POINT ( 'NONE',  ( 3.313708498984756279, 7.999999999999991118, 23.04905278392014623 ) ) ;
#72022=CARTESIAN_POINT ( 'NONE',  ( -2.977408999572648707, -7.188101187499990274, 23.14280278187176165 ) ) ;
#72036=CARTESIAN_POINT ( 'NONE',  ( 7.999999999999991118, 3.313708498984757611, 7.674052779823366421 ) ) ;
#72052=CARTESIAN_POINT ( 'NONE',  ( 3.313708498984762496, -7.999999999999989342, 10.35530278432982598 ) ) ;
#72054=CARTESIAN_POINT ( 'NONE',  ( -5.656854249492373476, -5.656854249492376141, 16.01780277982336642 ) ) ;
#72081=CYLINDRICAL_SURFACE ( 'NONE', #55964, 7.999999999999991118 ) ;
#72084=CARTESIAN_POINT ( 'NONE',  ( 8.000000000000035527, 3.313708498984715423, 16.67405277982336642 ) ) ;
#72085=SHAPE_REPRESENTATION_RELATIONSHIP ( 'NONE' , 'NONE' ,  #48857, #37253 ) ;
#72089=CARTESIAN_POINT ( 'NONE',  ( 5.082755093536320601, -5.082755093536318824, 6.549052781871754547 ) ) ;
#72102=CARTESIAN_POINT ( 'NONE',  ( -4.401442555609577197E-16, 7.188101187499992051, 10.48655278187175455 ) ) ;
#72109=DIRECTION ( 'NONE',  ( -0.000000000000000000, -0.000000000000000000, 1.000000000000000000 ) ) ;
#72114=CARTESIAN_POINT ( 'NONE',  ( -7.188101187499990274, -2.977408999572651815, 4.955302781871752771 ) ) ;
#72130=CARTESIAN_POINT ( 'NONE',  ( 7.999999999999991118, 3.313708498984757611, 25.67405277982336997 ) ) ;
#72136=CARTESIAN_POINT ( 'NONE',  ( -7.999999999994261479, 6.398094505892175214E-06, 25.01756343669228499 ) ) ;
#72142=CARTESIAN_POINT ( 'NONE',  ( -3.313708498984757167, 7.999999999999991118, 2.236552783920143561 ) ) ;
#72164=CARTESIAN_POINT ( 'NONE',  ( 1.320432766682872962E-15, -7.188101187499992051, 3.361552781871751883 ) ) ;
#72166=EDGE_CURVE ( 'NONE', #39299, #59170, #71407, .T. ) ;
#72177=CARTESIAN_POINT ( 'NONE',  ( -4.401442555609577197E-16, 7.188101187499992051, 26.61155278187175455 ) ) ;
#72183=CARTESIAN_POINT ( 'NONE',  ( -7.796932491751043415, 2.081755106361893759, -0.000000000000000000 ) ) ;
#72187=VECTOR ( 'NONE', #59541, 1000.000000000000000 ) ;
#72196=CARTESIAN_POINT ( 'NONE',  ( -3.313708498984757611, 7.999999999999991118, 24.73655278392014978 ) ) ;
#72197=CARTESIAN_POINT ( 'NONE',  ( 5.656854249492376141, -5.656854249492374365, 22.39280277982336997 ) ) ;
#72199=EDGE_CURVE ( 'NONE', #31338, #62523, #4455, .T. ) ;
#72203=CARTESIAN_POINT ( 'NONE',  ( 1.320432766682872962E-15, -7.188101187499992051, 23.23655278187175455 ) ) ;
#72222=CARTESIAN_POINT ( 'NONE',  ( 7.999999999999992895, -3.313708498984756279, 10.48655277982336642 ) ) ;
#72254=DIRECTION ( 'NONE',  ( -0.000000000000000000, -0.000000000000000000, 1.000000000000000000 ) ) ;
#72255=CARTESIAN_POINT ( 'NONE',  ( 5.662595241051936235, -5.662595241051934458, 27.07561528394063188 ) ) ;
#72290=CARTESIAN_POINT ( 'NONE',  ( -7.188101187499992051, 0.000000000000000000, 1.486552781871753437 ) ) ;
#72292=CARTESIAN_POINT ( 'NONE',  ( 3.313708498984756279, 7.999999999999991118, 15.54905278392014623 ) ) ;
#72293=DIRECTION ( 'NONE',  ( -0.000000000000000000, -0.000000000000000000, 1.000000000000000000 ) ) ;
#72318=CARTESIAN_POINT ( 'NONE',  ( 5.656854249492376141, -5.656854249492374365, 26.89280277982336642 ) ) ;
#72335=CARTESIAN_POINT ( 'NONE',  ( 3.313708498984756279, 7.999999999999991118, 17.04905278392014623 ) ) ;
#72359=CARTESIAN_POINT ( 'NONE',  ( 2.977408999572650927, -7.188101187499990274, 12.45530278187175277 ) ) ;
#72361=ORIENTED_EDGE ( 'NONE', *, *, #66091, .T. ) ;
#72369=CARTESIAN_POINT ( 'NONE',  ( -4.898587196589407898E-16, 7.999999999999991118, 14.14280278392014623 ) ) ;
#72371=CARTESIAN_POINT ( 'NONE',  ( -4.898587196589407898E-16, 7.999999999999991118, 18.64280278392014623 ) ) ;
#72375=CARTESIAN_POINT ( 'NONE',  ( -3.313708498984757611, 7.999999999999991118, 12.54905277982336287 ) ) ;
#72381=CARTESIAN_POINT ( 'NONE',  ( 1.320432766682872962E-15, -7.188101187499992051, 16.86155278187175810 ) ) ;
#72400=CARTESIAN_POINT ( 'NONE',  ( -7.999999999999989342, -3.313708498984762496, 25.11155278392014623 ) ) ;
#72407=CARTESIAN_POINT ( 'NONE',  ( 7.188101187499991163, 2.977408999572648707, 17.70530278187175455 ) ) ;
#72415=CARTESIAN_POINT ( 'NONE',  ( 7.999999999999991118, 9.797174393178815797E-16, 18.08030277982336642 ) ) ;
#72425=CARTESIAN_POINT ( 'NONE',  ( -5.656854249492375253, 5.656854249492375253, 11.14280277982336642 ) ) ;
#72426=CARTESIAN_POINT ( 'NONE',  ( 5.656854249492374365, 5.656854249492375253, 21.45530278392014623 ) ) ;
#72444=CARTESIAN_POINT ( 'NONE',  ( 7.999999999999991118, 9.797174393178815797E-16, 12.13655278432982421 ) ) ;
#72476=CARTESIAN_POINT ( 'NONE',  ( 7.188101187499993827, -2.977408999572645598, 5.142802781871752771 ) ) ;
#72489=CARTESIAN_POINT ( 'NONE',  ( -5.082755093536319713, 5.082755093536319713, 9.174052781871752771 ) ) ;
#72498=DIRECTION ( 'NONE',  ( 1.000000000000000000, 0.000000000000000000, 0.000000000000000000 ) ) ;
#72501=CARTESIAN_POINT ( 'NONE',  ( 5.082755093536320601, -5.082755093536318824, 2.424052781871754103 ) ) ;
#72515=DIRECTION ( 'NONE',  ( -0.000000000000000000, -0.000000000000000000, 1.000000000000000000 ) ) ;
#72518=CARTESIAN_POINT ( 'NONE',  ( -3.313708498984757167, 7.999999999999991118, 24.54905277982336287 ) ) ;
#72530=CARTESIAN_POINT ( 'NONE',  ( -4.898587196589407898E-16, 7.999999999999991118, 2.142802783920143117 ) ) ;
#72534=FACE_OUTER_BOUND ( 'NONE', #15075, .T. ) ;
#72543=CARTESIAN_POINT ( 'NONE',  ( -7.999999999999991118, 3.313708498984757167, 0.9240527839201456706 ) ) ;
#72554=CARTESIAN_POINT ( 'NONE',  ( -7.188101187499992051, 0.000000000000000000, 4.486552781871752771 ) ) ;
#72561=VERTEX_POINT ( 'NONE', #19994 ) ;
#72568=CARTESIAN_POINT ( 'NONE',  ( -5.082755093536319713, 5.082755093536319713, 25.29905278187175810 ) ) ;
#72591=CARTESIAN_POINT ( 'NONE',  ( -7.188101187499992051, 0.000000000000000000, 19.86155278187175455 ) ) ;
#72601=CARTESIAN_POINT ( 'NONE',  ( -7.999999999999991118, 0.000000000000000000, 17.51780278392014623 ) ) ;
#72610=CARTESIAN_POINT ( 'NONE',  ( -7.999999999999989342, -3.313708498984762496, 8.424052779823362869 ) ) ;
#72649=( BOUNDED_CURVE ( )  B_SPLINE_CURVE ( 2, ( #53558, #72001, #60697, #42590, #31277, #20316, #2984, #32031, #42957 ),
 .UNSPECIFIED., .F., .F. ) 
 B_SPLINE_CURVE_WITH_KNOTS ( ( 3, 2, 2, 2, 3 ),
 ( 0.7677200384551818857, 0.7743382433814469668, 0.7809565189659037898, 0.7875747945503606129, 0.7941930320969252666 ),
 .UNSPECIFIED. ) 
 CURVE ( )  GEOMETRIC_REPRESENTATION_ITEM ( )  RATIONAL_B_SPLINE_CURVE ( ( 0.9999983746590511702, 0.9238803451904374908, 1.000000000000000000, 0.9238795325112867385, 1.000000000000000000, 0.9238795325112867385, 1.000000000000000000, 0.9238799700062350073, 0.9999991250151324396 ) ) 
 REPRESENTATION_ITEM ( '' )  );
#72676=CARTESIAN_POINT ( 'NONE',  ( 7.188101187499992051, 8.802885111219154394E-16, 25.11155278187175810 ) ) ;
#72702=CARTESIAN_POINT ( 'NONE',  ( 1.469576158976822172E-15, -7.999999999999991118, 26.70530277982336642 ) ) ;
#72719=CARTESIAN_POINT ( 'NONE',  ( -5.656854249492375253, 5.656854249492375253, 17.33030278392014623 ) ) ;
#72730=CARTESIAN_POINT ( 'NONE',  ( -7.999999999999991118, 0.000000000000000000, 2.330302779823365089 ) ) ;
#72741=CARTESIAN_POINT ( 'NONE',  ( -4.401442555609577197E-16, 7.188101187499992051, 17.61155278187175810 ) ) ;
#72753=CARTESIAN_POINT ( 'NONE',  ( 7.999999999999991118, 9.797174393178815797E-16, 6.267802783920147114 ) ) ;
#72764=CARTESIAN_POINT ( 'NONE',  ( 7.188101187499993827, -2.977408999572645598, 14.14280278187175455 ) ) ;
#72767=ORIENTED_EDGE ( 'NONE', *, *, #28852, .F. ) ;
#72789=CARTESIAN_POINT ( 'NONE',  ( 7.188101187499992051, 8.802885111219154394E-16, 17.61155278187175810 ) ) ;
#72804=CARTESIAN_POINT ( 'NONE',  ( 3.313708498984762496, -7.999999999999989342, 7.299052779823365533 ) ) ;
#72805=CARTESIAN_POINT ( 'NONE',  ( 0.000000000000000000, 0.000000000000000000, 30.00000000000000000 ) ) ;
#72820=CARTESIAN_POINT ( 'NONE',  ( 7.999999999999991118, 3.313708498984757611, 9.230302784329824206 ) ) ;
#72821=CARTESIAN_POINT ( 'NONE',  ( -6.062601303906716588, -5.219661428662635494, 1.000679062340938064 ) ) ;
#72851=AXIS2_PLACEMENT_3D ( 'NONE', #4395, #9686, #39831 ) ;
#72852=CARTESIAN_POINT ( 'NONE',  ( -4.401442555609577197E-16, 7.188101187499992051, 5.611552781871753659 ) ) ;
#72864=CARTESIAN_POINT ( 'NONE',  ( 5.082755093536320601, -5.082755093536318824, 9.924052781871754547 ) ) ;
#72875=DIRECTION ( 'NONE',  ( -0.000000000000000000, -0.000000000000000000, 1.000000000000000000 ) ) ;
#72878=CARTESIAN_POINT ( 'NONE',  ( 7.188101187499992051, 8.802885111219154394E-16, 2.611552781871750994 ) ) ;
#72892=CARTESIAN_POINT ( 'NONE',  ( 3.313708498984762496, -7.999999999999989342, 28.29905277982336997 ) ) ;
#72903=CARTESIAN_POINT ( 'NONE',  ( 7.999999999999991118, 3.313708498984757611, 1.861552783920143117 ) ) ;
#72919=ORIENTED_EDGE ( 'NONE', *, *, #67405, .T. ) ;
#72924=CARTESIAN_POINT ( 'NONE',  ( 2.977408999572646486, 7.188101187499992051, 2.517802781871750994 ) ) ;
#72929=ORIENTED_EDGE ( 'NONE', *, *, #36030, .F. ) ;
#72938=CARTESIAN_POINT ( 'NONE',  ( -2.977408999572648707, -7.188101187499990274, 24.26780278187175455 ) ) ;
#72952=ORIENTED_EDGE ( 'NONE', *, *, #73063, .F. ) ;
#72964=CARTESIAN_POINT ( 'NONE',  ( 7.188101187499992051, 2.977408999572647819, 22.20530278187175810 ) ) ;
#72982=CARTESIAN_POINT ( 'NONE',  ( 5.656854249492376141, -5.656854249492374365, 10.39280277982336465 ) ) ;
#72984=CARTESIAN_POINT ( 'NONE',  ( 7.999999999988127719, 1.377684776014802281E-05, 21.26780317368888618 ) ) ;
#73010=CARTESIAN_POINT ( 'NONE',  ( 8.008118988124993010, -3.317071493978877239, 22.66936528394063188 ) ) ;
#73044=CARTESIAN_POINT ( 'NONE',  ( 7.188101187499992051, 8.802885111219154394E-16, 22.11155278187175455 ) ) ;
#73063=EDGE_CURVE ( 'NONE', #9404, #22615, #61735, .T. ) ;
#73069=CARTESIAN_POINT ( 'NONE',  ( -7.999999999999991118, 0.000000000000000000, 26.33030277982336997 ) ) ;
#73087=CARTESIAN_POINT ( 'NONE',  ( 7.999999999999991118, 3.313708498984757611, 19.86155278392014978 ) ) ;
#73109=CARTESIAN_POINT ( 'NONE',  ( 7.188101187499993827, -2.977408999572645598, 15.64280278187175277 ) ) ;
#73122=CARTESIAN_POINT ( 'NONE',  ( 1.469576158976822172E-15, -7.999999999999991118, 5.892802783920146226 ) ) ;
#73134=CARTESIAN_POINT ( 'NONE',  ( 7.188101187499993827, -2.977408999572645598, 11.14280278187175810 ) ) ;
#73158=CARTESIAN_POINT ( 'NONE',  ( 7.188101187499993827, -2.977408999572645598, 19.01780278187175810 ) ) ;
#73165=VERTEX_POINT ( 'NONE', #72730 ) ;
#73176=CARTESIAN_POINT ( 'NONE',  ( 7.999999999999991118, 3.313708498984757611, 10.67405277982336465 ) ) ;
#73177=CARTESIAN_POINT ( 'NONE',  ( -3.313708498984759387, -7.999999999999989342, 4.299052783920145338 ) ) ;
#73190=CARTESIAN_POINT ( 'NONE',  ( -3.313708498984759387, -7.999999999999989342, 2.799052783920144005 ) ) ;
#73192=CARTESIAN_POINT ( 'NONE',  ( -5.656854249492373476, -5.656854249492376141, 14.57405278432982598 ) ) ;
#73224=CARTESIAN_POINT ( 'NONE',  ( -7.188101187499992051, 0.000000000000000000, 2.986552781871751439 ) ) ;
#73226=VERTEX_POINT ( 'NONE', #15741 ) ;
#73236=CARTESIAN_POINT ( 'NONE',  ( -4.401442555609577197E-16, 7.188101187499992051, 7.486552781871751883 ) ) ;
#73266=CARTESIAN_POINT ( 'NONE',  ( -3.313708498984758943, -7.999999999999989342, 25.11155277982337353 ) ) ;
#73272=CARTESIAN_POINT ( 'NONE',  ( -5.656854249492373476, -5.656854249492376141, 25.20530278392014978 ) ) ;
#73278=CARTESIAN_POINT ( 'NONE',  ( -7.999999999999991118, 0.000000000000000000, 27.88655278432982598 ) ) ;
#73288=EDGE_CURVE ( 'NONE', #852, #26401, #74421, .T. ) ;
#73313=CARTESIAN_POINT ( 'NONE',  ( 1.469576158976822172E-15, -7.999999999999991118, 10.20530277982336465 ) ) ;
#73314=CARTESIAN_POINT ( 'NONE',  ( 2.977408999572650927, -7.188101187499990274, 16.95530278187175455 ) ) ;
#73315=VERTEX_POINT ( 'NONE', #44802 ) ;
#73337=CARTESIAN_POINT ( 'NONE',  ( 5.082755093536318824, 5.082755093536319713, 22.29905278187175455 ) ) ;
#73355=CARTESIAN_POINT ( 'NONE',  ( 3.313708498984756279, 7.999999999999991118, 6.361552779823365533 ) ) ;
#73381=CARTESIAN_POINT ( 'NONE',  ( -3.317071493978880348, -8.008118988124989457, 17.79436528394063188 ) ) ;
#73393=CARTESIAN_POINT ( 'NONE',  ( 7.999999999999968914, 3.313708498984778483, 21.17405277982336287 ) ) ;
#73412=VERTEX_POINT ( 'NONE', #45174 ) ;
#73415=CARTESIAN_POINT ( 'NONE',  ( 2.977408999572650927, -7.188101187499990274, 23.33030278187175455 ) ) ;
#73431=CARTESIAN_POINT ( 'NONE',  ( 7.999999999999992895, -3.313708498984756279, 25.48655277982336997 ) ) ;
#73437=CARTESIAN_POINT ( 'NONE',  ( -4.898587196589407898E-16, 7.999999999999991118, 28.95530277982336642 ) ) ;
#73445=CARTESIAN_POINT ( 'NONE',  ( 1.469576158976822172E-15, -7.999999999999991118, 14.70530277982336642 ) ) ;
#73456=CARTESIAN_POINT ( 'NONE',  ( 5.656854249492374365, 5.656854249492375253, 15.45530278392014623 ) ) ;
#73459=ADVANCED_FACE ( 'NONE', ( #9732 ), #68926, .F. ) ;
#73472=EDGE_CURVE ( 'NONE', #6157, #1239, #53275, .T. ) ;
#73475=CARTESIAN_POINT ( 'NONE',  ( 7.188101187499992051, 2.977408999572647819, 15.83030278187175277 ) ) ;
#73478=EDGE_LOOP ( 'NONE', ( #25512, #15702, #32258, #32111 ) ) ;
#73498=CARTESIAN_POINT ( 'NONE',  ( -5.082755093536317936, -5.082755093536320601, 15.17405278187175455 ) ) ;
#73499=ORIENTED_EDGE ( 'NONE', *, *, #41660, .F. ) ;
#73512=( BOUNDED_CURVE ( )  B_SPLINE_CURVE ( 2, ( #11108, #546, #45061, #51086, #22397, #23528, #69560, #40144, #63149 ),
 .UNSPECIFIED., .F., .F. ) 
 B_SPLINE_CURVE_WITH_KNOTS ( ( 3, 2, 2, 2, 3 ),
 ( 0.6315789473684211286, 0.6381578947368422572, 0.6447368421052632748, 0.6513157894736841813, 0.6578947368421053099 ),
 .UNSPECIFIED. ) 
 CURVE ( )  GEOMETRIC_REPRESENTATION_ITEM ( )  RATIONAL_B_SPLINE_CURVE ( ( 0.9999999999999986677, 0.9238795325112880708, 1.000000000000000000, 0.9238795325112867385, 1.000000000000000000, 0.9238795325112867385, 1.000000000000000000, 0.9238795325112867385, 1.000000000000000000 ) ) 
 REPRESENTATION_ITEM ( '' )  );
#73523=CARTESIAN_POINT ( 'NONE',  ( 7.188101187499993827, -2.977408999572645598, 16.01780278187175455 ) ) ;
#73540=CARTESIAN_POINT ( 'NONE',  ( -3.313708498984758943, -7.999999999999989342, 1.111552779823363757 ) ) ;
#73557=CARTESIAN_POINT ( 'NONE',  ( 3.313708498984762496, -7.999999999999989342, 13.35530278432982421 ) ) ;
#73559=VECTOR ( 'NONE', #12584, 1000.000000000000000 ) ;
#73568=CYLINDRICAL_SURFACE ( 'NONE', #45387, 7.999999999999991118 ) ;
#73589=CARTESIAN_POINT ( 'NONE',  ( 1.320432766682872962E-15, -7.188101187499992051, 3.361552781871751883 ) ) ;
#73593=CARTESIAN_POINT ( 'NONE',  ( -3.313708498984757611, 7.999999999999991118, 20.04905277982336642 ) ) ;
#73602=CARTESIAN_POINT ( 'NONE',  ( 7.188101187499993827, -2.977408999572645598, 5.517802781871753659 ) ) ;
#73645=CARTESIAN_POINT ( 'NONE',  ( 7.999999999999991118, 9.797174393178815797E-16, 0.2678027839201451155 ) ) ;
#73666=FACE_OUTER_BOUND ( 'NONE', #40721, .T. ) ;
#73668=AXIS2_PLACEMENT_3D ( 'NONE', #8316, #60748, #4817 ) ;
#73679=CARTESIAN_POINT ( 'NONE',  ( 2.977408999572650927, -7.188101187499990274, 18.45530278187175455 ) ) ;
#73691=EDGE_CURVE ( 'NONE', #34597, #35470, #59830, .T. ) ;
#73694=CARTESIAN_POINT ( 'NONE',  ( -7.999999999999991118, 0.000000000000000000, 8.330302779823362869 ) ) ;
#73702=CARTESIAN_POINT ( 'NONE',  ( 7.188101187499993827, -2.977408999572645598, 17.51780278187175455 ) ) ;
#73709=ORIENTED_EDGE ( 'NONE', *, *, #38481, .F. ) ;
#73721=CARTESIAN_POINT ( 'NONE',  ( 3.313708498984762496, -7.999999999999989342, 1.299052779823363979 ) ) ;
#73749=CARTESIAN_POINT ( 'NONE',  ( -3.317071493978878571, 8.008118988124991233, 23.23186528394063899 ) ) ;
#73782=CARTESIAN_POINT ( 'NONE',  ( -2.977408999572648707, -7.188101187499990274, 26.14280278187176165 ) ) ;
#73802=CARTESIAN_POINT ( 'NONE',  ( 7.999999999999991118, 0.000000000000000000, 30.00000000000000000 ) ) ;
#73808=CARTESIAN_POINT ( 'NONE',  ( 1.469576158976822172E-15, -7.999999999999991118, 20.70530277982336642 ) ) ;
#73812=ORIENTED_EDGE ( 'NONE', *, *, #38985, .F. ) ;
#73826=CARTESIAN_POINT ( 'NONE',  ( 5.656854249492376141, -5.656854249492374365, 15.08030278392014623 ) ) ;
#73853=ORIENTED_EDGE ( 'NONE', *, *, #44562, .F. ) ;
#73876=CARTESIAN_POINT ( 'NONE',  ( 5.082755093536318824, 5.082755093536319713, 12.92405278187175277 ) ) ;
#73900=CARTESIAN_POINT ( 'NONE',  ( -7.188101187499990274, -2.977408999572651371, 13.95530278187175277 ) ) ;
#73915=CARTESIAN_POINT ( 'NONE',  ( -5.656854249492373476, -5.656854249492376141, 2.517802779823365089 ) ) ;
#73916=CARTESIAN_POINT ( 'NONE',  ( 7.999999999667481099, -7.293937043860970585E-05, 4.767800658666735636 ) ) ;
#73922=CARTESIAN_POINT ( 'NONE',  ( -7.188101187499992051, 0.000000000000000000, 28.48655278187175810 ) ) ;
#73931=CARTESIAN_POINT ( 'NONE',  ( -5.656854249492373476, -5.656854249492376141, 8.574052784329824206 ) ) ;
#73954=ORIENTED_EDGE ( 'NONE', *, *, #17459, .F. ) ;
#73961=CARTESIAN_POINT ( 'NONE',  ( 7.188101187499991163, 2.977408999572648707, 3.830302781871751883 ) ) ;
#73975=CARTESIAN_POINT ( 'NONE',  ( 5.082755093536320601, -5.082755093536318824, 5.424052781871753659 ) ) ;
#73995=EDGE_LOOP ( 'NONE', ( #3281, #40620, #45926, #17258 ) ) ;
#74003=CARTESIAN_POINT ( 'NONE',  ( -5.656854249492375253, 5.656854249492375253, 18.64280277982336642 ) ) ;
#74016=CARTESIAN_POINT ( 'NONE',  ( 3.313708498984756279, 7.999999999999991118, 24.41780278432982954 ) ) ;
#74049=CARTESIAN_POINT ( 'NONE',  ( -2.977408999572648707, -7.188101187499990274, 21.26780278187175810 ) ) ;
#74074=CARTESIAN_POINT ( 'NONE',  ( 1.320432766682872962E-15, -7.188101187499992051, 15.73655278187175632 ) ) ;
#74084=CONICAL_SURFACE ( 'NONE', #9024, 12.50000000000000178, 0.06208826691561822320 ) ;
#74095=CARTESIAN_POINT ( 'NONE',  ( 1.469576158976822172E-15, -7.999999999999991118, 1.205302779823363979 ) ) ;
#74100=CARTESIAN_POINT ( 'NONE',  ( 7.999999999999992895, -3.313708498984756279, 15.17405278392014623 ) ) ;
#74104=ORIENTED_EDGE ( 'NONE', *, *, #37242, .T. ) ;
#74122=CARTESIAN_POINT ( 'NONE',  ( 3.313708498984756279, 7.999999999999991118, 8.049052783920144449 ) ) ;
#74123=CARTESIAN_POINT ( 'NONE',  ( 8.008118988124991233, 9.807117285998411148E-16, 21.26311528394063188 ) ) ;
#74153=CARTESIAN_POINT ( 'NONE',  ( -5.082755093536319713, 5.082755093536319713, 25.67405278187175810 ) ) ;
#74154=DIRECTION ( 'NONE',  ( -0.000000000000000000, -0.000000000000000000, 1.000000000000000000 ) ) ;
#74156=CARTESIAN_POINT ( 'NONE',  ( 0.000000000000000000, 0.000000000000000000, 30.00000000000000000 ) ) ;
#74178=CARTESIAN_POINT ( 'NONE',  ( -5.656854249492373476, -5.656854249492376141, 19.01780277982336642 ) ) ;
#74196=CARTESIAN_POINT ( 'NONE',  ( -3.313708498984757167, 7.999999999999991118, 14.23655278392014623 ) ) ;
#74212=CARTESIAN_POINT ( 'NONE',  ( -3.313708498984759387, -7.999999999999989342, 28.11155277982336642 ) ) ;
#74242=CARTESIAN_POINT ( 'NONE',  ( 7.999999999981424637, 1.723583929636134980E-05, 16.76780327155163874 ) ) ;
#74246=CARTESIAN_POINT ( 'NONE',  ( 2.977408999572650927, -7.188101187499990274, 10.95530278187175455 ) ) ;
#74270=CARTESIAN_POINT ( 'NONE',  ( -5.082755093536319713, 5.082755093536319713, 7.674052781871751883 ) ) ;
#74273=CARTESIAN_POINT ( 'NONE',  ( 5.656854249492374365, 5.656854249492375253, 0.3240527843298232069 ) ) ;
#74284=CARTESIAN_POINT ( 'NONE',  ( -7.999999999999989342, -3.313708498984762496, 5.424052779823364645 ) ) ;
#74302=CARTESIAN_POINT ( 'NONE',  ( -5.656854249492373476, -5.656854249492376141, 4.074052784329823318 ) ) ;
#74328=CARTESIAN_POINT ( 'NONE',  ( 7.999999999999991118, 0.000000000000000000, 30.00000000000000000 ) ) ;
#74333=CARTESIAN_POINT ( 'NONE',  ( -5.656854249492375253, 5.656854249492375253, 20.14280277982336642 ) ) ;
#74343=CARTESIAN_POINT ( 'NONE',  ( 7.188101187499991163, 2.977408999572648707, 5.705302781871753659 ) ) ;
#74352=CARTESIAN_POINT ( 'NONE',  ( -7.188101187499992051, 0.000000000000000000, 27.36155278187175455 ) ) ;
#74371=CARTESIAN_POINT ( 'NONE',  ( -5.656854249492373476, -5.656854249492376141, 20.51780277982336642 ) ) ;
#74379=ORIENTED_EDGE ( 'NONE', *, *, #46194, .F. ) ;
#74385=CARTESIAN_POINT ( 'NONE',  ( 5.656854249492374365, 5.656854249492375253, 24.32405278432982598 ) ) ;
#74420=EDGE_CURVE ( 'NONE', #47940, #13756, #28153, .T. ) ;
#74421=( BOUNDED_CURVE ( )  B_SPLINE_CURVE ( 2, ( #50828, #51570, #67068, #27072, #16107, #74212, #39519, #15367, #16482 ),
 .UNSPECIFIED., .F., .F. ) 
 B_SPLINE_CURVE_WITH_KNOTS ( ( 3, 2, 2, 2, 3 ),
 ( 0.02631578947368422988, 0.03289473684210528909, 0.03947368421052634135, 0.04605263157894740056, 0.05263157894736845976 ),
 .UNSPECIFIED. ) 
 CURVE ( )  GEOMETRIC_REPRESENTATION_ITEM ( )  RATIONAL_B_SPLINE_CURVE ( ( 0.9999999999999997780, 0.9238795325112869605, 1.000000000000000000, 0.9238795325112867385, 1.000000000000000000, 0.9238795325112867385, 1.000000000000000000, 0.9238795325112862944, 1.000000000000000444 ) ) 
 REPRESENTATION_ITEM ( '' )  );
#74423=CARTESIAN_POINT ( 'NONE',  ( 7.188101187499993827, -2.977408999572645598, 18.64280278187175810 ) ) ;
#74443=CARTESIAN_POINT ( 'NONE',  ( -5.082755093536319713, 5.082755093536319713, 18.17405278187175455 ) ) ;
#74448=ORIENTED_EDGE ( 'NONE', *, *, #41660, .T. ) ;
#74463=CARTESIAN_POINT ( 'NONE',  ( 7.999999999999992895, -3.313708498984756279, 2.986552779823361981 ) ) ;
#74492=CARTESIAN_POINT ( 'NONE',  ( -8.008118988124991233, 3.317071493978878127, 21.91936528394063188 ) ) ;
#74512=CARTESIAN_POINT ( 'NONE',  ( -3.313708498984758943, -7.999999999999989342, 7.299052783920144449 ) ) ;
#74517=CARTESIAN_POINT ( 'NONE',  ( -5.656854249492373476, -5.656854249492376141, 8.705302783920146226 ) ) ;
#74529=CARTESIAN_POINT ( 'NONE',  ( 7.188101187499993827, -2.977408999572645598, 17.51780278187175455 ) ) ;
#74555=CARTESIAN_POINT ( 'NONE',  ( -3.313708498984757167, 7.999999999999991118, 23.04905277982336642 ) ) ;
#74560=EDGE_CURVE ( 'NONE', #60098, #3266, #13437, .T. ) ;
#74574=CARTESIAN_POINT ( 'NONE',  ( 3.313708498984756279, 7.999999999999991118, 14.04905278392014978 ) ) ;
#74576=ORIENTED_EDGE ( 'NONE', *, *, #12287, .T. ) ;
#74586=ORIENTED_EDGE ( 'NONE', *, *, #22789, .F. ) ;
#74592=CARTESIAN_POINT ( 'NONE',  ( -7.999999999999991118, 9.797174393178815797E-16, 30.00000000000000000 ) ) ;
#74609=VERTEX_POINT ( 'NONE', #28397 ) ;
#74622=EDGE_LOOP ( 'NONE', ( #36204, #22554, #51833, #60742 ) ) ;
#74625=CARTESIAN_POINT ( 'NONE',  ( 1.320432766682872962E-15, -7.188101187499992051, 6.361552781871754547 ) ) ;
#74636=AXIS2_PLACEMENT_3D ( 'NONE', #72805, #66767, #20735 ) ;
#74707=COLOUR_RGB('Off White',0.89,0.88,0.83);
#74708=FILL_AREA_STYLE_COLOUR('',#74707);
#74709=FILL_AREA_STYLE('',(#74708));
#74710=SURFACE_STYLE_FILL_AREA(#74709);
#74711=SURFACE_SIDE_STYLE('',(#74710));
#74712=SURFACE_STYLE_USAGE(.BOTH.,#74711);
#74713=PRESENTATION_STYLE_ASSIGNMENT((#74712));
ENDSEC;
END-ISO-10303-21;
